ISO-10303-21;
HEADER;
/* Generated by software containing ST-Developer
 * from STEP Tools, Inc. (www.steptools.com) 
 */

FILE_DESCRIPTION(
/* description */ (''),
/* implementation_level */ '2;1');

FILE_NAME(
/* name */ '10_Handwheel_Lock_Screw_ISO_4762_M8x20.step',
/* time_stamp */ '2026-10-26T03:50:32-07:00',
/* author */ (''),
/* organization */ (''),
/* preprocessor_version */ 'ST-DEVELOPER v20.2',
/* originating_system */ 'Autodesk Translation Framework v15.15.0.0',
/* authorisation */ '');

FILE_SCHEMA (('AUTOMOTIVE_DESIGN { 1 0 10303 214 3 1 1 }'));
ENDSEC;

DATA;
#10=MECHANICAL_DESIGN_GEOMETRIC_PRESENTATION_REPRESENTATION('',(#1047),#76660);
#160=B_SPLINE_SURFACE_WITH_KNOTS('',3,3,((#51582,#51583,#51584,#51585,#51586,
#51587,#51588,#51589,#51590,#51591,#51592,#51593,#51594,#51595,#51596,#51597,
#51598,#51599,#51600,#51601,#51602,#51603,#51604,#51605,#51606,#51607,#51608,
#51609,#51610,#51611,#51612,#51613,#51614,#51615,#51616,#51617,#51618,#51619,
#51620,#51621,#51622,#51623,#51624,#51625,#51626,#51627,#51628,#51629,#51630,
#51631,#51632,#51633,#51634,#51635,#51636,#51637,#51638,#51639,#51640,#51641,
#51642,#51643,#51644,#51645,#51646,#51647,#51648,#51649,#51650,#51651,#51652,
#51653,#51654,#51655,#51656,#51657,#51658,#51659,#51660,#51661,#51662,#51663,
#51664,#51665,#51666,#51667,#51668,#51669,#51670,#51671,#51672,#51673,#51674,
#51675,#51676,#51677,#51678,#51679,#51680,#51681,#51682,#51683,#51684),
(#51685,#51686,#51687,#51688,#51689,#51690,#51691,#51692,#51693,#51694,
#51695,#51696,#51697,#51698,#51699,#51700,#51701,#51702,#51703,#51704,#51705,
#51706,#51707,#51708,#51709,#51710,#51711,#51712,#51713,#51714,#51715,#51716,
#51717,#51718,#51719,#51720,#51721,#51722,#51723,#51724,#51725,#51726,#51727,
#51728,#51729,#51730,#51731,#51732,#51733,#51734,#51735,#51736,#51737,#51738,
#51739,#51740,#51741,#51742,#51743,#51744,#51745,#51746,#51747,#51748,#51749,
#51750,#51751,#51752,#51753,#51754,#51755,#51756,#51757,#51758,#51759,#51760,
#51761,#51762,#51763,#51764,#51765,#51766,#51767,#51768,#51769,#51770,#51771,
#51772,#51773,#51774,#51775,#51776,#51777,#51778,#51779,#51780,#51781,#51782,
#51783,#51784,#51785,#51786,#51787),(#51788,#51789,#51790,#51791,#51792,
#51793,#51794,#51795,#51796,#51797,#51798,#51799,#51800,#51801,#51802,#51803,
#51804,#51805,#51806,#51807,#51808,#51809,#51810,#51811,#51812,#51813,#51814,
#51815,#51816,#51817,#51818,#51819,#51820,#51821,#51822,#51823,#51824,#51825,
#51826,#51827,#51828,#51829,#51830,#51831,#51832,#51833,#51834,#51835,#51836,
#51837,#51838,#51839,#51840,#51841,#51842,#51843,#51844,#51845,#51846,#51847,
#51848,#51849,#51850,#51851,#51852,#51853,#51854,#51855,#51856,#51857,#51858,
#51859,#51860,#51861,#51862,#51863,#51864,#51865,#51866,#51867,#51868,#51869,
#51870,#51871,#51872,#51873,#51874,#51875,#51876,#51877,#51878,#51879,#51880,
#51881,#51882,#51883,#51884,#51885,#51886,#51887,#51888,#51889,#51890),
(#51891,#51892,#51893,#51894,#51895,#51896,#51897,#51898,#51899,#51900,
#51901,#51902,#51903,#51904,#51905,#51906,#51907,#51908,#51909,#51910,#51911,
#51912,#51913,#51914,#51915,#51916,#51917,#51918,#51919,#51920,#51921,#51922,
#51923,#51924,#51925,#51926,#51927,#51928,#51929,#51930,#51931,#51932,#51933,
#51934,#51935,#51936,#51937,#51938,#51939,#51940,#51941,#51942,#51943,#51944,
#51945,#51946,#51947,#51948,#51949,#51950,#51951,#51952,#51953,#51954,#51955,
#51956,#51957,#51958,#51959,#51960,#51961,#51962,#51963,#51964,#51965,#51966,
#51967,#51968,#51969,#51970,#51971,#51972,#51973,#51974,#51975,#51976,#51977,
#51978,#51979,#51980,#51981,#51982,#51983,#51984,#51985,#51986,#51987,#51988,
#51989,#51990,#51991,#51992,#51993)),.UNSPECIFIED.,.F.,.F.,.F.,(4,4),(4,
1,1,1,1,1,1,1,1,1,1,1,1,1,1,1,1,1,1,1,1,1,1,1,1,1,1,1,1,1,1,1,1,1,1,1,1,
1,1,1,1,1,1,1,1,1,1,1,1,1,1,1,1,1,1,1,1,1,1,1,1,1,1,1,1,1,1,1,1,1,1,1,1,
1,1,1,1,1,1,1,1,1,1,1,1,1,1,1,1,1,1,1,1,1,1,1,1,1,1,1,4),(0.,0.0820126057383863),
(8.31473274985795,9.30632309046341,10.2979134310689,11.2895037716743,12.2810941122798,
13.2726844528853,14.2642747934907,15.2558651340962,16.2474554747016,17.2390458153071,
18.2306361559126,19.222226496518,20.2138168371235,21.205407177729,22.1969975183344,
23.1885878589399,24.1801781995453,25.1717685401508,26.1633588807563,27.1549492213617,
28.1465395619672,29.1381299025727,30.1297202431781,31.1213105837836,32.112900924389,
33.1044912649945,34.0960816056,35.0876719462054,36.0792622868109,37.0708526274164,
38.0624429680218,39.0540333086273,40.0456236492327,41.0372139898382,42.0288043304437,
43.0203946710491,44.0119850116546,45.0035753522601,45.9951656928655,46.986756033471,
47.9783463740764,48.9699367146819,49.9615270552874,50.9531173958928,51.9447077364983,
52.9362980771037,53.9278884177092,54.9194787583147,55.9110690989201,56.9026594395256,
57.8942497801311,58.8858401207365,59.877430461342,60.8690208019474,61.8606111425529,
62.8522014831584,63.8437918237638,64.8353821643693,65.8269725049748,66.8185628455802,
67.8101531861857,68.8017435267912,69.7933338673966,70.7849242080021,71.7765145486075,
72.768104889213,73.7596952298185,74.7512855704239,75.7428759110294,76.7344662516349,
77.7260565922403,78.7176469328458,79.7092372734512,80.7008276140567,81.6924179546622,
82.6840082952676,83.6755986358731,84.6671889764786,85.658779317084,86.6503696576895,
87.6419599982949,88.6335503389004,89.6251406795059,90.6167310201113,91.6083213607168,
92.5999117013223,93.5915020419277,94.5830923825332,95.5746827231386,96.5662730637441,
97.5578634043496,98.549453744955,99.5410440855605,100.532634426166,101.524224766771,
102.515815107377,103.507405447982,104.498995788588,105.490586129193,106.482176469799,
107.473766810404),.UNSPECIFIED.);
#161=B_SPLINE_SURFACE_WITH_KNOTS('',3,3,((#52148,#52149,#52150,#52151,#52152,
#52153,#52154,#52155,#52156,#52157,#52158,#52159,#52160,#52161,#52162,#52163,
#52164,#52165,#52166,#52167,#52168,#52169,#52170,#52171,#52172,#52173,#52174,
#52175,#52176,#52177,#52178,#52179,#52180,#52181,#52182,#52183,#52184,#52185,
#52186,#52187,#52188,#52189,#52190,#52191,#52192,#52193,#52194,#52195,#52196,
#52197,#52198,#52199,#52200,#52201,#52202,#52203,#52204,#52205,#52206,#52207,
#52208,#52209,#52210,#52211,#52212,#52213,#52214,#52215,#52216,#52217,#52218,
#52219,#52220,#52221,#52222,#52223,#52224,#52225,#52226,#52227,#52228,#52229,
#52230,#52231,#52232,#52233,#52234,#52235,#52236,#52237,#52238,#52239,#52240,
#52241,#52242,#52243,#52244,#52245,#52246,#52247,#52248,#52249,#52250),
(#52251,#52252,#52253,#52254,#52255,#52256,#52257,#52258,#52259,#52260,
#52261,#52262,#52263,#52264,#52265,#52266,#52267,#52268,#52269,#52270,#52271,
#52272,#52273,#52274,#52275,#52276,#52277,#52278,#52279,#52280,#52281,#52282,
#52283,#52284,#52285,#52286,#52287,#52288,#52289,#52290,#52291,#52292,#52293,
#52294,#52295,#52296,#52297,#52298,#52299,#52300,#52301,#52302,#52303,#52304,
#52305,#52306,#52307,#52308,#52309,#52310,#52311,#52312,#52313,#52314,#52315,
#52316,#52317,#52318,#52319,#52320,#52321,#52322,#52323,#52324,#52325,#52326,
#52327,#52328,#52329,#52330,#52331,#52332,#52333,#52334,#52335,#52336,#52337,
#52338,#52339,#52340,#52341,#52342,#52343,#52344,#52345,#52346,#52347,#52348,
#52349,#52350,#52351,#52352,#52353),(#52354,#52355,#52356,#52357,#52358,
#52359,#52360,#52361,#52362,#52363,#52364,#52365,#52366,#52367,#52368,#52369,
#52370,#52371,#52372,#52373,#52374,#52375,#52376,#52377,#52378,#52379,#52380,
#52381,#52382,#52383,#52384,#52385,#52386,#52387,#52388,#52389,#52390,#52391,
#52392,#52393,#52394,#52395,#52396,#52397,#52398,#52399,#52400,#52401,#52402,
#52403,#52404,#52405,#52406,#52407,#52408,#52409,#52410,#52411,#52412,#52413,
#52414,#52415,#52416,#52417,#52418,#52419,#52420,#52421,#52422,#52423,#52424,
#52425,#52426,#52427,#52428,#52429,#52430,#52431,#52432,#52433,#52434,#52435,
#52436,#52437,#52438,#52439,#52440,#52441,#52442,#52443,#52444,#52445,#52446,
#52447,#52448,#52449,#52450,#52451,#52452,#52453,#52454,#52455,#52456),
(#52457,#52458,#52459,#52460,#52461,#52462,#52463,#52464,#52465,#52466,
#52467,#52468,#52469,#52470,#52471,#52472,#52473,#52474,#52475,#52476,#52477,
#52478,#52479,#52480,#52481,#52482,#52483,#52484,#52485,#52486,#52487,#52488,
#52489,#52490,#52491,#52492,#52493,#52494,#52495,#52496,#52497,#52498,#52499,
#52500,#52501,#52502,#52503,#52504,#52505,#52506,#52507,#52508,#52509,#52510,
#52511,#52512,#52513,#52514,#52515,#52516,#52517,#52518,#52519,#52520,#52521,
#52522,#52523,#52524,#52525,#52526,#52527,#52528,#52529,#52530,#52531,#52532,
#52533,#52534,#52535,#52536,#52537,#52538,#52539,#52540,#52541,#52542,#52543,
#52544,#52545,#52546,#52547,#52548,#52549,#52550,#52551,#52552,#52553,#52554,
#52555,#52556,#52557,#52558,#52559)),.UNSPECIFIED.,.F.,.F.,.F.,(4,4),(4,
1,1,1,1,1,1,1,1,1,1,1,1,1,1,1,1,1,1,1,1,1,1,1,1,1,1,1,1,1,1,1,1,1,1,1,1,
1,1,1,1,1,1,1,1,1,1,1,1,1,1,1,1,1,1,1,1,1,1,1,1,1,1,1,1,1,1,1,1,1,1,1,1,
1,1,1,1,1,1,1,1,1,1,1,1,1,1,1,1,1,1,1,1,1,1,1,1,1,1,1,4),(0.,0.0820126057383863),
(11.6152142277546,12.6068045683601,13.5983949089656,14.589985249571,15.5815755901765,
16.573165930782,17.5647562713874,18.5563466119929,19.5479369525983,20.5395272932038,
21.5311176338093,22.5227079744147,23.5142983150202,24.5058886556257,25.4974789962311,
26.4890693368366,27.480659677442,28.4722500180475,29.463840358653,30.4554306992584,
31.4470210398639,32.4386113804694,33.4302017210748,34.4217920616803,35.4133824022857,
36.4049727428912,37.3965630834967,38.3881534241021,39.3797437647076,40.3713341053131,
41.3629244459185,42.354514786524,43.3461051271294,44.3376954677349,45.3292858083404,
46.3208761489458,47.3124664895513,48.3040568301568,49.2956471707622,50.2872375113677,
51.2788278519731,52.2704181925786,53.2620085331841,54.2535988737895,55.245189214395,
56.2367795550005,57.2283698956059,58.2199602362114,59.2115505768168,60.2031409174223,
61.1947312580278,62.1863215986332,63.1779119392387,64.1695022798442,65.1610926204496,
66.1526829610551,67.1442733016605,68.135863642266,69.1274539828715,70.1190443234769,
71.1106346640824,72.1022250046879,73.0938153452933,74.0854056858988,75.0769960265042,
76.0685863671097,77.0601767077152,78.0517670483206,79.0433573889261,80.0349477295316,
81.026538070137,82.0181284107425,83.0097187513479,84.0013090919534,84.9928994325589,
85.9844897731643,86.9760801137698,87.9676704543753,88.9592607949807,89.9508511355862,
90.9424414761916,91.9340318167971,92.9256221574026,93.917212498008,94.9088028386135,
95.900393179219,96.8919835198244,97.8835738604299,98.8751642010353,99.8667545416408,
100.858344882246,101.849935222852,102.841525563457,103.833115904063,104.824706244668,
105.816296585274,106.807886925879,107.799477266485,108.79106760709,109.782657947695,
110.774248288301),.UNSPECIFIED.);
#441=B_SPLINE_CURVE_WITH_KNOTS('',3,(#50317,#50318,#50319,#50320,#50321,
#50322,#50323,#50324,#50325,#50326),.UNSPECIFIED.,.F.,.F.,(4,3,3,4),(-4.09274904019425,
-3.96636136242185,-2.97477102181639,-2.06120159751579),.UNSPECIFIED.);
#442=B_SPLINE_CURVE_WITH_KNOTS('',3,(#50329,#50330,#50331,#50332,#50333,
#50334,#50335),.UNSPECIFIED.,.F.,.F.,(4,3,4),(0.,0.991590340605456,1.11004521091126),
 .UNSPECIFIED.);
#443=B_SPLINE_CURVE_WITH_KNOTS('',3,(#50340,#50341,#50342,#50343,#50344,
#50345,#50346,#50347,#50348,#50349,#50350,#50351,#50352,#50353,#50354,#50355,
#50356,#50357,#50358,#50359,#50360,#50361),.UNSPECIFIED.,.F.,.F.,(4,3,3,
3,3,3,3,4),(-10.3759343473738,-9.91590340605462,-8.92431306544916,-7.9327227248437,
-6.94113238423824,-5.94954204363277,-4.95795170302731,-4.09274904019425),
 .UNSPECIFIED.);
#444=B_SPLINE_CURVE_WITH_KNOTS('',3,(#50362,#50363,#50364,#50365,#50366,
#50367,#50368,#50369,#50370,#50371,#50372,#50373,#50374,#50375,#50376,#50377,
#50378,#50379,#50380,#50381,#50382,#50383),.UNSPECIFIED.,.F.,.F.,(4,3,3,
3,3,3,3,4),(1.11004521091126,1.98318068121092,2.97477102181639,3.96636136242185,
4.95795170302731,5.94954204363278,6.94113238423824,7.39323051809085),
 .UNSPECIFIED.);
#445=B_SPLINE_CURVE_WITH_KNOTS('',3,(#50388,#50389,#50390,#50391,#50392,
#50393,#50394,#50395,#50396,#50397,#50398,#50399,#50400,#50401,#50402,#50403,
#50404,#50405,#50406,#50407,#50408,#50409),.UNSPECIFIED.,.F.,.F.,(4,3,3,
3,3,3,3,4),(-16.6591196545534,-15.8654454496874,-14.8738551090819,-13.8822647684765,
-12.890674427871,-11.8990840872655,-10.9074937466601,-10.3759343473738),
 .UNSPECIFIED.);
#446=B_SPLINE_CURVE_WITH_KNOTS('',3,(#50410,#50411,#50412,#50413,#50414,
#50415,#50416,#50417,#50418,#50419,#50420,#50421,#50422,#50423,#50424,#50425,
#50426,#50427,#50428,#50429,#50430,#50431),.UNSPECIFIED.,.F.,.F.,(4,3,3,
3,3,3,3,4),(7.39323051809085,7.9327227248437,8.92431306544916,9.91590340605462,
10.9074937466601,11.8990840872655,12.890674427871,13.6764158252704),
 .UNSPECIFIED.);
#447=B_SPLINE_CURVE_WITH_KNOTS('',3,(#50436,#50437,#50438,#50439,#50440,
#50441,#50442,#50443,#50444,#50445,#50446,#50447,#50448,#50449,#50450,#50451,
#50452,#50453,#50454,#50455,#50456,#50457,#50458,#50459,#50460),
 .UNSPECIFIED.,.F.,.F.,(4,3,3,3,3,3,3,3,4),(-22.942304961733,-22.8065778339256,
-21.8149874933202,-20.8233971527147,-19.8318068121092,-18.8402164715038,
-17.8486261308983,-16.8570357902929,-16.6591196545534),.UNSPECIFIED.);
#448=B_SPLINE_CURVE_WITH_KNOTS('',3,(#50461,#50462,#50463,#50464,#50465,
#50466,#50467,#50468,#50469,#50470,#50471,#50472,#50473,#50474,#50475,#50476,
#50477,#50478,#50479,#50480,#50481,#50482,#50483,#50484,#50485),
 .UNSPECIFIED.,.F.,.F.,(4,3,3,3,3,3,3,3,4),(13.6764158252704,13.8822647684765,
14.8738551090819,15.8654454496874,16.8570357902929,17.8486261308983,18.8402164715038,
19.8318068121093,19.95960113245),.UNSPECIFIED.);
#449=B_SPLINE_CURVE_WITH_KNOTS('',3,(#50490,#50491,#50492,#50493,#50494,
#50495,#50496,#50497,#50498,#50499,#50500,#50501,#50502,#50503,#50504,#50505,
#50506,#50507,#50508,#50509,#50510,#50511),.UNSPECIFIED.,.F.,.F.,(4,3,3,
3,3,3,3,4),(-29.2254902689126,-28.7561198775584,-27.7645295369529,-26.7729391963475,
-25.781348855742,-24.7897585151366,-23.7981681745311,-22.942304961733),
 .UNSPECIFIED.);
#450=B_SPLINE_CURVE_WITH_KNOTS('',3,(#50512,#50513,#50514,#50515,#50516,
#50517,#50518,#50519,#50520,#50521,#50522,#50523,#50524,#50525,#50526,#50527,
#50528,#50529,#50530,#50531,#50532,#50533),.UNSPECIFIED.,.F.,.F.,(4,3,3,
3,3,3,3,4),(19.95960113245,20.8233971527147,21.8149874933202,22.8065778339256,
23.7981681745311,24.7897585151366,25.781348855742,26.2427864396296),
 .UNSPECIFIED.);
#451=B_SPLINE_CURVE_WITH_KNOTS('',3,(#50538,#50539,#50540,#50541,#50542,
#50543,#50544,#50545,#50546,#50547,#50548,#50549,#50550,#50551,#50552,#50553,
#50554,#50555,#50556,#50557,#50558,#50559),.UNSPECIFIED.,.F.,.F.,(4,3,3,
3,3,3,3,4),(-35.5086755760922,-34.7056619211912,-33.7140715805857,-32.7224812399803,
-31.7308908993748,-30.7393005587693,-29.7477102181639,-29.2254902689126),
 .UNSPECIFIED.);
#452=B_SPLINE_CURVE_WITH_KNOTS('',3,(#50560,#50561,#50562,#50563,#50564,
#50565,#50566,#50567,#50568,#50569,#50570,#50571,#50572,#50573,#50574,#50575,
#50576,#50577,#50578,#50579,#50580,#50581),.UNSPECIFIED.,.F.,.F.,(4,3,3,
3,3,3,3,4),(26.2427864396296,26.7729391963475,27.7645295369529,28.7561198775584,
29.7477102181639,30.7393005587693,31.7308908993748,32.5259717468092),
 .UNSPECIFIED.);
#453=B_SPLINE_CURVE_WITH_KNOTS('',3,(#50586,#50587,#50588,#50589,#50590,
#50591,#50592,#50593,#50594,#50595,#50596,#50597,#50598,#50599,#50600,#50601,
#50602,#50603,#50604,#50605,#50606,#50607,#50608,#50609,#50610),
 .UNSPECIFIED.,.F.,.F.,(4,3,3,3,3,3,3,3,4),(-41.7918608832718,-41.6467943054294,
-40.655203964824,-39.6636136242185,-38.672023283613,-37.6804329430076,-36.6888426024021,
-35.6972522617966,-35.5086755760922),.UNSPECIFIED.);
#454=B_SPLINE_CURVE_WITH_KNOTS('',3,(#50611,#50612,#50613,#50614,#50615,
#50616,#50617,#50618,#50619,#50620,#50621,#50622,#50623,#50624,#50625,#50626,
#50627,#50628,#50629,#50630,#50631,#50632,#50633,#50634,#50635),
 .UNSPECIFIED.,.F.,.F.,(4,3,3,3,3,3,3,3,4),(32.5259717468092,32.7224812399802,
33.7140715805857,34.7056619211912,35.6972522617966,36.6888426024021,37.6804329430076,
38.672023283613,38.8091570539888),.UNSPECIFIED.);
#455=B_SPLINE_CURVE_WITH_KNOTS('',3,(#50640,#50641,#50642,#50643,#50644,
#50645,#50646,#50647,#50648,#50649,#50650,#50651,#50652,#50653,#50654,#50655,
#50656,#50657,#50658,#50659,#50660,#50661),.UNSPECIFIED.,.F.,.F.,(4,3,3,
3,3,3,3,4),(-48.0750461904514,-47.5963363490622,-46.6047460084567,-45.6131556678513,
-44.6215653272458,-43.6299749866404,-42.6383846460349,-41.7918608832718),
 .UNSPECIFIED.);
#456=B_SPLINE_CURVE_WITH_KNOTS('',3,(#50662,#50663,#50664,#50665,#50666,
#50667,#50668,#50669,#50670,#50671,#50672,#50673,#50674,#50675,#50676,#50677,
#50678,#50679,#50680,#50681,#50682,#50683),.UNSPECIFIED.,.F.,.F.,(4,3,3,
3,3,3,3,4),(38.8091570539888,39.6636136242185,40.6552039648239,41.6467943054294,
42.6383846460349,43.6299749866403,44.6215653272458,45.0923423611684),
 .UNSPECIFIED.);
#457=B_SPLINE_CURVE_WITH_KNOTS('',3,(#50688,#50689,#50690,#50691,#50692,
#50693,#50694,#50695,#50696,#50697,#50698,#50699,#50700,#50701,#50702,#50703,
#50704,#50705,#50706,#50707,#50708,#50709),.UNSPECIFIED.,.F.,.F.,(4,3,3,
3,3,3,3,4),(-54.358231497631,-53.545878392695,-52.5542880520895,-51.5626977114841,
-50.5711073708786,-49.5795170302731,-48.5879266896677,-48.0750461904514),
 .UNSPECIFIED.);
#458=B_SPLINE_CURVE_WITH_KNOTS('',3,(#50710,#50711,#50712,#50713,#50714,
#50715,#50716,#50717,#50718,#50719,#50720,#50721,#50722,#50723,#50724,#50725,
#50726,#50727,#50728,#50729,#50730,#50731),.UNSPECIFIED.,.F.,.F.,(4,3,3,
3,3,3,3,4),(45.0923423611684,45.6131556678513,46.6047460084567,47.5963363490622,
48.5879266896676,49.5795170302731,50.5711073708786,51.375527668348),
 .UNSPECIFIED.);
#459=B_SPLINE_CURVE_WITH_KNOTS('',3,(#50736,#50737,#50738,#50739,#50740,
#50741,#50742,#50743,#50744,#50745,#50746,#50747,#50748,#50749,#50750,#50751,
#50752,#50753,#50754,#50755,#50756,#50757,#50758,#50759,#50760),
 .UNSPECIFIED.,.F.,.F.,(4,3,3,3,3,3,3,3,4),(-60.6414168048105,-60.4870107769332,
-59.4954204363278,-58.5038300957223,-57.5122397551168,-56.5206494145114,
-55.5290590739059,-54.5374687333004,-54.358231497631),.UNSPECIFIED.);
#460=B_SPLINE_CURVE_WITH_KNOTS('',3,(#50761,#50762,#50763,#50764,#50765,
#50766,#50767,#50768,#50769,#50770,#50771,#50772,#50773,#50774,#50775,#50776,
#50777,#50778,#50779,#50780,#50781,#50782,#50783,#50784,#50785),
 .UNSPECIFIED.,.F.,.F.,(4,3,3,3,3,3,3,3,4),(51.375527668348,51.562697711484,
52.5542880520895,53.545878392695,54.5374687333004,55.5290590739059,56.5206494145114,
57.5122397551168,57.6587129755276),.UNSPECIFIED.);
#461=B_SPLINE_CURVE_WITH_KNOTS('',3,(#50790,#50791,#50792,#50793,#50794,
#50795,#50796,#50797,#50798,#50799,#50800,#50801,#50802,#50803,#50804,#50805,
#50806,#50807,#50808,#50809,#50810,#50811),.UNSPECIFIED.,.F.,.F.,(4,3,3,
3,3,3,3,4),(-66.9246021119901,-66.436552820566,-65.4449624799605,-64.4533721393551,
-63.4617817987496,-62.4701914581441,-61.4786011175387,-60.6414168048105),
 .UNSPECIFIED.);
#462=B_SPLINE_CURVE_WITH_KNOTS('',3,(#50812,#50813,#50814,#50815,#50816,
#50817,#50818,#50819,#50820,#50821,#50822,#50823,#50824,#50825,#50826,#50827,
#50828,#50829,#50830,#50831,#50832,#50833),.UNSPECIFIED.,.F.,.F.,(4,3,3,
3,3,3,3,4),(57.6587129755276,58.5038300957223,59.4954204363277,60.4870107769332,
61.4786011175387,62.4701914581441,63.4617817987496,63.9418982827072),
 .UNSPECIFIED.);
#463=B_SPLINE_CURVE_WITH_KNOTS('',3,(#50838,#50839,#50840,#50841,#50842,
#50843,#50844,#50845,#50846,#50847,#50848,#50849,#50850,#50851,#50852,#50853,
#50854,#50855,#50856,#50857,#50858,#50859),.UNSPECIFIED.,.F.,.F.,(4,3,3,
3,3,3,3,4),(-73.2077874191697,-72.3860948641988,-71.3945045235933,-70.4029141829878,
-69.4113238423824,-68.4197335017769,-67.4281431611715,-66.9246021119901),
 .UNSPECIFIED.);
#464=B_SPLINE_CURVE_WITH_KNOTS('',3,(#50860,#50861,#50862,#50863,#50864,
#50865,#50866,#50867,#50868,#50869,#50870,#50871,#50872,#50873,#50874,#50875,
#50876,#50877,#50878,#50879,#50880,#50881),.UNSPECIFIED.,.F.,.F.,(4,3,3,
3,3,3,3,4),(63.9418982827072,64.4533721393551,65.4449624799605,66.436552820566,
67.4281431611714,68.4197335017769,69.4113238423824,70.2250835898868),
 .UNSPECIFIED.);
#465=B_SPLINE_CURVE_WITH_KNOTS('',3,(#50886,#50887,#50888,#50889,#50890,
#50891,#50892,#50893,#50894,#50895,#50896,#50897,#50898,#50899,#50900,#50901,
#50902,#50903,#50904,#50905,#50906,#50907,#50908,#50909,#50910),
 .UNSPECIFIED.,.F.,.F.,(4,3,3,3,3,3,3,3,4),(-79.4909727263493,-79.327227248437,
-78.3356369078316,-77.3440465672261,-76.3524562266206,-75.3608658860151,
-74.3692755454097,-73.3776852048042,-73.2077874191697),.UNSPECIFIED.);
#466=B_SPLINE_CURVE_WITH_KNOTS('',3,(#50911,#50912,#50913,#50914,#50915,
#50916,#50917,#50918,#50919,#50920,#50921,#50922,#50923,#50924,#50925,#50926,
#50927,#50928,#50929,#50930,#50931,#50932,#50933,#50934,#50935),
 .UNSPECIFIED.,.F.,.F.,(4,3,3,3,3,3,3,3,4),(70.2250835898868,70.4029141829878,
71.3945045235933,72.3860948641988,73.3776852048042,74.3692755454097,75.3608658860151,
76.3524562266206,76.5082688970663),.UNSPECIFIED.);
#467=B_SPLINE_CURVE_WITH_KNOTS('',3,(#50940,#50941,#50942,#50943,#50944,
#50945,#50946,#50947,#50948,#50949,#50950,#50951,#50952,#50953,#50954,#50955,
#50956,#50957,#50958,#50959,#50960,#50961),.UNSPECIFIED.,.F.,.F.,(4,3,3,
3,3,3,3,4),(-85.7741580335289,-85.2767692920698,-84.2851789514643,-83.2935886108589,
-82.3019982702534,-81.3104079296479,-80.3188175890425,-79.4909727263493),
 .UNSPECIFIED.);
#468=B_SPLINE_CURVE_WITH_KNOTS('',3,(#50962,#50963,#50964,#50965,#50966,
#50967,#50968,#50969,#50970,#50971,#50972,#50973,#50974,#50975,#50976,#50977,
#50978,#50979,#50980,#50981,#50982,#50983),.UNSPECIFIED.,.F.,.F.,(4,3,3,
3,3,3,3,4),(76.5082688970663,77.3440465672261,78.3356369078315,79.327227248437,
80.3188175890425,81.3104079296479,82.3019982702534,82.7914542042459),
 .UNSPECIFIED.);
#469=B_SPLINE_CURVE_WITH_KNOTS('',3,(#50988,#50989,#50990,#50991,#50992,
#50993,#50994,#50995,#50996,#50997,#50998,#50999,#51000,#51001,#51002,#51003,
#51004,#51005,#51006,#51007,#51008,#51009),.UNSPECIFIED.,.F.,.F.,(4,3,3,
3,3,3,3,4),(-92.0573433407085,-91.2263113357026,-90.2347209950971,-89.2431306544916,
-88.2515403138862,-87.2599499732807,-86.2683596326753,-85.7741580335289),
 .UNSPECIFIED.);
#470=B_SPLINE_CURVE_WITH_KNOTS('',3,(#51010,#51011,#51012,#51013,#51014,
#51015,#51016,#51017,#51018,#51019,#51020,#51021,#51022,#51023,#51024,#51025,
#51026,#51027,#51028,#51029,#51030,#51031),.UNSPECIFIED.,.F.,.F.,(4,3,3,
3,3,3,3,4),(82.7914542042459,83.2935886108588,84.2851789514643,85.2767692920698,
86.2683596326752,87.2599499732807,88.2515403138862,89.0746395114255),
 .UNSPECIFIED.);
#471=B_SPLINE_CURVE_WITH_KNOTS('',3,(#51036,#51037,#51038,#51039,#51040,
#51041,#51042,#51043,#51044,#51045,#51046,#51047,#51048,#51049,#51050,#51051,
#51052,#51053,#51054,#51055,#51056,#51057,#51058,#51059,#51060),
 .UNSPECIFIED.,.F.,.F.,(4,3,3,3,3,3,3,3,4),(-98.3405286478881,-98.1674437199408,
-97.1758533793353,-96.1842630387299,-95.1926726981244,-94.201082357519,
-93.2094920169135,-92.217901676308,-92.0573433407085),.UNSPECIFIED.);
#472=B_SPLINE_CURVE_WITH_KNOTS('',3,(#51061,#51062,#51063,#51064,#51065,
#51066,#51067,#51068,#51069,#51070,#51071,#51072,#51073,#51074,#51075,#51076,
#51077,#51078,#51079,#51080,#51081,#51082,#51083,#51084,#51085),
 .UNSPECIFIED.,.F.,.F.,(4,3,3,3,3,3,3,3,4),(89.0746395114255,89.2431306544916,
90.2347209950971,91.2263113357025,92.217901676308,93.2094920169135,94.2010823575189,
95.1926726981244,95.3578248186051),.UNSPECIFIED.);
#473=B_SPLINE_CURVE_WITH_KNOTS('',3,(#51091,#51092,#51093,#51094,#51095,
#51096,#51097,#51098,#51099),.UNSPECIFIED.,.F.,.F.,(4,1,1,1,1,1,4),(103.672557568463,
103.833115904063,104.824706244668,105.816296585274,106.807886925879,107.799477266485,
108.713046690785),.UNSPECIFIED.);
#474=B_SPLINE_CURVE_WITH_KNOTS('',3,(#51102,#51103,#51104,#51105,#51106,
#51107,#51108),.UNSPECIFIED.,.F.,.F.,(4,1,1,1,4),(103.672557568463,104.498995788588,
105.490586129193,106.482176469799,107.473766810404),.UNSPECIFIED.);
#475=B_SPLINE_CURVE_WITH_KNOTS('',3,(#51113,#51114,#51115,#51116,#51117,
#51118,#51119,#51120,#51121,#51122),.UNSPECIFIED.,.F.,.F.,(4,1,1,1,1,1,
1,4),(97.3893722612836,97.8835738604299,98.8751642010353,99.8667545416408,
100.858344882246,101.849935222852,102.841525563457,103.672557568463),
 .UNSPECIFIED.);
#476=B_SPLINE_CURVE_WITH_KNOTS('',3,(#51123,#51124,#51125,#51126,#51127,
#51128,#51129,#51130,#51131,#51132,#51133),.UNSPECIFIED.,.F.,.F.,(4,1,1,
1,1,1,1,1,4),(97.3893722612836,97.5578634043496,98.549453744955,99.5410440855605,
100.532634426166,101.524224766771,102.515815107377,103.507405447982,103.672557568463),
 .UNSPECIFIED.);
#477=B_SPLINE_CURVE_WITH_KNOTS('',3,(#51138,#51139,#51140,#51141,#51142,
#51143,#51144,#51145,#51146,#51147),.UNSPECIFIED.,.F.,.F.,(4,1,1,1,1,1,
1,4),(91.106186954104,91.9340318167971,92.9256221574026,93.917212498008,
94.9088028386135,95.900393179219,96.8919835198244,97.3893722612836),
 .UNSPECIFIED.);
#478=B_SPLINE_CURVE_WITH_KNOTS('',3,(#51148,#51149,#51150,#51151,#51152,
#51153,#51154,#51155,#51156,#51157),.UNSPECIFIED.,.F.,.F.,(4,1,1,1,1,1,
1,4),(91.106186954104,91.6083213607168,92.5999117013223,93.5915020419277,
94.5830923825332,95.5746827231386,96.5662730637441,97.3893722612836),
 .UNSPECIFIED.);
#479=B_SPLINE_CURVE_WITH_KNOTS('',3,(#51162,#51163,#51164,#51165,#51166,
#51167,#51168,#51169,#51170,#51171,#51172),.UNSPECIFIED.,.F.,.F.,(4,1,1,
1,1,1,1,1,4),(84.8230016469244,84.9928994325589,85.9844897731643,86.9760801137698,
87.9676704543753,88.9592607949807,89.9508511355862,90.9424414761916,91.106186954104),
 .UNSPECIFIED.);
#480=B_SPLINE_CURVE_WITH_KNOTS('',3,(#51173,#51174,#51175,#51176,#51177,
#51178,#51179,#51180,#51181,#51182),.UNSPECIFIED.,.F.,.F.,(4,1,1,1,1,1,
1,4),(84.8230016469244,85.658779317084,86.6503696576895,87.6419599982949,
88.6335503389004,89.6251406795059,90.6167310201113,91.106186954104),
 .UNSPECIFIED.);
#481=B_SPLINE_CURVE_WITH_KNOTS('',3,(#51187,#51188,#51189,#51190,#51191,
#51192,#51193,#51194,#51195,#51196),.UNSPECIFIED.,.F.,.F.,(4,1,1,1,1,1,
1,4),(78.5398163397448,79.0433573889261,80.0349477295316,81.026538070137,
82.0181284107425,83.0097187513479,84.0013090919534,84.8230016469244),
 .UNSPECIFIED.);
#482=B_SPLINE_CURVE_WITH_KNOTS('',3,(#51197,#51198,#51199,#51200,#51201,
#51202,#51203,#51204,#51205,#51206,#51207),.UNSPECIFIED.,.F.,.F.,(4,1,1,
1,1,1,1,1,4),(78.5398163397448,78.7176469328458,79.7092372734512,80.7008276140567,
81.6924179546622,82.6840082952676,83.6755986358731,84.6671889764786,84.8230016469244),
 .UNSPECIFIED.);
#483=B_SPLINE_CURVE_WITH_KNOTS('',3,(#51212,#51213,#51214,#51215,#51216,
#51217,#51218,#51219,#51220,#51221),.UNSPECIFIED.,.F.,.F.,(4,1,1,1,1,1,
1,4),(72.2566310325652,73.0938153452933,74.0854056858988,75.0769960265042,
76.0685863671097,77.0601767077152,78.0517670483206,78.5398163397448),
 .UNSPECIFIED.);
#484=B_SPLINE_CURVE_WITH_KNOTS('',3,(#51222,#51223,#51224,#51225,#51226,
#51227,#51228,#51229,#51230,#51231),.UNSPECIFIED.,.F.,.F.,(4,1,1,1,1,1,
1,4),(72.2566310325652,72.768104889213,73.7596952298185,74.7512855704239,
75.7428759110294,76.7344662516349,77.7260565922403,78.5398163397448),
 .UNSPECIFIED.);
#485=B_SPLINE_CURVE_WITH_KNOTS('',3,(#51236,#51237,#51238,#51239,#51240,
#51241,#51242,#51243,#51244,#51245,#51246),.UNSPECIFIED.,.F.,.F.,(4,1,1,
1,1,1,1,1,4),(65.9734457253856,66.1526829610551,67.1442733016605,68.135863642266,
69.1274539828715,70.1190443234769,71.1106346640824,72.1022250046879,72.2566310325652),
 .UNSPECIFIED.);
#486=B_SPLINE_CURVE_WITH_KNOTS('',3,(#51247,#51248,#51249,#51250,#51251,
#51252,#51253,#51254,#51255,#51256),.UNSPECIFIED.,.F.,.F.,(4,1,1,1,1,1,
1,4),(65.9734457253856,66.8185628455802,67.8101531861857,68.8017435267912,
69.7933338673966,70.7849242080021,71.7765145486075,72.2566310325652),
 .UNSPECIFIED.);
#487=B_SPLINE_CURVE_WITH_KNOTS('',3,(#51261,#51262,#51263,#51264,#51265,
#51266,#51267,#51268,#51269,#51270),.UNSPECIFIED.,.F.,.F.,(4,1,1,1,1,1,
1,4),(59.690260418206,60.2031409174223,61.1947312580278,62.1863215986332,
63.1779119392387,64.1695022798442,65.1610926204496,65.9734457253856),
 .UNSPECIFIED.);
#488=B_SPLINE_CURVE_WITH_KNOTS('',3,(#51271,#51272,#51273,#51274,#51275,
#51276,#51277,#51278,#51279,#51280,#51281),.UNSPECIFIED.,.F.,.F.,(4,1,1,
1,1,1,1,1,4),(59.690260418206,59.877430461342,60.8690208019474,61.8606111425529,
62.8522014831584,63.8437918237638,64.8353821643693,65.8269725049748,65.9734457253856),
 .UNSPECIFIED.);
#489=B_SPLINE_CURVE_WITH_KNOTS('',3,(#51286,#51287,#51288,#51289,#51290,
#51291,#51292,#51293,#51294,#51295),.UNSPECIFIED.,.F.,.F.,(4,1,1,1,1,1,
1,4),(53.4070751110264,54.2535988737895,55.245189214395,56.2367795550005,
57.2283698956059,58.2199602362114,59.2115505768168,59.690260418206),
 .UNSPECIFIED.);
#490=B_SPLINE_CURVE_WITH_KNOTS('',3,(#51296,#51297,#51298,#51299,#51300,
#51301,#51302,#51303,#51304,#51305),.UNSPECIFIED.,.F.,.F.,(4,1,1,1,1,1,
1,4),(53.4070751110264,53.9278884177092,54.9194787583147,55.9110690989201,
56.9026594395256,57.8942497801311,58.8858401207365,59.690260418206),
 .UNSPECIFIED.);
#491=B_SPLINE_CURVE_WITH_KNOTS('',3,(#51310,#51311,#51312,#51313,#51314,
#51315,#51316,#51317,#51318,#51319,#51320),.UNSPECIFIED.,.F.,.F.,(4,1,1,
1,1,1,1,1,4),(47.1238898038469,47.3124664895513,48.3040568301568,49.2956471707622,
50.2872375113677,51.2788278519731,52.2704181925786,53.2620085331841,53.4070751110264),
 .UNSPECIFIED.);
#492=B_SPLINE_CURVE_WITH_KNOTS('',3,(#51321,#51322,#51323,#51324,#51325,
#51326,#51327,#51328,#51329,#51330),.UNSPECIFIED.,.F.,.F.,(4,1,1,1,1,1,
1,4),(47.1238898038468,47.9783463740764,48.9699367146819,49.9615270552874,
50.9531173958928,51.9447077364983,52.9362980771037,53.4070751110264),
 .UNSPECIFIED.);
#493=B_SPLINE_CURVE_WITH_KNOTS('',3,(#51335,#51336,#51337,#51338,#51339,
#51340,#51341,#51342,#51343,#51344),.UNSPECIFIED.,.F.,.F.,(4,1,1,1,1,1,
1,4),(40.8407044966673,41.3629244459185,42.354514786524,43.3461051271294,
44.3376954677349,45.3292858083404,46.3208761489458,47.1238898038469),
 .UNSPECIFIED.);
#494=B_SPLINE_CURVE_WITH_KNOTS('',3,(#51345,#51346,#51347,#51348,#51349,
#51350,#51351,#51352,#51353,#51354,#51355),.UNSPECIFIED.,.F.,.F.,(4,1,1,
1,1,1,1,1,4),(40.8407044966672,41.0372139898382,42.0288043304437,43.0203946710491,
44.0119850116546,45.0035753522601,45.9951656928655,46.986756033471,47.1238898038468),
 .UNSPECIFIED.);
#495=B_SPLINE_CURVE_WITH_KNOTS('',3,(#51360,#51361,#51362,#51363,#51364,
#51365,#51366,#51367,#51368,#51369),.UNSPECIFIED.,.F.,.F.,(4,1,1,1,1,1,
1,4),(34.5575191894877,35.4133824022857,36.4049727428912,37.3965630834967,
38.3881534241021,39.3797437647076,40.3713341053131,40.8407044966673),
 .UNSPECIFIED.);
#496=B_SPLINE_CURVE_WITH_KNOTS('',3,(#51370,#51371,#51372,#51373,#51374,
#51375,#51376,#51377,#51378,#51379),.UNSPECIFIED.,.F.,.F.,(4,1,1,1,1,1,
1,4),(34.5575191894877,35.0876719462054,36.0792622868109,37.0708526274164,
38.0624429680218,39.0540333086273,40.0456236492327,40.8407044966672),
 .UNSPECIFIED.);
#497=B_SPLINE_CURVE_WITH_KNOTS('',3,(#51384,#51385,#51386,#51387,#51388,
#51389,#51390,#51391,#51392,#51393,#51394),.UNSPECIFIED.,.F.,.F.,(4,1,1,
1,1,1,1,1,4),(28.2743338823081,28.4722500180475,29.463840358653,30.4554306992584,
31.4470210398639,32.4386113804694,33.4302017210748,34.4217920616803,34.5575191894877),
 .UNSPECIFIED.);
#498=B_SPLINE_CURVE_WITH_KNOTS('',3,(#51395,#51396,#51397,#51398,#51399,
#51400,#51401,#51402,#51403,#51404),.UNSPECIFIED.,.F.,.F.,(4,1,1,1,1,1,
1,4),(28.2743338823081,29.1381299025727,30.1297202431781,31.1213105837836,
32.112900924389,33.1044912649945,34.0960816056,34.5575191894877),
 .UNSPECIFIED.);
#499=B_SPLINE_CURVE_WITH_KNOTS('',3,(#51409,#51410,#51411,#51412,#51413,
#51414,#51415,#51416,#51417,#51418),.UNSPECIFIED.,.F.,.F.,(4,1,1,1,1,1,
1,4),(21.9911485751285,22.5227079744147,23.5142983150202,24.5058886556257,
25.4974789962311,26.4890693368366,27.480659677442,28.2743338823081),
 .UNSPECIFIED.);
#500=B_SPLINE_CURVE_WITH_KNOTS('',3,(#51419,#51420,#51421,#51422,#51423,
#51424,#51425,#51426,#51427,#51428,#51429),.UNSPECIFIED.,.F.,.F.,(4,1,1,
1,1,1,1,1,4),(21.9911485751285,22.1969975183344,23.1885878589399,24.1801781995453,
25.1717685401508,26.1633588807563,27.1549492213617,28.1465395619672,28.2743338823081),
 .UNSPECIFIED.);
#501=B_SPLINE_CURVE_WITH_KNOTS('',3,(#51434,#51435,#51436,#51437,#51438,
#51439,#51440,#51441,#51442,#51443),.UNSPECIFIED.,.F.,.F.,(4,1,1,1,1,1,
1,4),(15.7079632679489,16.573165930782,17.5647562713874,18.5563466119929,
19.5479369525983,20.5395272932038,21.5311176338093,21.9911485751285),
 .UNSPECIFIED.);
#502=B_SPLINE_CURVE_WITH_KNOTS('',3,(#51444,#51445,#51446,#51447,#51448,
#51449,#51450,#51451,#51452,#51453),.UNSPECIFIED.,.F.,.F.,(4,1,1,1,1,1,
1,4),(15.7079632679489,16.2474554747016,17.2390458153071,18.2306361559126,
19.222226496518,20.2138168371235,21.205407177729,21.9911485751285),
 .UNSPECIFIED.);
#503=B_SPLINE_CURVE_WITH_KNOTS('',3,(#51456,#51457,#51458,#51459,#51460,
#51461,#51462,#51463,#51464,#51465,#51466,#51467,#51468,#51469,#51470,#51471,
#51472,#51473,#51474,#51475,#51476,#51477,#51478,#51479,#51480,#51481,#51482,
#51483,#51484,#51485,#51486,#51487,#51488,#51489,#51490,#51491,#51492,#51493,
#51494,#51495,#51496,#51497,#51498,#51499,#51500,#51501,#51502,#51503,#51504,
#51505,#51506,#51507,#51508,#51509,#51510,#51511,#51512,#51513,#51514,#51515,
#51516),.UNSPECIFIED.,.F.,.F.,(4,3,3,3,3,3,3,3,3,3,3,3,3,3,3,3,3,3,3,3,
4),(-0.744397949170491,-0.718888480435814,-0.671065586721542,-0.646483273340718,
-0.600248581890479,-0.572968698430621,-0.555731357696308,-0.495420255894194,
-0.456580299181414,-0.439125670228373,-0.423945368768442,-0.376189396302194,
-0.32916572176442,-0.306302680888458,-0.285176397353076,-0.222891638647477,
-0.167168728985607,-0.151663890453069,-0.134867149404615,-0.0674335747023076,
0.),.UNSPECIFIED.);
#504=B_SPLINE_CURVE_WITH_KNOTS('',3,(#51521,#51522,#51523,#51524,#51525,
#51526,#51527,#51528,#51529,#51530,#51531,#51532,#51533,#51534,#51535,#51536,
#51537,#51538,#51539,#51540,#51541,#51542,#51543,#51544,#51545,#51546,#51547,
#51548,#51549,#51550,#51551,#51552,#51553,#51554,#51555,#51556,#51557,#51558,
#51559,#51560,#51561,#51562,#51563,#51564,#51565,#51566,#51567,#51568,#51569,
#51570,#51571,#51572,#51573,#51574,#51575,#51576,#51577,#51578,#51579,#51580,
#51581),.UNSPECIFIED.,.F.,.F.,(4,3,3,3,3,3,3,3,3,3,3,3,3,3,3,3,3,3,3,3,
4),(-0.741270768406373,-0.710653752603244,-0.663515400778915,-0.642552751532044,
-0.621528179181629,-0.557094712642544,-0.539607756557645,-0.476917461805843,
-0.415921284094216,-0.398576094285539,-0.383216406245164,-0.338950727439734,
-0.281486365585587,-0.260617405175195,-0.246177177084019,-0.184632882813014,
-0.134618480262488,-0.117250433969387,-0.0586252169846935,-0.00390747240475656,
0.),.UNSPECIFIED.);
#505=B_SPLINE_CURVE_WITH_KNOTS('',3,(#51994,#51995,#51996,#51997,#51998,
#51999,#52000),.UNSPECIFIED.,.F.,.F.,(4,3,4),(95.3578248186051,96.1842630387299,
97.0978324630305),.UNSPECIFIED.);
#506=B_SPLINE_CURVE_WITH_KNOTS('',3,(#52002,#52003,#52004,#52005,#52006,
#52007,#52008,#52009,#52010,#52011,#52012,#52013,#52014,#52015,#52016,#52017,
#52018,#52019,#52020,#52021,#52022,#52023,#52024,#52025,#52026,#52027,#52028,
#52029,#52030,#52031,#52032,#52033,#52034,#52035,#52036,#52037,#52038,#52039,
#52040,#52041,#52042,#52043,#52044,#52045,#52046,#52047,#52048,#52049,#52050,
#52051,#52052,#52053,#52054,#52055,#52056,#52057,#52058,#52059,#52060,#52061,
#52062),.UNSPECIFIED.,.F.,.F.,(4,3,3,3,3,3,3,3,3,3,3,3,3,3,3,3,3,3,3,3,
4),(-0.7443979491706,-0.718888480435923,-0.671065589306389,-0.646483278263035,
-0.600248517649804,-0.572968043327937,-0.555731292334261,-0.495420193045671,
-0.456580298674706,-0.439125676945103,-0.423945387737792,-0.376189396302257,
-0.329165721764475,-0.306302670249697,-0.285176394034303,-0.222891657896494,
-0.16716874342237,-0.151664010969902,-0.134867173180257,-0.0674335865901284,
0.),.UNSPECIFIED.);
#507=B_SPLINE_CURVE_WITH_KNOTS('',3,(#52063,#52064,#52065,#52066,#52067,
#52068,#52069,#52070,#52071),.UNSPECIFIED.,.F.,.F.,(4,1,1,1,1,1,4),(10.3759343473737,
11.2895037716743,12.2810941122798,13.2726844528853,14.2642747934907,15.2558651340962,
15.7079632679489),.UNSPECIFIED.);
#508=B_SPLINE_CURVE_WITH_KNOTS('',3,(#52077,#52078,#52079,#52080,#52081,
#52082,#52083,#52084,#52085,#52086,#52087,#52088,#52089,#52090,#52091,#52092,
#52093,#52094,#52095,#52096,#52097,#52098,#52099,#52100,#52101,#52102,#52103,
#52104,#52105,#52106,#52107,#52108,#52109,#52110,#52111,#52112,#52113,#52114,
#52115,#52116,#52117,#52118,#52119,#52120,#52121,#52122,#52123,#52124,#52125,
#52126,#52127,#52128,#52129,#52130,#52131,#52132,#52133,#52134,#52135,#52136,
#52137),.UNSPECIFIED.,.F.,.F.,(4,3,3,3,3,3,3,3,3,3,3,3,3,3,3,3,3,3,3,3,
4),(-0.741270768406355,-0.710653752603231,-0.663515385056919,-0.642552661274003,
-0.621528157125719,-0.557094687200405,-0.539607732337506,-0.476917424661932,
-0.415921204939973,-0.398576035954998,-0.383216387012519,-0.338950727439722,
-0.281486362115991,-0.260617409418295,-0.24617718206237,-0.184632886546777,
-0.134618488551931,-0.117250439398334,-0.0586252196991669,-0.00390755098249406,
0.),.UNSPECIFIED.);
#509=B_SPLINE_CURVE_WITH_KNOTS('',3,(#52140,#52141,#52142,#52143,#52144,
#52145,#52146,#52147),.UNSPECIFIED.,.F.,.F.,(4,1,1,1,1,4),(11.6152142277546,
12.6068045683601,13.5983949089656,14.589985249571,15.5815755901765,15.7079632679489),
 .UNSPECIFIED.);
#510=B_SPLINE_CURVE_WITH_KNOTS('',3,(#52560,#52561,#52562,#52563),
 .UNSPECIFIED.,.F.,.F.,(4,4),(-99.1590340605463,-98.3405286478881),
 .UNSPECIFIED.);
#1007=SHAPE_REPRESENTATION_RELATIONSHIP('SRR','None',#76744,#1027);
#1027=ADVANCED_BREP_SHAPE_REPRESENTATION('',(#1067),#76648);
#1047=STYLED_ITEM('',(#76913),#1067);
#1067=MANIFOLD_SOLID_BREP('Socket head screw',#26672);
#1086=TOROIDAL_SURFACE('',#27917,0.4183,0.025);
#1268=CYLINDRICAL_SURFACE('',#27876,0.3933);
#1269=CYLINDRICAL_SURFACE('',#27878,0.3933);
#1270=CYLINDRICAL_SURFACE('',#27879,0.3933);
#1271=CYLINDRICAL_SURFACE('',#27880,0.3933);
#1272=CYLINDRICAL_SURFACE('',#27881,0.3933);
#1273=CYLINDRICAL_SURFACE('',#27882,0.3933);
#1274=CYLINDRICAL_SURFACE('',#27883,0.3933);
#1275=CYLINDRICAL_SURFACE('',#27884,0.3933);
#1276=CYLINDRICAL_SURFACE('',#27885,0.3933);
#1277=CYLINDRICAL_SURFACE('',#27886,0.3933);
#1278=CYLINDRICAL_SURFACE('',#27887,0.3933);
#1279=CYLINDRICAL_SURFACE('',#27888,0.3933);
#1280=CYLINDRICAL_SURFACE('',#27889,0.3933);
#1281=CYLINDRICAL_SURFACE('',#27890,0.3933);
#1282=CYLINDRICAL_SURFACE('',#27891,0.3933);
#1283=CYLINDRICAL_SURFACE('',#27892,0.3933);
#1284=CYLINDRICAL_SURFACE('',#27893,0.322275);
#1285=CYLINDRICAL_SURFACE('',#27895,0.322275);
#1286=CYLINDRICAL_SURFACE('',#27896,0.322275);
#1287=CYLINDRICAL_SURFACE('',#27897,0.322275);
#1288=CYLINDRICAL_SURFACE('',#27898,0.322275);
#1289=CYLINDRICAL_SURFACE('',#27899,0.322275);
#1290=CYLINDRICAL_SURFACE('',#27900,0.322275);
#1291=CYLINDRICAL_SURFACE('',#27901,0.322275);
#1292=CYLINDRICAL_SURFACE('',#27902,0.322275);
#1293=CYLINDRICAL_SURFACE('',#27903,0.322275);
#1294=CYLINDRICAL_SURFACE('',#27904,0.322275);
#1295=CYLINDRICAL_SURFACE('',#27905,0.322275);
#1296=CYLINDRICAL_SURFACE('',#27906,0.322275);
#1297=CYLINDRICAL_SURFACE('',#27907,0.322275);
#1298=CYLINDRICAL_SURFACE('',#27908,0.322275);
#1299=CYLINDRICAL_SURFACE('',#27916,0.322275);
#1300=CYLINDRICAL_SURFACE('',#27921,0.3933);
#1301=CYLINDRICAL_SURFACE('',#28166,0.65);
#1635=FACE_BOUND('',#4809,.T.);
#1636=FACE_BOUND('',#4973,.T.);
#1944=PLANE('',#27909);
#1945=PLANE('',#27912);
#1946=PLANE('',#27922);
#1947=PLANE('',#27924);
#1948=PLANE('',#27926);
#1949=PLANE('',#27928);
#1950=PLANE('',#27930);
#1951=PLANE('',#27932);
#1952=PLANE('',#27934);
#1953=PLANE('',#27937);
#1954=PLANE('',#27938);
#1955=PLANE('',#27939);
#1956=PLANE('',#27940);
#1957=PLANE('',#27941);
#1958=PLANE('',#27942);
#1959=PLANE('',#27943);
#1960=PLANE('',#27944);
#1961=PLANE('',#27946);
#1962=PLANE('',#27947);
#1963=PLANE('',#27949);
#1964=PLANE('',#27950);
#1965=PLANE('',#27952);
#1966=PLANE('',#27953);
#1967=PLANE('',#27955);
#1968=PLANE('',#27956);
#1969=PLANE('',#27958);
#1970=PLANE('',#27959);
#1971=PLANE('',#27961);
#1972=PLANE('',#27962);
#1973=PLANE('',#27964);
#1974=PLANE('',#27965);
#1975=PLANE('',#27967);
#1976=PLANE('',#27968);
#1977=PLANE('',#27970);
#1978=PLANE('',#27971);
#1979=PLANE('',#27973);
#1980=PLANE('',#27974);
#1981=PLANE('',#27976);
#1982=PLANE('',#27977);
#1983=PLANE('',#27979);
#1984=PLANE('',#27980);
#1985=PLANE('',#27982);
#1986=PLANE('',#27983);
#1987=PLANE('',#27985);
#1988=PLANE('',#27986);
#1989=PLANE('',#27988);
#1990=PLANE('',#27989);
#1991=PLANE('',#27991);
#1992=PLANE('',#27992);
#1993=PLANE('',#27995);
#1994=PLANE('',#27996);
#1995=PLANE('',#27999);
#1996=PLANE('',#28000);
#1997=PLANE('',#28002);
#1998=PLANE('',#28003);
#1999=PLANE('',#28005);
#2000=PLANE('',#28006);
#2001=PLANE('',#28008);
#2002=PLANE('',#28009);
#2003=PLANE('',#28011);
#2004=PLANE('',#28012);
#2005=PLANE('',#28014);
#2006=PLANE('',#28015);
#2007=PLANE('',#28017);
#2008=PLANE('',#28018);
#2009=PLANE('',#28020);
#2010=PLANE('',#28021);
#2011=PLANE('',#28023);
#2012=PLANE('',#28024);
#2013=PLANE('',#28026);
#2014=PLANE('',#28027);
#2015=PLANE('',#28029);
#2016=PLANE('',#28030);
#2017=PLANE('',#28032);
#2018=PLANE('',#28033);
#2019=PLANE('',#28035);
#2020=PLANE('',#28036);
#2021=PLANE('',#28038);
#2022=PLANE('',#28039);
#2023=PLANE('',#28041);
#2024=PLANE('',#28042);
#2025=PLANE('',#28044);
#2026=PLANE('',#28045);
#2027=PLANE('',#28047);
#2028=PLANE('',#28048);
#2029=PLANE('',#28050);
#2030=PLANE('',#28051);
#2031=PLANE('',#28053);
#2032=PLANE('',#28054);
#2033=PLANE('',#28056);
#2034=PLANE('',#28057);
#2035=PLANE('',#28059);
#2036=PLANE('',#28060);
#2037=PLANE('',#28062);
#2038=PLANE('',#28063);
#2039=PLANE('',#28065);
#2040=PLANE('',#28066);
#2041=PLANE('',#28068);
#2042=PLANE('',#28069);
#2043=PLANE('',#28071);
#2044=PLANE('',#28072);
#2045=PLANE('',#28074);
#2046=PLANE('',#28075);
#2047=PLANE('',#28077);
#2048=PLANE('',#28078);
#2049=PLANE('',#28080);
#2050=PLANE('',#28081);
#2051=PLANE('',#28083);
#2052=PLANE('',#28084);
#2053=PLANE('',#28086);
#2054=PLANE('',#28087);
#2055=PLANE('',#28089);
#2056=PLANE('',#28090);
#2057=PLANE('',#28092);
#2058=PLANE('',#28093);
#2059=PLANE('',#28095);
#2060=PLANE('',#28096);
#2061=PLANE('',#28098);
#2062=PLANE('',#28099);
#2063=PLANE('',#28101);
#2064=PLANE('',#28103);
#2065=PLANE('',#28104);
#2066=PLANE('',#28105);
#2067=PLANE('',#28107);
#2068=PLANE('',#28108);
#2069=PLANE('',#28110);
#2070=PLANE('',#28111);
#2071=PLANE('',#28113);
#2072=PLANE('',#28114);
#2073=PLANE('',#28116);
#2074=PLANE('',#28117);
#2075=PLANE('',#28119);
#2076=PLANE('',#28120);
#2077=PLANE('',#28122);
#2078=PLANE('',#28123);
#2079=PLANE('',#28125);
#2080=PLANE('',#28126);
#2081=PLANE('',#28128);
#2082=PLANE('',#28129);
#2083=PLANE('',#28131);
#2084=PLANE('',#28132);
#2085=PLANE('',#28134);
#2086=PLANE('',#28135);
#2087=PLANE('',#28137);
#2088=PLANE('',#28138);
#2089=PLANE('',#28140);
#2090=PLANE('',#28141);
#2091=PLANE('',#28143);
#2092=PLANE('',#28144);
#2093=PLANE('',#28146);
#2094=PLANE('',#28147);
#2095=PLANE('',#28149);
#2096=PLANE('',#28150);
#2097=PLANE('',#28152);
#2098=PLANE('',#28153);
#2099=PLANE('',#28155);
#2100=PLANE('',#28156);
#2101=PLANE('',#28158);
#2102=PLANE('',#28159);
#2103=PLANE('',#28161);
#2104=PLANE('',#28205);
#3136=FACE_OUTER_BOUND('',#4770,.T.);
#3137=FACE_OUTER_BOUND('',#4771,.T.);
#3138=FACE_OUTER_BOUND('',#4772,.T.);
#3139=FACE_OUTER_BOUND('',#4773,.T.);
#3140=FACE_OUTER_BOUND('',#4774,.T.);
#3141=FACE_OUTER_BOUND('',#4775,.T.);
#3142=FACE_OUTER_BOUND('',#4776,.T.);
#3143=FACE_OUTER_BOUND('',#4777,.T.);
#3144=FACE_OUTER_BOUND('',#4778,.T.);
#3145=FACE_OUTER_BOUND('',#4779,.T.);
#3146=FACE_OUTER_BOUND('',#4780,.T.);
#3147=FACE_OUTER_BOUND('',#4781,.T.);
#3148=FACE_OUTER_BOUND('',#4782,.T.);
#3149=FACE_OUTER_BOUND('',#4783,.T.);
#3150=FACE_OUTER_BOUND('',#4784,.T.);
#3151=FACE_OUTER_BOUND('',#4785,.T.);
#3152=FACE_OUTER_BOUND('',#4786,.T.);
#3153=FACE_OUTER_BOUND('',#4787,.T.);
#3154=FACE_OUTER_BOUND('',#4788,.T.);
#3155=FACE_OUTER_BOUND('',#4789,.T.);
#3156=FACE_OUTER_BOUND('',#4790,.T.);
#3157=FACE_OUTER_BOUND('',#4791,.T.);
#3158=FACE_OUTER_BOUND('',#4792,.T.);
#3159=FACE_OUTER_BOUND('',#4793,.T.);
#3160=FACE_OUTER_BOUND('',#4794,.T.);
#3161=FACE_OUTER_BOUND('',#4795,.T.);
#3162=FACE_OUTER_BOUND('',#4796,.T.);
#3163=FACE_OUTER_BOUND('',#4797,.T.);
#3164=FACE_OUTER_BOUND('',#4798,.T.);
#3165=FACE_OUTER_BOUND('',#4799,.T.);
#3166=FACE_OUTER_BOUND('',#4800,.T.);
#3167=FACE_OUTER_BOUND('',#4801,.T.);
#3168=FACE_OUTER_BOUND('',#4802,.T.);
#3169=FACE_OUTER_BOUND('',#4803,.T.);
#3170=FACE_OUTER_BOUND('',#4804,.T.);
#3171=FACE_OUTER_BOUND('',#4805,.T.);
#3172=FACE_OUTER_BOUND('',#4806,.T.);
#3173=FACE_OUTER_BOUND('',#4807,.T.);
#3174=FACE_OUTER_BOUND('',#4808,.T.);
#3175=FACE_OUTER_BOUND('',#4810,.T.);
#3176=FACE_OUTER_BOUND('',#4811,.T.);
#3177=FACE_OUTER_BOUND('',#4812,.T.);
#3178=FACE_OUTER_BOUND('',#4813,.T.);
#3179=FACE_OUTER_BOUND('',#4814,.T.);
#3180=FACE_OUTER_BOUND('',#4815,.T.);
#3181=FACE_OUTER_BOUND('',#4816,.T.);
#3182=FACE_OUTER_BOUND('',#4817,.T.);
#3183=FACE_OUTER_BOUND('',#4818,.T.);
#3184=FACE_OUTER_BOUND('',#4819,.T.);
#3185=FACE_OUTER_BOUND('',#4820,.T.);
#3186=FACE_OUTER_BOUND('',#4821,.T.);
#3187=FACE_OUTER_BOUND('',#4822,.T.);
#3188=FACE_OUTER_BOUND('',#4823,.T.);
#3189=FACE_OUTER_BOUND('',#4824,.T.);
#3190=FACE_OUTER_BOUND('',#4825,.T.);
#3191=FACE_OUTER_BOUND('',#4826,.T.);
#3192=FACE_OUTER_BOUND('',#4827,.T.);
#3193=FACE_OUTER_BOUND('',#4828,.T.);
#3194=FACE_OUTER_BOUND('',#4829,.T.);
#3195=FACE_OUTER_BOUND('',#4830,.T.);
#3196=FACE_OUTER_BOUND('',#4831,.T.);
#3197=FACE_OUTER_BOUND('',#4832,.T.);
#3198=FACE_OUTER_BOUND('',#4833,.T.);
#3199=FACE_OUTER_BOUND('',#4834,.T.);
#3200=FACE_OUTER_BOUND('',#4835,.T.);
#3201=FACE_OUTER_BOUND('',#4836,.T.);
#3202=FACE_OUTER_BOUND('',#4837,.T.);
#3203=FACE_OUTER_BOUND('',#4838,.T.);
#3204=FACE_OUTER_BOUND('',#4839,.T.);
#3205=FACE_OUTER_BOUND('',#4840,.T.);
#3206=FACE_OUTER_BOUND('',#4841,.T.);
#3207=FACE_OUTER_BOUND('',#4842,.T.);
#3208=FACE_OUTER_BOUND('',#4843,.T.);
#3209=FACE_OUTER_BOUND('',#4844,.T.);
#3210=FACE_OUTER_BOUND('',#4845,.T.);
#3211=FACE_OUTER_BOUND('',#4846,.T.);
#3212=FACE_OUTER_BOUND('',#4847,.T.);
#3213=FACE_OUTER_BOUND('',#4848,.T.);
#3214=FACE_OUTER_BOUND('',#4849,.T.);
#3215=FACE_OUTER_BOUND('',#4850,.T.);
#3216=FACE_OUTER_BOUND('',#4851,.T.);
#3217=FACE_OUTER_BOUND('',#4852,.T.);
#3218=FACE_OUTER_BOUND('',#4853,.T.);
#3219=FACE_OUTER_BOUND('',#4854,.T.);
#3220=FACE_OUTER_BOUND('',#4855,.T.);
#3221=FACE_OUTER_BOUND('',#4856,.T.);
#3222=FACE_OUTER_BOUND('',#4857,.T.);
#3223=FACE_OUTER_BOUND('',#4858,.T.);
#3224=FACE_OUTER_BOUND('',#4859,.T.);
#3225=FACE_OUTER_BOUND('',#4860,.T.);
#3226=FACE_OUTER_BOUND('',#4861,.T.);
#3227=FACE_OUTER_BOUND('',#4862,.T.);
#3228=FACE_OUTER_BOUND('',#4863,.T.);
#3229=FACE_OUTER_BOUND('',#4864,.T.);
#3230=FACE_OUTER_BOUND('',#4865,.T.);
#3231=FACE_OUTER_BOUND('',#4866,.T.);
#3232=FACE_OUTER_BOUND('',#4867,.T.);
#3233=FACE_OUTER_BOUND('',#4868,.T.);
#3234=FACE_OUTER_BOUND('',#4869,.T.);
#3235=FACE_OUTER_BOUND('',#4870,.T.);
#3236=FACE_OUTER_BOUND('',#4871,.T.);
#3237=FACE_OUTER_BOUND('',#4872,.T.);
#3238=FACE_OUTER_BOUND('',#4873,.T.);
#3239=FACE_OUTER_BOUND('',#4874,.T.);
#3240=FACE_OUTER_BOUND('',#4875,.T.);
#3241=FACE_OUTER_BOUND('',#4876,.T.);
#3242=FACE_OUTER_BOUND('',#4877,.T.);
#3243=FACE_OUTER_BOUND('',#4878,.T.);
#3244=FACE_OUTER_BOUND('',#4879,.T.);
#3245=FACE_OUTER_BOUND('',#4880,.T.);
#3246=FACE_OUTER_BOUND('',#4881,.T.);
#3247=FACE_OUTER_BOUND('',#4882,.T.);
#3248=FACE_OUTER_BOUND('',#4883,.T.);
#3249=FACE_OUTER_BOUND('',#4884,.T.);
#3250=FACE_OUTER_BOUND('',#4885,.T.);
#3251=FACE_OUTER_BOUND('',#4886,.T.);
#3252=FACE_OUTER_BOUND('',#4887,.T.);
#3253=FACE_OUTER_BOUND('',#4888,.T.);
#3254=FACE_OUTER_BOUND('',#4889,.T.);
#3255=FACE_OUTER_BOUND('',#4890,.T.);
#3256=FACE_OUTER_BOUND('',#4891,.T.);
#3257=FACE_OUTER_BOUND('',#4892,.T.);
#3258=FACE_OUTER_BOUND('',#4893,.T.);
#3259=FACE_OUTER_BOUND('',#4894,.T.);
#3260=FACE_OUTER_BOUND('',#4895,.T.);
#3261=FACE_OUTER_BOUND('',#4896,.T.);
#3262=FACE_OUTER_BOUND('',#4897,.T.);
#3263=FACE_OUTER_BOUND('',#4898,.T.);
#3264=FACE_OUTER_BOUND('',#4899,.T.);
#3265=FACE_OUTER_BOUND('',#4900,.T.);
#3266=FACE_OUTER_BOUND('',#4901,.T.);
#3267=FACE_OUTER_BOUND('',#4902,.T.);
#3268=FACE_OUTER_BOUND('',#4903,.T.);
#3269=FACE_OUTER_BOUND('',#4904,.T.);
#3270=FACE_OUTER_BOUND('',#4905,.T.);
#3271=FACE_OUTER_BOUND('',#4906,.T.);
#3272=FACE_OUTER_BOUND('',#4907,.T.);
#3273=FACE_OUTER_BOUND('',#4908,.T.);
#3274=FACE_OUTER_BOUND('',#4909,.T.);
#3275=FACE_OUTER_BOUND('',#4910,.T.);
#3276=FACE_OUTER_BOUND('',#4911,.T.);
#3277=FACE_OUTER_BOUND('',#4912,.T.);
#3278=FACE_OUTER_BOUND('',#4913,.T.);
#3279=FACE_OUTER_BOUND('',#4914,.T.);
#3280=FACE_OUTER_BOUND('',#4915,.T.);
#3281=FACE_OUTER_BOUND('',#4916,.T.);
#3282=FACE_OUTER_BOUND('',#4917,.T.);
#3283=FACE_OUTER_BOUND('',#4918,.T.);
#3284=FACE_OUTER_BOUND('',#4919,.T.);
#3285=FACE_OUTER_BOUND('',#4920,.T.);
#3286=FACE_OUTER_BOUND('',#4921,.T.);
#3287=FACE_OUTER_BOUND('',#4922,.T.);
#3288=FACE_OUTER_BOUND('',#4923,.T.);
#3289=FACE_OUTER_BOUND('',#4924,.T.);
#3290=FACE_OUTER_BOUND('',#4925,.T.);
#3291=FACE_OUTER_BOUND('',#4926,.T.);
#3292=FACE_OUTER_BOUND('',#4927,.T.);
#3293=FACE_OUTER_BOUND('',#4928,.T.);
#3294=FACE_OUTER_BOUND('',#4929,.T.);
#3295=FACE_OUTER_BOUND('',#4930,.T.);
#3296=FACE_OUTER_BOUND('',#4931,.T.);
#3297=FACE_OUTER_BOUND('',#4932,.T.);
#3298=FACE_OUTER_BOUND('',#4933,.T.);
#3299=FACE_OUTER_BOUND('',#4934,.T.);
#3300=FACE_OUTER_BOUND('',#4935,.T.);
#3301=FACE_OUTER_BOUND('',#4936,.T.);
#3302=FACE_OUTER_BOUND('',#4937,.T.);
#3303=FACE_OUTER_BOUND('',#4938,.T.);
#3304=FACE_OUTER_BOUND('',#4939,.T.);
#3305=FACE_OUTER_BOUND('',#4940,.T.);
#3306=FACE_OUTER_BOUND('',#4941,.T.);
#3307=FACE_OUTER_BOUND('',#4942,.T.);
#3308=FACE_OUTER_BOUND('',#4943,.T.);
#3309=FACE_OUTER_BOUND('',#4944,.T.);
#3310=FACE_OUTER_BOUND('',#4945,.T.);
#3311=FACE_OUTER_BOUND('',#4946,.T.);
#3312=FACE_OUTER_BOUND('',#4947,.T.);
#3313=FACE_OUTER_BOUND('',#4948,.T.);
#3314=FACE_OUTER_BOUND('',#4949,.T.);
#3315=FACE_OUTER_BOUND('',#4950,.T.);
#3316=FACE_OUTER_BOUND('',#4951,.T.);
#3317=FACE_OUTER_BOUND('',#4952,.T.);
#3318=FACE_OUTER_BOUND('',#4953,.T.);
#3319=FACE_OUTER_BOUND('',#4954,.T.);
#3320=FACE_OUTER_BOUND('',#4955,.T.);
#3321=FACE_OUTER_BOUND('',#4956,.T.);
#3322=FACE_OUTER_BOUND('',#4957,.T.);
#3323=FACE_OUTER_BOUND('',#4958,.T.);
#3324=FACE_OUTER_BOUND('',#4959,.T.);
#3325=FACE_OUTER_BOUND('',#4960,.T.);
#3326=FACE_OUTER_BOUND('',#4961,.T.);
#3327=FACE_OUTER_BOUND('',#4962,.T.);
#3328=FACE_OUTER_BOUND('',#4963,.T.);
#3329=FACE_OUTER_BOUND('',#4964,.T.);
#3330=FACE_OUTER_BOUND('',#4965,.T.);
#3331=FACE_OUTER_BOUND('',#4966,.T.);
#3332=FACE_OUTER_BOUND('',#4967,.T.);
#3333=FACE_OUTER_BOUND('',#4968,.T.);
#3334=FACE_OUTER_BOUND('',#4969,.T.);
#3335=FACE_OUTER_BOUND('',#4970,.T.);
#3336=FACE_OUTER_BOUND('',#4971,.T.);
#3337=FACE_OUTER_BOUND('',#4972,.T.);
#4770=EDGE_LOOP('',(#20189,#20190,#20191,#20192));
#4771=EDGE_LOOP('',(#20193,#20194,#20195,#20196));
#4772=EDGE_LOOP('',(#20197,#20198,#20199,#20200));
#4773=EDGE_LOOP('',(#20201,#20202,#20203,#20204));
#4774=EDGE_LOOP('',(#20205,#20206,#20207,#20208));
#4775=EDGE_LOOP('',(#20209,#20210,#20211,#20212));
#4776=EDGE_LOOP('',(#20213,#20214,#20215,#20216));
#4777=EDGE_LOOP('',(#20217,#20218,#20219,#20220));
#4778=EDGE_LOOP('',(#20221,#20222,#20223,#20224));
#4779=EDGE_LOOP('',(#20225,#20226,#20227,#20228));
#4780=EDGE_LOOP('',(#20229,#20230,#20231,#20232));
#4781=EDGE_LOOP('',(#20233,#20234,#20235,#20236));
#4782=EDGE_LOOP('',(#20237,#20238,#20239,#20240));
#4783=EDGE_LOOP('',(#20241,#20242,#20243,#20244));
#4784=EDGE_LOOP('',(#20245,#20246,#20247,#20248));
#4785=EDGE_LOOP('',(#20249,#20250,#20251,#20252));
#4786=EDGE_LOOP('',(#20253,#20254,#20255,#20256));
#4787=EDGE_LOOP('',(#20257,#20258,#20259,#20260));
#4788=EDGE_LOOP('',(#20261,#20262,#20263,#20264));
#4789=EDGE_LOOP('',(#20265,#20266,#20267,#20268));
#4790=EDGE_LOOP('',(#20269,#20270,#20271,#20272));
#4791=EDGE_LOOP('',(#20273,#20274,#20275,#20276));
#4792=EDGE_LOOP('',(#20277,#20278,#20279,#20280));
#4793=EDGE_LOOP('',(#20281,#20282,#20283,#20284));
#4794=EDGE_LOOP('',(#20285,#20286,#20287,#20288));
#4795=EDGE_LOOP('',(#20289,#20290,#20291,#20292));
#4796=EDGE_LOOP('',(#20293,#20294,#20295,#20296));
#4797=EDGE_LOOP('',(#20297,#20298,#20299,#20300));
#4798=EDGE_LOOP('',(#20301,#20302,#20303,#20304));
#4799=EDGE_LOOP('',(#20305,#20306,#20307,#20308));
#4800=EDGE_LOOP('',(#20309,#20310,#20311,#20312));
#4801=EDGE_LOOP('',(#20313,#20314,#20315,#20316,#20317));
#4802=EDGE_LOOP('',(#20318,#20319,#20320,#20321,#20322,#20323,#20324,#20325,
#20326,#20327,#20328,#20329,#20330,#20331,#20332,#20333,#20334,#20335,#20336,
#20337,#20338,#20339,#20340,#20341,#20342,#20343,#20344,#20345,#20346,#20347,
#20348,#20349,#20350,#20351,#20352));
#4803=EDGE_LOOP('',(#20353,#20354,#20355,#20356,#20357));
#4804=EDGE_LOOP('',(#20358,#20359,#20360,#20361));
#4805=EDGE_LOOP('',(#20362,#20363,#20364,#20365,#20366,#20367,#20368,#20369,
#20370,#20371,#20372,#20373,#20374,#20375,#20376,#20377,#20378,#20379,#20380,
#20381,#20382,#20383,#20384,#20385,#20386,#20387,#20388,#20389,#20390,#20391,
#20392,#20393,#20394,#20395,#20396));
#4806=EDGE_LOOP('',(#20397,#20398,#20399,#20400,#20401,#20402));
#4807=EDGE_LOOP('',(#20403,#20404,#20405,#20406));
#4808=EDGE_LOOP('',(#20407));
#4809=EDGE_LOOP('',(#20408));
#4810=EDGE_LOOP('',(#20409,#20410));
#4811=EDGE_LOOP('',(#20411,#20412));
#4812=EDGE_LOOP('',(#20413,#20414));
#4813=EDGE_LOOP('',(#20415,#20416));
#4814=EDGE_LOOP('',(#20417,#20418));
#4815=EDGE_LOOP('',(#20419,#20420));
#4816=EDGE_LOOP('',(#20421,#20422,#20423,#20424,#20425,#20426,#20427,#20428));
#4817=EDGE_LOOP('',(#20429,#20430,#20431,#20432));
#4818=EDGE_LOOP('',(#20433,#20434,#20435,#20436));
#4819=EDGE_LOOP('',(#20437,#20438,#20439,#20440));
#4820=EDGE_LOOP('',(#20441,#20442,#20443,#20444));
#4821=EDGE_LOOP('',(#20445,#20446,#20447,#20448));
#4822=EDGE_LOOP('',(#20449,#20450,#20451,#20452));
#4823=EDGE_LOOP('',(#20453,#20454,#20455,#20456));
#4824=EDGE_LOOP('',(#20457,#20458,#20459));
#4825=EDGE_LOOP('',(#20460,#20461,#20462,#20463));
#4826=EDGE_LOOP('',(#20464,#20465,#20466));
#4827=EDGE_LOOP('',(#20467,#20468,#20469,#20470));
#4828=EDGE_LOOP('',(#20471,#20472,#20473));
#4829=EDGE_LOOP('',(#20474,#20475,#20476,#20477));
#4830=EDGE_LOOP('',(#20478,#20479,#20480));
#4831=EDGE_LOOP('',(#20481,#20482,#20483,#20484));
#4832=EDGE_LOOP('',(#20485,#20486,#20487));
#4833=EDGE_LOOP('',(#20488,#20489,#20490,#20491));
#4834=EDGE_LOOP('',(#20492,#20493,#20494));
#4835=EDGE_LOOP('',(#20495,#20496,#20497,#20498));
#4836=EDGE_LOOP('',(#20499,#20500,#20501));
#4837=EDGE_LOOP('',(#20502,#20503,#20504,#20505));
#4838=EDGE_LOOP('',(#20506,#20507,#20508));
#4839=EDGE_LOOP('',(#20509,#20510,#20511,#20512));
#4840=EDGE_LOOP('',(#20513,#20514,#20515));
#4841=EDGE_LOOP('',(#20516,#20517,#20518,#20519));
#4842=EDGE_LOOP('',(#20520,#20521,#20522));
#4843=EDGE_LOOP('',(#20523,#20524,#20525,#20526));
#4844=EDGE_LOOP('',(#20527,#20528,#20529));
#4845=EDGE_LOOP('',(#20530,#20531,#20532,#20533));
#4846=EDGE_LOOP('',(#20534,#20535,#20536));
#4847=EDGE_LOOP('',(#20537,#20538,#20539,#20540));
#4848=EDGE_LOOP('',(#20541,#20542,#20543));
#4849=EDGE_LOOP('',(#20544,#20545,#20546,#20547));
#4850=EDGE_LOOP('',(#20548,#20549,#20550));
#4851=EDGE_LOOP('',(#20551,#20552,#20553,#20554));
#4852=EDGE_LOOP('',(#20555,#20556,#20557));
#4853=EDGE_LOOP('',(#20558,#20559,#20560,#20561));
#4854=EDGE_LOOP('',(#20562,#20563,#20564));
#4855=EDGE_LOOP('',(#20565,#20566,#20567,#20568));
#4856=EDGE_LOOP('',(#20569,#20570,#20571,#20572));
#4857=EDGE_LOOP('',(#20573,#20574,#20575,#20576));
#4858=EDGE_LOOP('',(#20577,#20578,#20579,#20580));
#4859=EDGE_LOOP('',(#20581,#20582,#20583,#20584));
#4860=EDGE_LOOP('',(#20585,#20586,#20587));
#4861=EDGE_LOOP('',(#20588,#20589,#20590,#20591));
#4862=EDGE_LOOP('',(#20592,#20593,#20594));
#4863=EDGE_LOOP('',(#20595,#20596,#20597,#20598));
#4864=EDGE_LOOP('',(#20599,#20600,#20601));
#4865=EDGE_LOOP('',(#20602,#20603,#20604,#20605));
#4866=EDGE_LOOP('',(#20606,#20607,#20608));
#4867=EDGE_LOOP('',(#20609,#20610,#20611,#20612));
#4868=EDGE_LOOP('',(#20613,#20614,#20615));
#4869=EDGE_LOOP('',(#20616,#20617,#20618,#20619));
#4870=EDGE_LOOP('',(#20620,#20621,#20622));
#4871=EDGE_LOOP('',(#20623,#20624,#20625,#20626));
#4872=EDGE_LOOP('',(#20627,#20628,#20629));
#4873=EDGE_LOOP('',(#20630,#20631,#20632,#20633));
#4874=EDGE_LOOP('',(#20634,#20635,#20636));
#4875=EDGE_LOOP('',(#20637,#20638,#20639,#20640));
#4876=EDGE_LOOP('',(#20641,#20642,#20643));
#4877=EDGE_LOOP('',(#20644,#20645,#20646,#20647));
#4878=EDGE_LOOP('',(#20648,#20649,#20650));
#4879=EDGE_LOOP('',(#20651,#20652,#20653,#20654));
#4880=EDGE_LOOP('',(#20655,#20656,#20657));
#4881=EDGE_LOOP('',(#20658,#20659,#20660,#20661));
#4882=EDGE_LOOP('',(#20662,#20663,#20664));
#4883=EDGE_LOOP('',(#20665,#20666,#20667,#20668));
#4884=EDGE_LOOP('',(#20669,#20670,#20671));
#4885=EDGE_LOOP('',(#20672,#20673,#20674,#20675));
#4886=EDGE_LOOP('',(#20676,#20677,#20678));
#4887=EDGE_LOOP('',(#20679,#20680,#20681,#20682));
#4888=EDGE_LOOP('',(#20683,#20684,#20685));
#4889=EDGE_LOOP('',(#20686,#20687,#20688,#20689));
#4890=EDGE_LOOP('',(#20690,#20691,#20692));
#4891=EDGE_LOOP('',(#20693,#20694,#20695,#20696));
#4892=EDGE_LOOP('',(#20697,#20698,#20699));
#4893=EDGE_LOOP('',(#20700,#20701,#20702,#20703));
#4894=EDGE_LOOP('',(#20704,#20705,#20706));
#4895=EDGE_LOOP('',(#20707,#20708,#20709,#20710));
#4896=EDGE_LOOP('',(#20711,#20712,#20713));
#4897=EDGE_LOOP('',(#20714,#20715,#20716,#20717));
#4898=EDGE_LOOP('',(#20718,#20719,#20720));
#4899=EDGE_LOOP('',(#20721,#20722,#20723,#20724));
#4900=EDGE_LOOP('',(#20725,#20726,#20727));
#4901=EDGE_LOOP('',(#20728,#20729,#20730,#20731));
#4902=EDGE_LOOP('',(#20732,#20733,#20734));
#4903=EDGE_LOOP('',(#20735,#20736,#20737,#20738));
#4904=EDGE_LOOP('',(#20739,#20740,#20741));
#4905=EDGE_LOOP('',(#20742,#20743,#20744,#20745));
#4906=EDGE_LOOP('',(#20746,#20747,#20748));
#4907=EDGE_LOOP('',(#20749,#20750,#20751,#20752));
#4908=EDGE_LOOP('',(#20753,#20754,#20755));
#4909=EDGE_LOOP('',(#20756,#20757,#20758,#20759));
#4910=EDGE_LOOP('',(#20760,#20761,#20762));
#4911=EDGE_LOOP('',(#20763,#20764,#20765,#20766));
#4912=EDGE_LOOP('',(#20767,#20768,#20769));
#4913=EDGE_LOOP('',(#20770,#20771,#20772,#20773));
#4914=EDGE_LOOP('',(#20774,#20775,#20776));
#4915=EDGE_LOOP('',(#20777,#20778,#20779,#20780));
#4916=EDGE_LOOP('',(#20781,#20782,#20783));
#4917=EDGE_LOOP('',(#20784,#20785,#20786,#20787));
#4918=EDGE_LOOP('',(#20788,#20789,#20790));
#4919=EDGE_LOOP('',(#20791,#20792,#20793,#20794));
#4920=EDGE_LOOP('',(#20795,#20796,#20797));
#4921=EDGE_LOOP('',(#20798,#20799,#20800,#20801));
#4922=EDGE_LOOP('',(#20802,#20803,#20804));
#4923=EDGE_LOOP('',(#20805,#20806,#20807,#20808));
#4924=EDGE_LOOP('',(#20809,#20810,#20811));
#4925=EDGE_LOOP('',(#20812,#20813,#20814,#20815));
#4926=EDGE_LOOP('',(#20816,#20817,#20818));
#4927=EDGE_LOOP('',(#20819,#20820,#20821));
#4928=EDGE_LOOP('',(#20822,#20823,#20824,#20825));
#4929=EDGE_LOOP('',(#20826,#20827,#20828,#20829));
#4930=EDGE_LOOP('',(#20830,#20831,#20832));
#4931=EDGE_LOOP('',(#20833,#20834,#20835,#20836));
#4932=EDGE_LOOP('',(#20837,#20838,#20839));
#4933=EDGE_LOOP('',(#20840,#20841,#20842,#20843));
#4934=EDGE_LOOP('',(#20844,#20845,#20846));
#4935=EDGE_LOOP('',(#20847,#20848,#20849,#20850));
#4936=EDGE_LOOP('',(#20851,#20852,#20853));
#4937=EDGE_LOOP('',(#20854,#20855,#20856,#20857));
#4938=EDGE_LOOP('',(#20858,#20859,#20860));
#4939=EDGE_LOOP('',(#20861,#20862,#20863,#20864));
#4940=EDGE_LOOP('',(#20865,#20866,#20867));
#4941=EDGE_LOOP('',(#20868,#20869,#20870,#20871));
#4942=EDGE_LOOP('',(#20872,#20873,#20874));
#4943=EDGE_LOOP('',(#20875,#20876,#20877,#20878));
#4944=EDGE_LOOP('',(#20879,#20880,#20881));
#4945=EDGE_LOOP('',(#20882,#20883,#20884,#20885));
#4946=EDGE_LOOP('',(#20886,#20887,#20888));
#4947=EDGE_LOOP('',(#20889,#20890,#20891,#20892));
#4948=EDGE_LOOP('',(#20893,#20894,#20895));
#4949=EDGE_LOOP('',(#20896,#20897,#20898,#20899));
#4950=EDGE_LOOP('',(#20900,#20901,#20902));
#4951=EDGE_LOOP('',(#20903,#20904,#20905,#20906));
#4952=EDGE_LOOP('',(#20907,#20908,#20909));
#4953=EDGE_LOOP('',(#20910,#20911,#20912,#20913));
#4954=EDGE_LOOP('',(#20914,#20915,#20916));
#4955=EDGE_LOOP('',(#20917,#20918,#20919,#20920));
#4956=EDGE_LOOP('',(#20921,#20922,#20923));
#4957=EDGE_LOOP('',(#20924,#20925,#20926,#20927));
#4958=EDGE_LOOP('',(#20928,#20929,#20930));
#4959=EDGE_LOOP('',(#20931,#20932,#20933,#20934));
#4960=EDGE_LOOP('',(#20935,#20936,#20937));
#4961=EDGE_LOOP('',(#20938,#20939,#20940,#20941));
#4962=EDGE_LOOP('',(#20942,#20943,#20944));
#4963=EDGE_LOOP('',(#20945,#20946,#20947,#20948));
#4964=EDGE_LOOP('',(#20949,#20950,#20951));
#4965=EDGE_LOOP('',(#20952,#20953,#20954,#20955));
#4966=EDGE_LOOP('',(#20956,#20957,#20958));
#4967=EDGE_LOOP('',(#20959));
#4968=EDGE_LOOP('',(#20960,#20961,#20962,#20963,#20964,#20965));
#4969=EDGE_LOOP('',(#20966,#20967,#20968,#20969));
#4970=EDGE_LOOP('',(#20970,#20971,#20972,#20973,#20974,#20975,#20976,#20977,
#20978,#20979,#20980,#20981,#20982,#20983,#20984,#20985,#20986,#20987,#20988,
#20989,#20990,#20991,#20992,#20993,#20994,#20995,#20996,#20997,#20998,#20999,
#21000,#21001,#21002,#21003,#21004,#21005,#21006,#21007,#21008,#21009,#21010,
#21011,#21012,#21013,#21014,#21015,#21016,#21017,#21018,#21019,#21020,#21021,
#21022,#21023,#21024,#21025,#21026,#21027,#21028,#21029,#21030,#21031,#21032,
#21033,#21034,#21035,#21036,#21037,#21038,#21039,#21040,#21041,#21042,#21043,
#21044,#21045,#21046,#21047,#21048,#21049,#21050,#21051,#21052,#21053,#21054,
#21055,#21056,#21057,#21058,#21059,#21060,#21061,#21062,#21063,#21064,#21065,
#21066,#21067,#21068,#21069,#21070,#21071,#21072,#21073,#21074,#21075,#21076,
#21077,#21078,#21079,#21080,#21081,#21082,#21083,#21084,#21085,#21086,#21087,
#21088,#21089,#21090,#21091,#21092,#21093,#21094,#21095,#21096,#21097,#21098,
#21099,#21100,#21101,#21102,#21103,#21104,#21105,#21106,#21107,#21108,#21109,
#21110,#21111,#21112,#21113,#21114,#21115,#21116,#21117));
#4971=EDGE_LOOP('',(#21118,#21119,#21120,#21121,#21122,#21123,#21124,#21125,
#21126,#21127,#21128,#21129,#21130,#21131,#21132,#21133,#21134,#21135,#21136,
#21137,#21138,#21139,#21140,#21141,#21142,#21143,#21144,#21145,#21146,#21147,
#21148,#21149,#21150,#21151,#21152,#21153,#21154,#21155,#21156,#21157,#21158,
#21159,#21160,#21161,#21162,#21163,#21164,#21165,#21166,#21167,#21168,#21169,
#21170,#21171,#21172,#21173,#21174,#21175,#21176,#21177,#21178,#21179,#21180,
#21181,#21182,#21183,#21184,#21185,#21186,#21187,#21188,#21189,#21190,#21191,
#21192,#21193));
#4972=EDGE_LOOP('',(#21194));
#4973=EDGE_LOOP('',(#21195,#21196,#21197,#21198,#21199,#21200));
#6090=CIRCLE('',#27877,0.3933);
#6091=CIRCLE('',#27894,0.322275);
#6092=CIRCLE('',#27910,0.3933);
#6093=CIRCLE('',#27911,0.3933);
#6094=CIRCLE('',#27913,0.3933);
#6095=CIRCLE('',#27914,0.3933);
#6096=CIRCLE('',#27915,0.322275);
#6097=CIRCLE('',#27918,0.025);
#6098=CIRCLE('',#27919,0.4183);
#6099=CIRCLE('',#27920,0.3933);
#6100=CIRCLE('',#27923,0.62);
#6101=CIRCLE('',#27925,0.346410161513775);
#6102=CIRCLE('',#27927,0.346410161513775);
#6103=CIRCLE('',#27929,0.346410161513775);
#6104=CIRCLE('',#27931,0.346410161513775);
#6105=CIRCLE('',#27933,0.346410161513775);
#6106=CIRCLE('',#27935,0.346410161513775);
#6107=CIRCLE('',#27945,0.65);
#6108=CIRCLE('',#27948,0.65);
#6109=CIRCLE('',#27951,0.65);
#6110=CIRCLE('',#27954,0.65);
#6111=CIRCLE('',#27957,0.65);
#6112=CIRCLE('',#27960,0.65);
#6113=CIRCLE('',#27963,0.65);
#6114=CIRCLE('',#27966,0.65);
#6115=CIRCLE('',#27969,0.65);
#6116=CIRCLE('',#27972,0.65);
#6117=CIRCLE('',#27975,0.65);
#6118=CIRCLE('',#27978,0.65);
#6119=CIRCLE('',#27981,0.65);
#6120=CIRCLE('',#27984,0.65);
#6121=CIRCLE('',#27987,0.65);
#6122=CIRCLE('',#27990,0.65);
#6123=CIRCLE('',#27993,0.65);
#6124=CIRCLE('',#27994,0.65);
#6125=CIRCLE('',#27997,0.65);
#6126=CIRCLE('',#27998,0.65);
#6127=CIRCLE('',#28001,0.65);
#6128=CIRCLE('',#28004,0.65);
#6129=CIRCLE('',#28007,0.65);
#6130=CIRCLE('',#28010,0.65);
#6131=CIRCLE('',#28013,0.65);
#6132=CIRCLE('',#28016,0.65);
#6133=CIRCLE('',#28019,0.65);
#6134=CIRCLE('',#28022,0.65);
#6135=CIRCLE('',#28025,0.65);
#6136=CIRCLE('',#28028,0.65);
#6137=CIRCLE('',#28031,0.65);
#6138=CIRCLE('',#28034,0.65);
#6139=CIRCLE('',#28037,0.65);
#6140=CIRCLE('',#28040,0.65);
#6141=CIRCLE('',#28043,0.65);
#6142=CIRCLE('',#28046,0.65);
#6143=CIRCLE('',#28049,0.65);
#6144=CIRCLE('',#28052,0.65);
#6145=CIRCLE('',#28055,0.65);
#6146=CIRCLE('',#28058,0.65);
#6147=CIRCLE('',#28061,0.65);
#6148=CIRCLE('',#28064,0.65);
#6149=CIRCLE('',#28067,0.65);
#6150=CIRCLE('',#28070,0.65);
#6151=CIRCLE('',#28073,0.65);
#6152=CIRCLE('',#28076,0.65);
#6153=CIRCLE('',#28079,0.65);
#6154=CIRCLE('',#28082,0.65);
#6155=CIRCLE('',#28085,0.65);
#6156=CIRCLE('',#28088,0.65);
#6157=CIRCLE('',#28091,0.65);
#6158=CIRCLE('',#28094,0.65);
#6159=CIRCLE('',#28097,0.65);
#6160=CIRCLE('',#28100,0.65);
#6161=CIRCLE('',#28102,0.65);
#6162=CIRCLE('',#28106,0.65);
#6163=CIRCLE('',#28109,0.65);
#6164=CIRCLE('',#28112,0.65);
#6165=CIRCLE('',#28115,0.65);
#6166=CIRCLE('',#28118,0.65);
#6167=CIRCLE('',#28121,0.65);
#6168=CIRCLE('',#28124,0.65);
#6169=CIRCLE('',#28127,0.65);
#6170=CIRCLE('',#28130,0.65);
#6171=CIRCLE('',#28133,0.65);
#6172=CIRCLE('',#28136,0.65);
#6173=CIRCLE('',#28139,0.65);
#6174=CIRCLE('',#28142,0.65);
#6175=CIRCLE('',#28145,0.65);
#6176=CIRCLE('',#28148,0.65);
#6177=CIRCLE('',#28151,0.65);
#6178=CIRCLE('',#28154,0.65);
#6179=CIRCLE('',#28157,0.65);
#6180=CIRCLE('',#28160,0.65);
#6181=CIRCLE('',#28162,0.35);
#6182=CIRCLE('',#28165,0.65);
#6183=CIRCLE('',#28167,0.65);
#6184=CIRCLE('',#28168,0.65);
#6185=CIRCLE('',#28169,0.65);
#6186=CIRCLE('',#28170,0.65);
#6187=CIRCLE('',#28171,0.65);
#6188=CIRCLE('',#28172,0.65);
#6189=CIRCLE('',#28173,0.65);
#6190=CIRCLE('',#28174,0.65);
#6191=CIRCLE('',#28175,0.65);
#6192=CIRCLE('',#28176,0.65);
#6193=CIRCLE('',#28177,0.65);
#6194=CIRCLE('',#28178,0.65);
#6195=CIRCLE('',#28179,0.65);
#6196=CIRCLE('',#28180,0.65);
#6197=CIRCLE('',#28181,0.65);
#6198=CIRCLE('',#28182,0.65);
#6199=CIRCLE('',#28183,0.65);
#6200=CIRCLE('',#28184,0.65);
#6201=CIRCLE('',#28185,0.65);
#6202=CIRCLE('',#28186,0.65);
#6203=CIRCLE('',#28187,0.65);
#6204=CIRCLE('',#28188,0.65);
#6205=CIRCLE('',#28189,0.65);
#6206=CIRCLE('',#28190,0.65);
#6207=CIRCLE('',#28191,0.65);
#6208=CIRCLE('',#28192,0.65);
#6209=CIRCLE('',#28193,0.65);
#6210=CIRCLE('',#28194,0.65);
#6211=CIRCLE('',#28195,0.65);
#6212=CIRCLE('',#28196,0.65);
#6213=CIRCLE('',#28197,0.65);
#6214=CIRCLE('',#28198,0.65);
#6215=CIRCLE('',#28199,0.65);
#6216=CIRCLE('',#28200,0.65);
#6217=CIRCLE('',#28201,0.65);
#6218=CIRCLE('',#28202,0.65);
#6219=CIRCLE('',#28204,0.6);
#7456=LINE('',#50315,#9612);
#7457=LINE('',#50339,#9613);
#7458=LINE('',#50387,#9614);
#7459=LINE('',#50435,#9615);
#7460=LINE('',#50489,#9616);
#7461=LINE('',#50537,#9617);
#7462=LINE('',#50585,#9618);
#7463=LINE('',#50639,#9619);
#7464=LINE('',#50687,#9620);
#7465=LINE('',#50735,#9621);
#7466=LINE('',#50789,#9622);
#7467=LINE('',#50837,#9623);
#7468=LINE('',#50885,#9624);
#7469=LINE('',#50939,#9625);
#7470=LINE('',#50987,#9626);
#7471=LINE('',#51035,#9627);
#7472=LINE('',#51089,#9628);
#7473=LINE('',#51112,#9629);
#7474=LINE('',#51137,#9630);
#7475=LINE('',#51161,#9631);
#7476=LINE('',#51186,#9632);
#7477=LINE('',#51211,#9633);
#7478=LINE('',#51235,#9634);
#7479=LINE('',#51260,#9635);
#7480=LINE('',#51285,#9636);
#7481=LINE('',#51309,#9637);
#7482=LINE('',#51334,#9638);
#7483=LINE('',#51359,#9639);
#7484=LINE('',#51383,#9640);
#7485=LINE('',#51408,#9641);
#7486=LINE('',#51433,#9642);
#7487=LINE('',#52576,#9643);
#7488=LINE('',#52580,#9644);
#7489=LINE('',#52584,#9645);
#7490=LINE('',#52588,#9646);
#7491=LINE('',#52592,#9647);
#7492=LINE('',#52595,#9648);
#7493=LINE('',#52599,#9649);
#7494=LINE('',#52603,#9650);
#7495=LINE('',#52604,#9651);
#7496=LINE('',#52605,#9652);
#7497=LINE('',#52608,#9653);
#7498=LINE('',#52609,#9654);
#7499=LINE('',#52612,#9655);
#7500=LINE('',#52613,#9656);
#7501=LINE('',#52616,#9657);
#7502=LINE('',#52617,#9658);
#7503=LINE('',#52620,#9659);
#7504=LINE('',#52621,#9660);
#7505=LINE('',#52623,#9661);
#7506=LINE('',#52627,#9662);
#7507=LINE('',#52629,#9663);
#7508=LINE('',#52631,#9664);
#7509=LINE('',#52632,#9665);
#7510=LINE('',#52636,#9666);
#7511=LINE('',#52639,#9667);
#7512=LINE('',#52640,#9668);
#7513=LINE('',#52646,#9669);
#7514=LINE('',#52648,#9670);
#7515=LINE('',#52650,#9671);
#7516=LINE('',#52651,#9672);
#7517=LINE('',#52655,#9673);
#7518=LINE('',#52658,#9674);
#7519=LINE('',#52659,#9675);
#7520=LINE('',#52665,#9676);
#7521=LINE('',#52667,#9677);
#7522=LINE('',#52669,#9678);
#7523=LINE('',#52670,#9679);
#7524=LINE('',#52674,#9680);
#7525=LINE('',#52677,#9681);
#7526=LINE('',#52678,#9682);
#7527=LINE('',#52684,#9683);
#7528=LINE('',#52686,#9684);
#7529=LINE('',#52688,#9685);
#7530=LINE('',#52689,#9686);
#7531=LINE('',#52693,#9687);
#7532=LINE('',#52696,#9688);
#7533=LINE('',#52697,#9689);
#7534=LINE('',#52703,#9690);
#7535=LINE('',#52705,#9691);
#7536=LINE('',#52707,#9692);
#7537=LINE('',#52708,#9693);
#7538=LINE('',#52712,#9694);
#7539=LINE('',#52715,#9695);
#7540=LINE('',#52716,#9696);
#7541=LINE('',#52722,#9697);
#7542=LINE('',#52724,#9698);
#7543=LINE('',#52726,#9699);
#7544=LINE('',#52727,#9700);
#7545=LINE('',#52731,#9701);
#7546=LINE('',#52734,#9702);
#7547=LINE('',#52735,#9703);
#7548=LINE('',#52741,#9704);
#7549=LINE('',#52743,#9705);
#7550=LINE('',#52745,#9706);
#7551=LINE('',#52746,#9707);
#7552=LINE('',#52750,#9708);
#7553=LINE('',#52753,#9709);
#7554=LINE('',#52754,#9710);
#7555=LINE('',#52760,#9711);
#7556=LINE('',#52762,#9712);
#7557=LINE('',#52764,#9713);
#7558=LINE('',#52765,#9714);
#7559=LINE('',#52769,#9715);
#7560=LINE('',#52772,#9716);
#7561=LINE('',#52773,#9717);
#7562=LINE('',#52779,#9718);
#7563=LINE('',#52781,#9719);
#7564=LINE('',#52783,#9720);
#7565=LINE('',#52784,#9721);
#7566=LINE('',#52789,#9722);
#7567=LINE('',#52793,#9723);
#7568=LINE('',#52794,#9724);
#7569=LINE('',#52802,#9725);
#7570=LINE('',#52804,#9726);
#7571=LINE('',#52806,#9727);
#7572=LINE('',#52807,#9728);
#7573=LINE('',#52811,#9729);
#7574=LINE('',#52814,#9730);
#7575=LINE('',#52815,#9731);
#7576=LINE('',#52821,#9732);
#7577=LINE('',#52823,#9733);
#7578=LINE('',#52825,#9734);
#7579=LINE('',#52826,#9735);
#7580=LINE('',#52830,#9736);
#7581=LINE('',#52833,#9737);
#7582=LINE('',#52834,#9738);
#7583=LINE('',#52840,#9739);
#7584=LINE('',#52842,#9740);
#7585=LINE('',#52844,#9741);
#7586=LINE('',#52845,#9742);
#7587=LINE('',#52849,#9743);
#7588=LINE('',#52852,#9744);
#7589=LINE('',#52853,#9745);
#7590=LINE('',#52859,#9746);
#7591=LINE('',#52861,#9747);
#7592=LINE('',#52863,#9748);
#7593=LINE('',#52864,#9749);
#7594=LINE('',#52868,#9750);
#7595=LINE('',#52871,#9751);
#7596=LINE('',#52872,#9752);
#7597=LINE('',#52878,#9753);
#7598=LINE('',#52880,#9754);
#7599=LINE('',#52882,#9755);
#7600=LINE('',#52883,#9756);
#7601=LINE('',#52887,#9757);
#7602=LINE('',#52890,#9758);
#7603=LINE('',#52891,#9759);
#7604=LINE('',#52897,#9760);
#7605=LINE('',#52899,#9761);
#7606=LINE('',#52901,#9762);
#7607=LINE('',#52902,#9763);
#7608=LINE('',#52906,#9764);
#7609=LINE('',#52909,#9765);
#7610=LINE('',#52910,#9766);
#7611=LINE('',#52916,#9767);
#7612=LINE('',#52918,#9768);
#7613=LINE('',#52920,#9769);
#7614=LINE('',#52921,#9770);
#7615=LINE('',#52925,#9771);
#7616=LINE('',#52928,#9772);
#7617=LINE('',#52929,#9773);
#7618=LINE('',#52935,#9774);
#7619=LINE('',#52937,#9775);
#7620=LINE('',#52939,#9776);
#7621=LINE('',#52940,#9777);
#7622=LINE('',#52944,#9778);
#7623=LINE('',#52947,#9779);
#7624=LINE('',#52948,#9780);
#7625=LINE('',#52954,#9781);
#7626=LINE('',#52956,#9782);
#7627=LINE('',#52958,#9783);
#7628=LINE('',#52959,#9784);
#7629=LINE('',#52963,#9785);
#7630=LINE('',#52966,#9786);
#7631=LINE('',#52967,#9787);
#7632=LINE('',#52973,#9788);
#7633=LINE('',#52975,#9789);
#7634=LINE('',#52977,#9790);
#7635=LINE('',#52978,#9791);
#7636=LINE('',#52982,#9792);
#7637=LINE('',#52985,#9793);
#7638=LINE('',#52986,#9794);
#7639=LINE('',#52992,#9795);
#7640=LINE('',#52994,#9796);
#7641=LINE('',#52996,#9797);
#7642=LINE('',#52997,#9798);
#7643=LINE('',#53001,#9799);
#7644=LINE('',#53004,#9800);
#7645=LINE('',#53005,#9801);
#7646=LINE('',#53011,#9802);
#7647=LINE('',#53013,#9803);
#7648=LINE('',#53015,#9804);
#7649=LINE('',#53016,#9805);
#7650=LINE('',#53020,#9806);
#7651=LINE('',#53023,#9807);
#7652=LINE('',#53024,#9808);
#7653=LINE('',#53030,#9809);
#7654=LINE('',#53032,#9810);
#7655=LINE('',#53034,#9811);
#7656=LINE('',#53035,#9812);
#7657=LINE('',#53039,#9813);
#7658=LINE('',#53042,#9814);
#7659=LINE('',#53043,#9815);
#7660=LINE('',#53049,#9816);
#7661=LINE('',#53051,#9817);
#7662=LINE('',#53053,#9818);
#7663=LINE('',#53054,#9819);
#7664=LINE('',#53058,#9820);
#7665=LINE('',#53061,#9821);
#7666=LINE('',#53062,#9822);
#7667=LINE('',#53068,#9823);
#7668=LINE('',#53070,#9824);
#7669=LINE('',#53072,#9825);
#7670=LINE('',#53073,#9826);
#7671=LINE('',#53077,#9827);
#7672=LINE('',#53080,#9828);
#7673=LINE('',#53081,#9829);
#7674=LINE('',#53087,#9830);
#7675=LINE('',#53089,#9831);
#7676=LINE('',#53091,#9832);
#7677=LINE('',#53092,#9833);
#7678=LINE('',#53096,#9834);
#7679=LINE('',#53099,#9835);
#7680=LINE('',#53100,#9836);
#7681=LINE('',#53106,#9837);
#7682=LINE('',#53108,#9838);
#7683=LINE('',#53110,#9839);
#7684=LINE('',#53111,#9840);
#7685=LINE('',#53115,#9841);
#7686=LINE('',#53118,#9842);
#7687=LINE('',#53119,#9843);
#7688=LINE('',#53127,#9844);
#7689=LINE('',#53128,#9845);
#7690=LINE('',#53131,#9846);
#7691=LINE('',#53133,#9847);
#7692=LINE('',#53134,#9848);
#7693=LINE('',#53137,#9849);
#7694=LINE('',#53138,#9850);
#7695=LINE('',#53144,#9851);
#7696=LINE('',#53146,#9852);
#7697=LINE('',#53148,#9853);
#7698=LINE('',#53149,#9854);
#7699=LINE('',#53153,#9855);
#7700=LINE('',#53156,#9856);
#7701=LINE('',#53157,#9857);
#7702=LINE('',#53163,#9858);
#7703=LINE('',#53165,#9859);
#7704=LINE('',#53167,#9860);
#7705=LINE('',#53168,#9861);
#7706=LINE('',#53172,#9862);
#7707=LINE('',#53175,#9863);
#7708=LINE('',#53176,#9864);
#7709=LINE('',#53182,#9865);
#7710=LINE('',#53184,#9866);
#7711=LINE('',#53186,#9867);
#7712=LINE('',#53187,#9868);
#7713=LINE('',#53191,#9869);
#7714=LINE('',#53194,#9870);
#7715=LINE('',#53195,#9871);
#7716=LINE('',#53201,#9872);
#7717=LINE('',#53203,#9873);
#7718=LINE('',#53205,#9874);
#7719=LINE('',#53206,#9875);
#7720=LINE('',#53210,#9876);
#7721=LINE('',#53213,#9877);
#7722=LINE('',#53214,#9878);
#7723=LINE('',#53220,#9879);
#7724=LINE('',#53222,#9880);
#7725=LINE('',#53224,#9881);
#7726=LINE('',#53225,#9882);
#7727=LINE('',#53229,#9883);
#7728=LINE('',#53232,#9884);
#7729=LINE('',#53233,#9885);
#7730=LINE('',#53239,#9886);
#7731=LINE('',#53241,#9887);
#7732=LINE('',#53243,#9888);
#7733=LINE('',#53244,#9889);
#7734=LINE('',#53248,#9890);
#7735=LINE('',#53251,#9891);
#7736=LINE('',#53252,#9892);
#7737=LINE('',#53258,#9893);
#7738=LINE('',#53260,#9894);
#7739=LINE('',#53262,#9895);
#7740=LINE('',#53263,#9896);
#7741=LINE('',#53267,#9897);
#7742=LINE('',#53270,#9898);
#7743=LINE('',#53271,#9899);
#7744=LINE('',#53277,#9900);
#7745=LINE('',#53279,#9901);
#7746=LINE('',#53281,#9902);
#7747=LINE('',#53282,#9903);
#7748=LINE('',#53286,#9904);
#7749=LINE('',#53289,#9905);
#7750=LINE('',#53290,#9906);
#7751=LINE('',#53296,#9907);
#7752=LINE('',#53298,#9908);
#7753=LINE('',#53300,#9909);
#7754=LINE('',#53301,#9910);
#7755=LINE('',#53305,#9911);
#7756=LINE('',#53308,#9912);
#7757=LINE('',#53309,#9913);
#7758=LINE('',#53316,#9914);
#7759=LINE('',#53320,#9915);
#7760=LINE('',#53338,#9916);
#7761=LINE('',#53362,#9917);
#9612=VECTOR('',#32153,0.4);
#9613=VECTOR('',#32158,0.4);
#9614=VECTOR('',#32161,0.4);
#9615=VECTOR('',#32164,0.4);
#9616=VECTOR('',#32167,0.4);
#9617=VECTOR('',#32170,0.4);
#9618=VECTOR('',#32173,0.4);
#9619=VECTOR('',#32176,0.4);
#9620=VECTOR('',#32179,0.4);
#9621=VECTOR('',#32182,0.4);
#9622=VECTOR('',#32185,0.4);
#9623=VECTOR('',#32188,0.4);
#9624=VECTOR('',#32191,0.4);
#9625=VECTOR('',#32194,0.4);
#9626=VECTOR('',#32197,0.4);
#9627=VECTOR('',#32200,0.4);
#9628=VECTOR('',#32203,0.322275);
#9629=VECTOR('',#32208,0.322275);
#9630=VECTOR('',#32211,0.322275);
#9631=VECTOR('',#32214,0.322275);
#9632=VECTOR('',#32217,0.322275);
#9633=VECTOR('',#32220,0.322275);
#9634=VECTOR('',#32223,0.322275);
#9635=VECTOR('',#32226,0.322275);
#9636=VECTOR('',#32229,0.322275);
#9637=VECTOR('',#32232,0.322275);
#9638=VECTOR('',#32235,0.322275);
#9639=VECTOR('',#32238,0.322275);
#9640=VECTOR('',#32241,0.322275);
#9641=VECTOR('',#32244,0.322275);
#9642=VECTOR('',#32247,0.322275);
#9643=VECTOR('',#32280,1.);
#9644=VECTOR('',#32285,1.);
#9645=VECTOR('',#32290,1.);
#9646=VECTOR('',#32295,1.);
#9647=VECTOR('',#32300,1.);
#9648=VECTOR('',#32305,1.);
#9649=VECTOR('',#32310,0.173205080756888);
#9650=VECTOR('',#32313,1.);
#9651=VECTOR('',#32314,1.);
#9652=VECTOR('',#32315,1.);
#9653=VECTOR('',#32318,1.);
#9654=VECTOR('',#32319,1.);
#9655=VECTOR('',#32322,1.);
#9656=VECTOR('',#32323,1.);
#9657=VECTOR('',#32326,1.);
#9658=VECTOR('',#32327,1.);
#9659=VECTOR('',#32330,1.);
#9660=VECTOR('',#32331,1.);
#9661=VECTOR('',#32334,1.);
#9662=VECTOR('',#32337,1.);
#9663=VECTOR('',#32338,1.);
#9664=VECTOR('',#32339,1.);
#9665=VECTOR('',#32340,1.);
#9666=VECTOR('',#32345,1.);
#9667=VECTOR('',#32348,1.);
#9668=VECTOR('',#32349,1.);
#9669=VECTOR('',#32356,1.);
#9670=VECTOR('',#32357,1.);
#9671=VECTOR('',#32358,1.);
#9672=VECTOR('',#32359,1.);
#9673=VECTOR('',#32364,1.);
#9674=VECTOR('',#32367,1.);
#9675=VECTOR('',#32368,1.);
#9676=VECTOR('',#32375,1.);
#9677=VECTOR('',#32376,1.);
#9678=VECTOR('',#32377,1.);
#9679=VECTOR('',#32378,1.);
#9680=VECTOR('',#32383,1.);
#9681=VECTOR('',#32386,1.);
#9682=VECTOR('',#32387,1.);
#9683=VECTOR('',#32394,1.);
#9684=VECTOR('',#32395,1.);
#9685=VECTOR('',#32396,1.);
#9686=VECTOR('',#32397,1.);
#9687=VECTOR('',#32402,1.);
#9688=VECTOR('',#32405,1.);
#9689=VECTOR('',#32406,1.);
#9690=VECTOR('',#32413,1.);
#9691=VECTOR('',#32414,1.);
#9692=VECTOR('',#32415,1.);
#9693=VECTOR('',#32416,1.);
#9694=VECTOR('',#32421,1.);
#9695=VECTOR('',#32424,1.);
#9696=VECTOR('',#32425,1.);
#9697=VECTOR('',#32432,1.);
#9698=VECTOR('',#32433,1.);
#9699=VECTOR('',#32434,1.);
#9700=VECTOR('',#32435,1.);
#9701=VECTOR('',#32440,1.);
#9702=VECTOR('',#32443,1.);
#9703=VECTOR('',#32444,1.);
#9704=VECTOR('',#32451,1.);
#9705=VECTOR('',#32452,1.);
#9706=VECTOR('',#32453,1.);
#9707=VECTOR('',#32454,1.);
#9708=VECTOR('',#32459,1.);
#9709=VECTOR('',#32462,1.);
#9710=VECTOR('',#32463,1.);
#9711=VECTOR('',#32470,1.);
#9712=VECTOR('',#32471,1.);
#9713=VECTOR('',#32472,1.);
#9714=VECTOR('',#32473,1.);
#9715=VECTOR('',#32478,1.);
#9716=VECTOR('',#32481,1.);
#9717=VECTOR('',#32482,1.);
#9718=VECTOR('',#32489,1.);
#9719=VECTOR('',#32490,1.);
#9720=VECTOR('',#32491,1.);
#9721=VECTOR('',#32492,1.);
#9722=VECTOR('',#32497,1.);
#9723=VECTOR('',#32502,1.);
#9724=VECTOR('',#32503,1.);
#9725=VECTOR('',#32512,1.);
#9726=VECTOR('',#32513,1.);
#9727=VECTOR('',#32514,1.);
#9728=VECTOR('',#32515,1.);
#9729=VECTOR('',#32520,1.);
#9730=VECTOR('',#32523,1.);
#9731=VECTOR('',#32524,1.);
#9732=VECTOR('',#32531,1.);
#9733=VECTOR('',#32532,1.);
#9734=VECTOR('',#32533,1.);
#9735=VECTOR('',#32534,1.);
#9736=VECTOR('',#32539,1.);
#9737=VECTOR('',#32542,1.);
#9738=VECTOR('',#32543,1.);
#9739=VECTOR('',#32550,1.);
#9740=VECTOR('',#32551,1.);
#9741=VECTOR('',#32552,1.);
#9742=VECTOR('',#32553,1.);
#9743=VECTOR('',#32558,1.);
#9744=VECTOR('',#32561,1.);
#9745=VECTOR('',#32562,1.);
#9746=VECTOR('',#32569,1.);
#9747=VECTOR('',#32570,1.);
#9748=VECTOR('',#32571,1.);
#9749=VECTOR('',#32572,1.);
#9750=VECTOR('',#32577,1.);
#9751=VECTOR('',#32580,1.);
#9752=VECTOR('',#32581,1.);
#9753=VECTOR('',#32588,1.);
#9754=VECTOR('',#32589,1.);
#9755=VECTOR('',#32590,1.);
#9756=VECTOR('',#32591,1.);
#9757=VECTOR('',#32596,1.);
#9758=VECTOR('',#32599,1.);
#9759=VECTOR('',#32600,1.);
#9760=VECTOR('',#32607,1.);
#9761=VECTOR('',#32608,1.);
#9762=VECTOR('',#32609,1.);
#9763=VECTOR('',#32610,1.);
#9764=VECTOR('',#32615,1.);
#9765=VECTOR('',#32618,1.);
#9766=VECTOR('',#32619,1.);
#9767=VECTOR('',#32626,1.);
#9768=VECTOR('',#32627,1.);
#9769=VECTOR('',#32628,1.);
#9770=VECTOR('',#32629,1.);
#9771=VECTOR('',#32634,1.);
#9772=VECTOR('',#32637,1.);
#9773=VECTOR('',#32638,1.);
#9774=VECTOR('',#32645,1.);
#9775=VECTOR('',#32646,1.);
#9776=VECTOR('',#32647,1.);
#9777=VECTOR('',#32648,1.);
#9778=VECTOR('',#32653,1.);
#9779=VECTOR('',#32656,1.);
#9780=VECTOR('',#32657,1.);
#9781=VECTOR('',#32664,1.);
#9782=VECTOR('',#32665,1.);
#9783=VECTOR('',#32666,1.);
#9784=VECTOR('',#32667,1.);
#9785=VECTOR('',#32672,1.);
#9786=VECTOR('',#32675,1.);
#9787=VECTOR('',#32676,1.);
#9788=VECTOR('',#32683,1.);
#9789=VECTOR('',#32684,1.);
#9790=VECTOR('',#32685,1.);
#9791=VECTOR('',#32686,1.);
#9792=VECTOR('',#32691,1.);
#9793=VECTOR('',#32694,1.);
#9794=VECTOR('',#32695,1.);
#9795=VECTOR('',#32702,1.);
#9796=VECTOR('',#32703,1.);
#9797=VECTOR('',#32704,1.);
#9798=VECTOR('',#32705,1.);
#9799=VECTOR('',#32710,1.);
#9800=VECTOR('',#32713,1.);
#9801=VECTOR('',#32714,1.);
#9802=VECTOR('',#32721,1.);
#9803=VECTOR('',#32722,1.);
#9804=VECTOR('',#32723,1.);
#9805=VECTOR('',#32724,1.);
#9806=VECTOR('',#32729,1.);
#9807=VECTOR('',#32732,1.);
#9808=VECTOR('',#32733,1.);
#9809=VECTOR('',#32740,1.);
#9810=VECTOR('',#32741,1.);
#9811=VECTOR('',#32742,1.);
#9812=VECTOR('',#32743,1.);
#9813=VECTOR('',#32748,1.);
#9814=VECTOR('',#32751,1.);
#9815=VECTOR('',#32752,1.);
#9816=VECTOR('',#32759,1.);
#9817=VECTOR('',#32760,1.);
#9818=VECTOR('',#32761,1.);
#9819=VECTOR('',#32762,1.);
#9820=VECTOR('',#32767,1.);
#9821=VECTOR('',#32770,1.);
#9822=VECTOR('',#32771,1.);
#9823=VECTOR('',#32778,1.);
#9824=VECTOR('',#32779,1.);
#9825=VECTOR('',#32780,1.);
#9826=VECTOR('',#32781,1.);
#9827=VECTOR('',#32786,1.);
#9828=VECTOR('',#32789,1.);
#9829=VECTOR('',#32790,1.);
#9830=VECTOR('',#32797,1.);
#9831=VECTOR('',#32798,1.);
#9832=VECTOR('',#32799,1.);
#9833=VECTOR('',#32800,1.);
#9834=VECTOR('',#32805,1.);
#9835=VECTOR('',#32808,1.);
#9836=VECTOR('',#32809,1.);
#9837=VECTOR('',#32816,1.);
#9838=VECTOR('',#32817,1.);
#9839=VECTOR('',#32818,1.);
#9840=VECTOR('',#32819,1.);
#9841=VECTOR('',#32824,1.);
#9842=VECTOR('',#32827,1.);
#9843=VECTOR('',#32828,1.);
#9844=VECTOR('',#32837,1.);
#9845=VECTOR('',#32838,1.);
#9846=VECTOR('',#32841,1.);
#9847=VECTOR('',#32842,1.);
#9848=VECTOR('',#32843,1.);
#9849=VECTOR('',#32846,1.);
#9850=VECTOR('',#32847,1.);
#9851=VECTOR('',#32854,1.);
#9852=VECTOR('',#32855,1.);
#9853=VECTOR('',#32856,1.);
#9854=VECTOR('',#32857,1.);
#9855=VECTOR('',#32862,1.);
#9856=VECTOR('',#32865,1.);
#9857=VECTOR('',#32866,1.);
#9858=VECTOR('',#32873,1.);
#9859=VECTOR('',#32874,1.);
#9860=VECTOR('',#32875,1.);
#9861=VECTOR('',#32876,1.);
#9862=VECTOR('',#32881,1.);
#9863=VECTOR('',#32884,1.);
#9864=VECTOR('',#32885,1.);
#9865=VECTOR('',#32892,1.);
#9866=VECTOR('',#32893,1.);
#9867=VECTOR('',#32894,1.);
#9868=VECTOR('',#32895,1.);
#9869=VECTOR('',#32900,1.);
#9870=VECTOR('',#32903,1.);
#9871=VECTOR('',#32904,1.);
#9872=VECTOR('',#32911,1.);
#9873=VECTOR('',#32912,1.);
#9874=VECTOR('',#32913,1.);
#9875=VECTOR('',#32914,1.);
#9876=VECTOR('',#32919,1.);
#9877=VECTOR('',#32922,1.);
#9878=VECTOR('',#32923,1.);
#9879=VECTOR('',#32930,1.);
#9880=VECTOR('',#32931,1.);
#9881=VECTOR('',#32932,1.);
#9882=VECTOR('',#32933,1.);
#9883=VECTOR('',#32938,1.);
#9884=VECTOR('',#32941,1.);
#9885=VECTOR('',#32942,1.);
#9886=VECTOR('',#32949,1.);
#9887=VECTOR('',#32950,1.);
#9888=VECTOR('',#32951,1.);
#9889=VECTOR('',#32952,1.);
#9890=VECTOR('',#32957,1.);
#9891=VECTOR('',#32960,1.);
#9892=VECTOR('',#32961,1.);
#9893=VECTOR('',#32968,1.);
#9894=VECTOR('',#32969,1.);
#9895=VECTOR('',#32970,1.);
#9896=VECTOR('',#32971,1.);
#9897=VECTOR('',#32976,1.);
#9898=VECTOR('',#32979,1.);
#9899=VECTOR('',#32980,1.);
#9900=VECTOR('',#32987,1.);
#9901=VECTOR('',#32988,1.);
#9902=VECTOR('',#32989,1.);
#9903=VECTOR('',#32990,1.);
#9904=VECTOR('',#32995,1.);
#9905=VECTOR('',#32998,1.);
#9906=VECTOR('',#32999,1.);
#9907=VECTOR('',#33006,1.);
#9908=VECTOR('',#33007,1.);
#9909=VECTOR('',#33008,1.);
#9910=VECTOR('',#33009,1.);
#9911=VECTOR('',#33014,1.);
#9912=VECTOR('',#33017,1.);
#9913=VECTOR('',#33018,1.);
#9914=VECTOR('',#33029,0.375);
#9915=VECTOR('',#33034,0.635);
#9916=VECTOR('',#33069,0.65);
#9917=VECTOR('',#33114,0.625);
#11846=VERTEX_POINT('',#50313);
#11847=VERTEX_POINT('',#50314);
#11848=VERTEX_POINT('',#50316);
#11849=VERTEX_POINT('',#50327);
#11850=VERTEX_POINT('',#50337);
#11851=VERTEX_POINT('',#50338);
#11852=VERTEX_POINT('',#50385);
#11853=VERTEX_POINT('',#50386);
#11854=VERTEX_POINT('',#50433);
#11855=VERTEX_POINT('',#50434);
#11856=VERTEX_POINT('',#50487);
#11857=VERTEX_POINT('',#50488);
#11858=VERTEX_POINT('',#50535);
#11859=VERTEX_POINT('',#50536);
#11860=VERTEX_POINT('',#50583);
#11861=VERTEX_POINT('',#50584);
#11862=VERTEX_POINT('',#50637);
#11863=VERTEX_POINT('',#50638);
#11864=VERTEX_POINT('',#50685);
#11865=VERTEX_POINT('',#50686);
#11866=VERTEX_POINT('',#50733);
#11867=VERTEX_POINT('',#50734);
#11868=VERTEX_POINT('',#50787);
#11869=VERTEX_POINT('',#50788);
#11870=VERTEX_POINT('',#50835);
#11871=VERTEX_POINT('',#50836);
#11872=VERTEX_POINT('',#50883);
#11873=VERTEX_POINT('',#50884);
#11874=VERTEX_POINT('',#50937);
#11875=VERTEX_POINT('',#50938);
#11876=VERTEX_POINT('',#50985);
#11877=VERTEX_POINT('',#50986);
#11878=VERTEX_POINT('',#51033);
#11879=VERTEX_POINT('',#51034);
#11880=VERTEX_POINT('',#51087);
#11881=VERTEX_POINT('',#51088);
#11882=VERTEX_POINT('',#51090);
#11883=VERTEX_POINT('',#51100);
#11884=VERTEX_POINT('',#51110);
#11885=VERTEX_POINT('',#51111);
#11886=VERTEX_POINT('',#51135);
#11887=VERTEX_POINT('',#51136);
#11888=VERTEX_POINT('',#51159);
#11889=VERTEX_POINT('',#51160);
#11890=VERTEX_POINT('',#51184);
#11891=VERTEX_POINT('',#51185);
#11892=VERTEX_POINT('',#51209);
#11893=VERTEX_POINT('',#51210);
#11894=VERTEX_POINT('',#51233);
#11895=VERTEX_POINT('',#51234);
#11896=VERTEX_POINT('',#51258);
#11897=VERTEX_POINT('',#51259);
#11898=VERTEX_POINT('',#51283);
#11899=VERTEX_POINT('',#51284);
#11900=VERTEX_POINT('',#51307);
#11901=VERTEX_POINT('',#51308);
#11902=VERTEX_POINT('',#51332);
#11903=VERTEX_POINT('',#51333);
#11904=VERTEX_POINT('',#51357);
#11905=VERTEX_POINT('',#51358);
#11906=VERTEX_POINT('',#51381);
#11907=VERTEX_POINT('',#51382);
#11908=VERTEX_POINT('',#51406);
#11909=VERTEX_POINT('',#51407);
#11910=VERTEX_POINT('',#51431);
#11911=VERTEX_POINT('',#51432);
#11912=VERTEX_POINT('',#51455);
#11913=VERTEX_POINT('',#51517);
#11914=VERTEX_POINT('',#51519);
#11915=VERTEX_POINT('',#52001);
#11916=VERTEX_POINT('',#52073);
#11917=VERTEX_POINT('',#52076);
#11918=VERTEX_POINT('',#52565);
#11919=VERTEX_POINT('',#52571);
#11920=VERTEX_POINT('',#52574);
#11921=VERTEX_POINT('',#52575);
#11922=VERTEX_POINT('',#52579);
#11923=VERTEX_POINT('',#52583);
#11924=VERTEX_POINT('',#52587);
#11925=VERTEX_POINT('',#52591);
#11926=VERTEX_POINT('',#52598);
#11927=VERTEX_POINT('',#52601);
#11928=VERTEX_POINT('',#52602);
#11929=VERTEX_POINT('',#52607);
#11930=VERTEX_POINT('',#52611);
#11931=VERTEX_POINT('',#52615);
#11932=VERTEX_POINT('',#52619);
#11933=VERTEX_POINT('',#52625);
#11934=VERTEX_POINT('',#52626);
#11935=VERTEX_POINT('',#52628);
#11936=VERTEX_POINT('',#52630);
#11937=VERTEX_POINT('',#52634);
#11938=VERTEX_POINT('',#52638);
#11939=VERTEX_POINT('',#52644);
#11940=VERTEX_POINT('',#52645);
#11941=VERTEX_POINT('',#52647);
#11942=VERTEX_POINT('',#52649);
#11943=VERTEX_POINT('',#52653);
#11944=VERTEX_POINT('',#52657);
#11945=VERTEX_POINT('',#52663);
#11946=VERTEX_POINT('',#52664);
#11947=VERTEX_POINT('',#52666);
#11948=VERTEX_POINT('',#52668);
#11949=VERTEX_POINT('',#52672);
#11950=VERTEX_POINT('',#52676);
#11951=VERTEX_POINT('',#52682);
#11952=VERTEX_POINT('',#52683);
#11953=VERTEX_POINT('',#52685);
#11954=VERTEX_POINT('',#52687);
#11955=VERTEX_POINT('',#52691);
#11956=VERTEX_POINT('',#52695);
#11957=VERTEX_POINT('',#52701);
#11958=VERTEX_POINT('',#52702);
#11959=VERTEX_POINT('',#52704);
#11960=VERTEX_POINT('',#52706);
#11961=VERTEX_POINT('',#52710);
#11962=VERTEX_POINT('',#52714);
#11963=VERTEX_POINT('',#52720);
#11964=VERTEX_POINT('',#52721);
#11965=VERTEX_POINT('',#52723);
#11966=VERTEX_POINT('',#52725);
#11967=VERTEX_POINT('',#52729);
#11968=VERTEX_POINT('',#52733);
#11969=VERTEX_POINT('',#52739);
#11970=VERTEX_POINT('',#52740);
#11971=VERTEX_POINT('',#52742);
#11972=VERTEX_POINT('',#52744);
#11973=VERTEX_POINT('',#52748);
#11974=VERTEX_POINT('',#52752);
#11975=VERTEX_POINT('',#52758);
#11976=VERTEX_POINT('',#52759);
#11977=VERTEX_POINT('',#52761);
#11978=VERTEX_POINT('',#52763);
#11979=VERTEX_POINT('',#52767);
#11980=VERTEX_POINT('',#52771);
#11981=VERTEX_POINT('',#52777);
#11982=VERTEX_POINT('',#52778);
#11983=VERTEX_POINT('',#52780);
#11984=VERTEX_POINT('',#52782);
#11985=VERTEX_POINT('',#52786);
#11986=VERTEX_POINT('',#52788);
#11987=VERTEX_POINT('',#52792);
#11988=VERTEX_POINT('',#52796);
#11989=VERTEX_POINT('',#52800);
#11990=VERTEX_POINT('',#52801);
#11991=VERTEX_POINT('',#52803);
#11992=VERTEX_POINT('',#52805);
#11993=VERTEX_POINT('',#52809);
#11994=VERTEX_POINT('',#52813);
#11995=VERTEX_POINT('',#52819);
#11996=VERTEX_POINT('',#52820);
#11997=VERTEX_POINT('',#52822);
#11998=VERTEX_POINT('',#52824);
#11999=VERTEX_POINT('',#52828);
#12000=VERTEX_POINT('',#52832);
#12001=VERTEX_POINT('',#52838);
#12002=VERTEX_POINT('',#52839);
#12003=VERTEX_POINT('',#52841);
#12004=VERTEX_POINT('',#52843);
#12005=VERTEX_POINT('',#52847);
#12006=VERTEX_POINT('',#52851);
#12007=VERTEX_POINT('',#52857);
#12008=VERTEX_POINT('',#52858);
#12009=VERTEX_POINT('',#52860);
#12010=VERTEX_POINT('',#52862);
#12011=VERTEX_POINT('',#52866);
#12012=VERTEX_POINT('',#52870);
#12013=VERTEX_POINT('',#52876);
#12014=VERTEX_POINT('',#52877);
#12015=VERTEX_POINT('',#52879);
#12016=VERTEX_POINT('',#52881);
#12017=VERTEX_POINT('',#52885);
#12018=VERTEX_POINT('',#52889);
#12019=VERTEX_POINT('',#52895);
#12020=VERTEX_POINT('',#52896);
#12021=VERTEX_POINT('',#52898);
#12022=VERTEX_POINT('',#52900);
#12023=VERTEX_POINT('',#52904);
#12024=VERTEX_POINT('',#52908);
#12025=VERTEX_POINT('',#52914);
#12026=VERTEX_POINT('',#52915);
#12027=VERTEX_POINT('',#52917);
#12028=VERTEX_POINT('',#52919);
#12029=VERTEX_POINT('',#52923);
#12030=VERTEX_POINT('',#52927);
#12031=VERTEX_POINT('',#52933);
#12032=VERTEX_POINT('',#52934);
#12033=VERTEX_POINT('',#52936);
#12034=VERTEX_POINT('',#52938);
#12035=VERTEX_POINT('',#52942);
#12036=VERTEX_POINT('',#52946);
#12037=VERTEX_POINT('',#52952);
#12038=VERTEX_POINT('',#52953);
#12039=VERTEX_POINT('',#52955);
#12040=VERTEX_POINT('',#52957);
#12041=VERTEX_POINT('',#52961);
#12042=VERTEX_POINT('',#52965);
#12043=VERTEX_POINT('',#52971);
#12044=VERTEX_POINT('',#52972);
#12045=VERTEX_POINT('',#52974);
#12046=VERTEX_POINT('',#52976);
#12047=VERTEX_POINT('',#52980);
#12048=VERTEX_POINT('',#52984);
#12049=VERTEX_POINT('',#52990);
#12050=VERTEX_POINT('',#52991);
#12051=VERTEX_POINT('',#52993);
#12052=VERTEX_POINT('',#52995);
#12053=VERTEX_POINT('',#52999);
#12054=VERTEX_POINT('',#53003);
#12055=VERTEX_POINT('',#53009);
#12056=VERTEX_POINT('',#53010);
#12057=VERTEX_POINT('',#53012);
#12058=VERTEX_POINT('',#53014);
#12059=VERTEX_POINT('',#53018);
#12060=VERTEX_POINT('',#53022);
#12061=VERTEX_POINT('',#53028);
#12062=VERTEX_POINT('',#53029);
#12063=VERTEX_POINT('',#53031);
#12064=VERTEX_POINT('',#53033);
#12065=VERTEX_POINT('',#53037);
#12066=VERTEX_POINT('',#53041);
#12067=VERTEX_POINT('',#53047);
#12068=VERTEX_POINT('',#53048);
#12069=VERTEX_POINT('',#53050);
#12070=VERTEX_POINT('',#53052);
#12071=VERTEX_POINT('',#53056);
#12072=VERTEX_POINT('',#53060);
#12073=VERTEX_POINT('',#53066);
#12074=VERTEX_POINT('',#53067);
#12075=VERTEX_POINT('',#53069);
#12076=VERTEX_POINT('',#53071);
#12077=VERTEX_POINT('',#53075);
#12078=VERTEX_POINT('',#53079);
#12079=VERTEX_POINT('',#53085);
#12080=VERTEX_POINT('',#53086);
#12081=VERTEX_POINT('',#53088);
#12082=VERTEX_POINT('',#53090);
#12083=VERTEX_POINT('',#53094);
#12084=VERTEX_POINT('',#53098);
#12085=VERTEX_POINT('',#53104);
#12086=VERTEX_POINT('',#53105);
#12087=VERTEX_POINT('',#53107);
#12088=VERTEX_POINT('',#53109);
#12089=VERTEX_POINT('',#53113);
#12090=VERTEX_POINT('',#53117);
#12091=VERTEX_POINT('',#53123);
#12092=VERTEX_POINT('',#53124);
#12093=VERTEX_POINT('',#53126);
#12094=VERTEX_POINT('',#53130);
#12095=VERTEX_POINT('',#53132);
#12096=VERTEX_POINT('',#53136);
#12097=VERTEX_POINT('',#53142);
#12098=VERTEX_POINT('',#53143);
#12099=VERTEX_POINT('',#53145);
#12100=VERTEX_POINT('',#53147);
#12101=VERTEX_POINT('',#53151);
#12102=VERTEX_POINT('',#53155);
#12103=VERTEX_POINT('',#53161);
#12104=VERTEX_POINT('',#53162);
#12105=VERTEX_POINT('',#53164);
#12106=VERTEX_POINT('',#53166);
#12107=VERTEX_POINT('',#53170);
#12108=VERTEX_POINT('',#53174);
#12109=VERTEX_POINT('',#53180);
#12110=VERTEX_POINT('',#53181);
#12111=VERTEX_POINT('',#53183);
#12112=VERTEX_POINT('',#53185);
#12113=VERTEX_POINT('',#53189);
#12114=VERTEX_POINT('',#53193);
#12115=VERTEX_POINT('',#53199);
#12116=VERTEX_POINT('',#53200);
#12117=VERTEX_POINT('',#53202);
#12118=VERTEX_POINT('',#53204);
#12119=VERTEX_POINT('',#53208);
#12120=VERTEX_POINT('',#53212);
#12121=VERTEX_POINT('',#53218);
#12122=VERTEX_POINT('',#53219);
#12123=VERTEX_POINT('',#53221);
#12124=VERTEX_POINT('',#53223);
#12125=VERTEX_POINT('',#53227);
#12126=VERTEX_POINT('',#53231);
#12127=VERTEX_POINT('',#53237);
#12128=VERTEX_POINT('',#53238);
#12129=VERTEX_POINT('',#53240);
#12130=VERTEX_POINT('',#53242);
#12131=VERTEX_POINT('',#53246);
#12132=VERTEX_POINT('',#53250);
#12133=VERTEX_POINT('',#53256);
#12134=VERTEX_POINT('',#53257);
#12135=VERTEX_POINT('',#53259);
#12136=VERTEX_POINT('',#53261);
#12137=VERTEX_POINT('',#53265);
#12138=VERTEX_POINT('',#53269);
#12139=VERTEX_POINT('',#53275);
#12140=VERTEX_POINT('',#53276);
#12141=VERTEX_POINT('',#53278);
#12142=VERTEX_POINT('',#53280);
#12143=VERTEX_POINT('',#53284);
#12144=VERTEX_POINT('',#53288);
#12145=VERTEX_POINT('',#53294);
#12146=VERTEX_POINT('',#53295);
#12147=VERTEX_POINT('',#53297);
#12148=VERTEX_POINT('',#53299);
#12149=VERTEX_POINT('',#53303);
#12150=VERTEX_POINT('',#53307);
#12151=VERTEX_POINT('',#53313);
#12152=VERTEX_POINT('',#53318);
#12153=VERTEX_POINT('',#53360);
#14817=EDGE_CURVE('',#11846,#11847,#7456,.T.);
#14818=EDGE_CURVE('',#11846,#11848,#441,.T.);
#14819=EDGE_CURVE('',#11848,#11849,#6090,.T.);
#14820=EDGE_CURVE('',#11849,#11847,#442,.T.);
#14821=EDGE_CURVE('',#11850,#11851,#7457,.T.);
#14822=EDGE_CURVE('',#11850,#11846,#443,.T.);
#14823=EDGE_CURVE('',#11847,#11851,#444,.T.);
#14824=EDGE_CURVE('',#11852,#11853,#7458,.T.);
#14825=EDGE_CURVE('',#11852,#11850,#445,.T.);
#14826=EDGE_CURVE('',#11851,#11853,#446,.T.);
#14827=EDGE_CURVE('',#11854,#11855,#7459,.T.);
#14828=EDGE_CURVE('',#11854,#11852,#447,.T.);
#14829=EDGE_CURVE('',#11853,#11855,#448,.T.);
#14830=EDGE_CURVE('',#11856,#11857,#7460,.T.);
#14831=EDGE_CURVE('',#11856,#11854,#449,.T.);
#14832=EDGE_CURVE('',#11855,#11857,#450,.T.);
#14833=EDGE_CURVE('',#11858,#11859,#7461,.T.);
#14834=EDGE_CURVE('',#11858,#11856,#451,.T.);
#14835=EDGE_CURVE('',#11857,#11859,#452,.T.);
#14836=EDGE_CURVE('',#11860,#11861,#7462,.T.);
#14837=EDGE_CURVE('',#11860,#11858,#453,.T.);
#14838=EDGE_CURVE('',#11859,#11861,#454,.T.);
#14839=EDGE_CURVE('',#11862,#11863,#7463,.T.);
#14840=EDGE_CURVE('',#11862,#11860,#455,.T.);
#14841=EDGE_CURVE('',#11861,#11863,#456,.T.);
#14842=EDGE_CURVE('',#11864,#11865,#7464,.T.);
#14843=EDGE_CURVE('',#11864,#11862,#457,.T.);
#14844=EDGE_CURVE('',#11863,#11865,#458,.T.);
#14845=EDGE_CURVE('',#11866,#11867,#7465,.T.);
#14846=EDGE_CURVE('',#11866,#11864,#459,.T.);
#14847=EDGE_CURVE('',#11865,#11867,#460,.T.);
#14848=EDGE_CURVE('',#11868,#11869,#7466,.T.);
#14849=EDGE_CURVE('',#11868,#11866,#461,.T.);
#14850=EDGE_CURVE('',#11867,#11869,#462,.T.);
#14851=EDGE_CURVE('',#11870,#11871,#7467,.T.);
#14852=EDGE_CURVE('',#11870,#11868,#463,.T.);
#14853=EDGE_CURVE('',#11869,#11871,#464,.T.);
#14854=EDGE_CURVE('',#11872,#11873,#7468,.T.);
#14855=EDGE_CURVE('',#11872,#11870,#465,.T.);
#14856=EDGE_CURVE('',#11871,#11873,#466,.T.);
#14857=EDGE_CURVE('',#11874,#11875,#7469,.T.);
#14858=EDGE_CURVE('',#11874,#11872,#467,.T.);
#14859=EDGE_CURVE('',#11873,#11875,#468,.T.);
#14860=EDGE_CURVE('',#11876,#11877,#7470,.T.);
#14861=EDGE_CURVE('',#11876,#11874,#469,.T.);
#14862=EDGE_CURVE('',#11875,#11877,#470,.T.);
#14863=EDGE_CURVE('',#11878,#11879,#7471,.T.);
#14864=EDGE_CURVE('',#11878,#11876,#471,.T.);
#14865=EDGE_CURVE('',#11877,#11879,#472,.T.);
#14866=EDGE_CURVE('',#11880,#11881,#7472,.T.);
#14867=EDGE_CURVE('',#11880,#11882,#473,.T.);
#14868=EDGE_CURVE('',#11883,#11882,#6091,.T.);
#14869=EDGE_CURVE('',#11881,#11883,#474,.T.);
#14870=EDGE_CURVE('',#11884,#11885,#7473,.T.);
#14871=EDGE_CURVE('',#11884,#11880,#475,.T.);
#14872=EDGE_CURVE('',#11885,#11881,#476,.T.);
#14873=EDGE_CURVE('',#11886,#11887,#7474,.T.);
#14874=EDGE_CURVE('',#11886,#11884,#477,.T.);
#14875=EDGE_CURVE('',#11887,#11885,#478,.T.);
#14876=EDGE_CURVE('',#11888,#11889,#7475,.T.);
#14877=EDGE_CURVE('',#11888,#11886,#479,.T.);
#14878=EDGE_CURVE('',#11889,#11887,#480,.T.);
#14879=EDGE_CURVE('',#11890,#11891,#7476,.T.);
#14880=EDGE_CURVE('',#11890,#11888,#481,.T.);
#14881=EDGE_CURVE('',#11891,#11889,#482,.T.);
#14882=EDGE_CURVE('',#11892,#11893,#7477,.T.);
#14883=EDGE_CURVE('',#11892,#11890,#483,.T.);
#14884=EDGE_CURVE('',#11893,#11891,#484,.T.);
#14885=EDGE_CURVE('',#11894,#11895,#7478,.T.);
#14886=EDGE_CURVE('',#11894,#11892,#485,.T.);
#14887=EDGE_CURVE('',#11895,#11893,#486,.T.);
#14888=EDGE_CURVE('',#11896,#11897,#7479,.T.);
#14889=EDGE_CURVE('',#11896,#11894,#487,.T.);
#14890=EDGE_CURVE('',#11897,#11895,#488,.T.);
#14891=EDGE_CURVE('',#11898,#11899,#7480,.T.);
#14892=EDGE_CURVE('',#11898,#11896,#489,.T.);
#14893=EDGE_CURVE('',#11899,#11897,#490,.T.);
#14894=EDGE_CURVE('',#11900,#11901,#7481,.T.);
#14895=EDGE_CURVE('',#11900,#11898,#491,.T.);
#14896=EDGE_CURVE('',#11901,#11899,#492,.T.);
#14897=EDGE_CURVE('',#11902,#11903,#7482,.T.);
#14898=EDGE_CURVE('',#11902,#11900,#493,.T.);
#14899=EDGE_CURVE('',#11903,#11901,#494,.T.);
#14900=EDGE_CURVE('',#11904,#11905,#7483,.T.);
#14901=EDGE_CURVE('',#11904,#11902,#495,.T.);
#14902=EDGE_CURVE('',#11905,#11903,#496,.T.);
#14903=EDGE_CURVE('',#11906,#11907,#7484,.T.);
#14904=EDGE_CURVE('',#11906,#11904,#497,.T.);
#14905=EDGE_CURVE('',#11907,#11905,#498,.T.);
#14906=EDGE_CURVE('',#11908,#11909,#7485,.T.);
#14907=EDGE_CURVE('',#11908,#11906,#499,.T.);
#14908=EDGE_CURVE('',#11909,#11907,#500,.T.);
#14909=EDGE_CURVE('',#11910,#11911,#7486,.T.);
#14910=EDGE_CURVE('',#11910,#11908,#501,.T.);
#14911=EDGE_CURVE('',#11911,#11909,#502,.T.);
#14912=EDGE_CURVE('',#11882,#11912,#503,.T.);
#14913=EDGE_CURVE('',#11913,#11912,#6092,.T.);
#14914=EDGE_CURVE('',#11914,#11913,#6093,.T.);
#14915=EDGE_CURVE('',#11914,#11883,#504,.T.);
#14916=EDGE_CURVE('',#11879,#11914,#505,.T.);
#14917=EDGE_CURVE('',#11915,#11849,#506,.T.);
#14918=EDGE_CURVE('',#11915,#11911,#507,.T.);
#14919=EDGE_CURVE('',#11849,#11916,#6094,.T.);
#14920=EDGE_CURVE('',#11916,#11848,#6095,.T.);
#14921=EDGE_CURVE('',#11848,#11917,#508,.T.);
#14922=EDGE_CURVE('',#11917,#11915,#6096,.T.);
#14923=EDGE_CURVE('',#11917,#11910,#509,.T.);
#14924=EDGE_CURVE('',#11912,#11878,#510,.T.);
#14925=EDGE_CURVE('',#11913,#11918,#6097,.T.);
#14926=EDGE_CURVE('',#11918,#11918,#6098,.T.);
#14927=EDGE_CURVE('',#11912,#11914,#6099,.T.);
#14928=EDGE_CURVE('',#11919,#11919,#6100,.T.);
#14929=EDGE_CURVE('',#11920,#11921,#7487,.T.);
#14930=EDGE_CURVE('',#11921,#11920,#6101,.T.);
#14931=EDGE_CURVE('',#11921,#11922,#7488,.T.);
#14932=EDGE_CURVE('',#11922,#11921,#6102,.T.);
#14933=EDGE_CURVE('',#11922,#11923,#7489,.T.);
#14934=EDGE_CURVE('',#11923,#11922,#6103,.T.);
#14935=EDGE_CURVE('',#11923,#11924,#7490,.T.);
#14936=EDGE_CURVE('',#11924,#11923,#6104,.T.);
#14937=EDGE_CURVE('',#11924,#11925,#7491,.T.);
#14938=EDGE_CURVE('',#11925,#11924,#6105,.T.);
#14939=EDGE_CURVE('',#11925,#11920,#7492,.T.);
#14940=EDGE_CURVE('',#11920,#11925,#6106,.T.);
#14941=EDGE_CURVE('',#11926,#11924,#7493,.T.);
#14942=EDGE_CURVE('',#11927,#11928,#7494,.T.);
#14943=EDGE_CURVE('',#11927,#11920,#7495,.T.);
#14944=EDGE_CURVE('',#11928,#11921,#7496,.T.);
#14945=EDGE_CURVE('',#11929,#11927,#7497,.T.);
#14946=EDGE_CURVE('',#11929,#11925,#7498,.T.);
#14947=EDGE_CURVE('',#11930,#11929,#7499,.T.);
#14948=EDGE_CURVE('',#11930,#11924,#7500,.T.);
#14949=EDGE_CURVE('',#11931,#11930,#7501,.T.);
#14950=EDGE_CURVE('',#11931,#11923,#7502,.T.);
#14951=EDGE_CURVE('',#11932,#11931,#7503,.T.);
#14952=EDGE_CURVE('',#11932,#11922,#7504,.T.);
#14953=EDGE_CURVE('',#11928,#11932,#7505,.T.);
#14954=EDGE_CURVE('',#11933,#11934,#7506,.T.);
#14955=EDGE_CURVE('',#11933,#11935,#7507,.T.);
#14956=EDGE_CURVE('',#11936,#11935,#7508,.T.);
#14957=EDGE_CURVE('',#11934,#11936,#7509,.T.);
#14958=EDGE_CURVE('',#11934,#11937,#6107,.T.);
#14959=EDGE_CURVE('',#11936,#11937,#7510,.T.);
#14960=EDGE_CURVE('',#11937,#11938,#7511,.T.);
#14961=EDGE_CURVE('',#11935,#11938,#7512,.T.);
#14962=EDGE_CURVE('',#11938,#11933,#6108,.T.);
#14963=EDGE_CURVE('',#11939,#11940,#7513,.T.);
#14964=EDGE_CURVE('',#11939,#11941,#7514,.T.);
#14965=EDGE_CURVE('',#11942,#11941,#7515,.T.);
#14966=EDGE_CURVE('',#11940,#11942,#7516,.T.);
#14967=EDGE_CURVE('',#11940,#11943,#6109,.T.);
#14968=EDGE_CURVE('',#11942,#11943,#7517,.T.);
#14969=EDGE_CURVE('',#11943,#11944,#7518,.T.);
#14970=EDGE_CURVE('',#11941,#11944,#7519,.T.);
#14971=EDGE_CURVE('',#11944,#11939,#6110,.T.);
#14972=EDGE_CURVE('',#11945,#11946,#7520,.T.);
#14973=EDGE_CURVE('',#11945,#11947,#7521,.T.);
#14974=EDGE_CURVE('',#11948,#11947,#7522,.T.);
#14975=EDGE_CURVE('',#11946,#11948,#7523,.T.);
#14976=EDGE_CURVE('',#11946,#11949,#6111,.T.);
#14977=EDGE_CURVE('',#11948,#11949,#7524,.T.);
#14978=EDGE_CURVE('',#11949,#11950,#7525,.T.);
#14979=EDGE_CURVE('',#11947,#11950,#7526,.T.);
#14980=EDGE_CURVE('',#11950,#11945,#6112,.T.);
#14981=EDGE_CURVE('',#11951,#11952,#7527,.T.);
#14982=EDGE_CURVE('',#11951,#11953,#7528,.T.);
#14983=EDGE_CURVE('',#11954,#11953,#7529,.T.);
#14984=EDGE_CURVE('',#11952,#11954,#7530,.T.);
#14985=EDGE_CURVE('',#11952,#11955,#6113,.T.);
#14986=EDGE_CURVE('',#11954,#11955,#7531,.T.);
#14987=EDGE_CURVE('',#11955,#11956,#7532,.T.);
#14988=EDGE_CURVE('',#11953,#11956,#7533,.T.);
#14989=EDGE_CURVE('',#11956,#11951,#6114,.T.);
#14990=EDGE_CURVE('',#11957,#11958,#7534,.T.);
#14991=EDGE_CURVE('',#11957,#11959,#7535,.T.);
#14992=EDGE_CURVE('',#11960,#11959,#7536,.T.);
#14993=EDGE_CURVE('',#11958,#11960,#7537,.T.);
#14994=EDGE_CURVE('',#11958,#11961,#6115,.T.);
#14995=EDGE_CURVE('',#11960,#11961,#7538,.T.);
#14996=EDGE_CURVE('',#11961,#11962,#7539,.T.);
#14997=EDGE_CURVE('',#11959,#11962,#7540,.T.);
#14998=EDGE_CURVE('',#11962,#11957,#6116,.T.);
#14999=EDGE_CURVE('',#11963,#11964,#7541,.T.);
#15000=EDGE_CURVE('',#11963,#11965,#7542,.T.);
#15001=EDGE_CURVE('',#11966,#11965,#7543,.T.);
#15002=EDGE_CURVE('',#11964,#11966,#7544,.T.);
#15003=EDGE_CURVE('',#11964,#11967,#6117,.T.);
#15004=EDGE_CURVE('',#11966,#11967,#7545,.T.);
#15005=EDGE_CURVE('',#11967,#11968,#7546,.T.);
#15006=EDGE_CURVE('',#11965,#11968,#7547,.T.);
#15007=EDGE_CURVE('',#11968,#11963,#6118,.T.);
#15008=EDGE_CURVE('',#11969,#11970,#7548,.T.);
#15009=EDGE_CURVE('',#11969,#11971,#7549,.T.);
#15010=EDGE_CURVE('',#11972,#11971,#7550,.T.);
#15011=EDGE_CURVE('',#11970,#11972,#7551,.T.);
#15012=EDGE_CURVE('',#11970,#11973,#6119,.T.);
#15013=EDGE_CURVE('',#11972,#11973,#7552,.T.);
#15014=EDGE_CURVE('',#11973,#11974,#7553,.T.);
#15015=EDGE_CURVE('',#11971,#11974,#7554,.T.);
#15016=EDGE_CURVE('',#11974,#11969,#6120,.T.);
#15017=EDGE_CURVE('',#11975,#11976,#7555,.T.);
#15018=EDGE_CURVE('',#11975,#11977,#7556,.T.);
#15019=EDGE_CURVE('',#11978,#11977,#7557,.T.);
#15020=EDGE_CURVE('',#11976,#11978,#7558,.T.);
#15021=EDGE_CURVE('',#11976,#11979,#6121,.T.);
#15022=EDGE_CURVE('',#11978,#11979,#7559,.T.);
#15023=EDGE_CURVE('',#11979,#11980,#7560,.T.);
#15024=EDGE_CURVE('',#11977,#11980,#7561,.T.);
#15025=EDGE_CURVE('',#11980,#11975,#6122,.T.);
#15026=EDGE_CURVE('',#11981,#11982,#7562,.T.);
#15027=EDGE_CURVE('',#11981,#11983,#7563,.T.);
#15028=EDGE_CURVE('',#11984,#11983,#7564,.T.);
#15029=EDGE_CURVE('',#11982,#11984,#7565,.T.);
#15030=EDGE_CURVE('',#11982,#11985,#6123,.T.);
#15031=EDGE_CURVE('',#11984,#11986,#7566,.T.);
#15032=EDGE_CURVE('',#11985,#11986,#6124,.T.);
#15033=EDGE_CURVE('',#11986,#11987,#7567,.T.);
#15034=EDGE_CURVE('',#11983,#11987,#7568,.T.);
#15035=EDGE_CURVE('',#11987,#11988,#6125,.T.);
#15036=EDGE_CURVE('',#11988,#11981,#6126,.T.);
#15037=EDGE_CURVE('',#11989,#11990,#7569,.T.);
#15038=EDGE_CURVE('',#11989,#11991,#7570,.T.);
#15039=EDGE_CURVE('',#11992,#11991,#7571,.T.);
#15040=EDGE_CURVE('',#11990,#11992,#7572,.T.);
#15041=EDGE_CURVE('',#11990,#11993,#6127,.T.);
#15042=EDGE_CURVE('',#11992,#11993,#7573,.T.);
#15043=EDGE_CURVE('',#11993,#11994,#7574,.T.);
#15044=EDGE_CURVE('',#11991,#11994,#7575,.T.);
#15045=EDGE_CURVE('',#11994,#11989,#6128,.T.);
#15046=EDGE_CURVE('',#11995,#11996,#7576,.T.);
#15047=EDGE_CURVE('',#11995,#11997,#7577,.T.);
#15048=EDGE_CURVE('',#11998,#11997,#7578,.T.);
#15049=EDGE_CURVE('',#11996,#11998,#7579,.T.);
#15050=EDGE_CURVE('',#11996,#11999,#6129,.T.);
#15051=EDGE_CURVE('',#11998,#11999,#7580,.T.);
#15052=EDGE_CURVE('',#11999,#12000,#7581,.T.);
#15053=EDGE_CURVE('',#11997,#12000,#7582,.T.);
#15054=EDGE_CURVE('',#12000,#11995,#6130,.T.);
#15055=EDGE_CURVE('',#12001,#12002,#7583,.T.);
#15056=EDGE_CURVE('',#12001,#12003,#7584,.T.);
#15057=EDGE_CURVE('',#12004,#12003,#7585,.T.);
#15058=EDGE_CURVE('',#12002,#12004,#7586,.T.);
#15059=EDGE_CURVE('',#12002,#12005,#6131,.T.);
#15060=EDGE_CURVE('',#12004,#12005,#7587,.T.);
#15061=EDGE_CURVE('',#12005,#12006,#7588,.T.);
#15062=EDGE_CURVE('',#12003,#12006,#7589,.T.);
#15063=EDGE_CURVE('',#12006,#12001,#6132,.T.);
#15064=EDGE_CURVE('',#12007,#12008,#7590,.T.);
#15065=EDGE_CURVE('',#12007,#12009,#7591,.T.);
#15066=EDGE_CURVE('',#12010,#12009,#7592,.T.);
#15067=EDGE_CURVE('',#12008,#12010,#7593,.T.);
#15068=EDGE_CURVE('',#12008,#12011,#6133,.T.);
#15069=EDGE_CURVE('',#12010,#12011,#7594,.T.);
#15070=EDGE_CURVE('',#12011,#12012,#7595,.T.);
#15071=EDGE_CURVE('',#12009,#12012,#7596,.T.);
#15072=EDGE_CURVE('',#12012,#12007,#6134,.T.);
#15073=EDGE_CURVE('',#12013,#12014,#7597,.T.);
#15074=EDGE_CURVE('',#12013,#12015,#7598,.T.);
#15075=EDGE_CURVE('',#12016,#12015,#7599,.T.);
#15076=EDGE_CURVE('',#12014,#12016,#7600,.T.);
#15077=EDGE_CURVE('',#12014,#12017,#6135,.T.);
#15078=EDGE_CURVE('',#12016,#12017,#7601,.T.);
#15079=EDGE_CURVE('',#12017,#12018,#7602,.T.);
#15080=EDGE_CURVE('',#12015,#12018,#7603,.T.);
#15081=EDGE_CURVE('',#12018,#12013,#6136,.T.);
#15082=EDGE_CURVE('',#12019,#12020,#7604,.T.);
#15083=EDGE_CURVE('',#12019,#12021,#7605,.T.);
#15084=EDGE_CURVE('',#12022,#12021,#7606,.T.);
#15085=EDGE_CURVE('',#12020,#12022,#7607,.T.);
#15086=EDGE_CURVE('',#12020,#12023,#6137,.T.);
#15087=EDGE_CURVE('',#12022,#12023,#7608,.T.);
#15088=EDGE_CURVE('',#12023,#12024,#7609,.T.);
#15089=EDGE_CURVE('',#12021,#12024,#7610,.T.);
#15090=EDGE_CURVE('',#12024,#12019,#6138,.T.);
#15091=EDGE_CURVE('',#12025,#12026,#7611,.T.);
#15092=EDGE_CURVE('',#12025,#12027,#7612,.T.);
#15093=EDGE_CURVE('',#12028,#12027,#7613,.T.);
#15094=EDGE_CURVE('',#12026,#12028,#7614,.T.);
#15095=EDGE_CURVE('',#12026,#12029,#6139,.T.);
#15096=EDGE_CURVE('',#12028,#12029,#7615,.T.);
#15097=EDGE_CURVE('',#12029,#12030,#7616,.T.);
#15098=EDGE_CURVE('',#12027,#12030,#7617,.T.);
#15099=EDGE_CURVE('',#12030,#12025,#6140,.T.);
#15100=EDGE_CURVE('',#12031,#12032,#7618,.T.);
#15101=EDGE_CURVE('',#12031,#12033,#7619,.T.);
#15102=EDGE_CURVE('',#12034,#12033,#7620,.T.);
#15103=EDGE_CURVE('',#12032,#12034,#7621,.T.);
#15104=EDGE_CURVE('',#12032,#12035,#6141,.T.);
#15105=EDGE_CURVE('',#12034,#12035,#7622,.T.);
#15106=EDGE_CURVE('',#12035,#12036,#7623,.T.);
#15107=EDGE_CURVE('',#12033,#12036,#7624,.T.);
#15108=EDGE_CURVE('',#12036,#12031,#6142,.T.);
#15109=EDGE_CURVE('',#12037,#12038,#7625,.T.);
#15110=EDGE_CURVE('',#12037,#12039,#7626,.T.);
#15111=EDGE_CURVE('',#12040,#12039,#7627,.T.);
#15112=EDGE_CURVE('',#12038,#12040,#7628,.T.);
#15113=EDGE_CURVE('',#12038,#12041,#6143,.T.);
#15114=EDGE_CURVE('',#12040,#12041,#7629,.T.);
#15115=EDGE_CURVE('',#12041,#12042,#7630,.T.);
#15116=EDGE_CURVE('',#12039,#12042,#7631,.T.);
#15117=EDGE_CURVE('',#12042,#12037,#6144,.T.);
#15118=EDGE_CURVE('',#12043,#12044,#7632,.T.);
#15119=EDGE_CURVE('',#12043,#12045,#7633,.T.);
#15120=EDGE_CURVE('',#12046,#12045,#7634,.T.);
#15121=EDGE_CURVE('',#12044,#12046,#7635,.T.);
#15122=EDGE_CURVE('',#12044,#12047,#6145,.T.);
#15123=EDGE_CURVE('',#12046,#12047,#7636,.T.);
#15124=EDGE_CURVE('',#12047,#12048,#7637,.T.);
#15125=EDGE_CURVE('',#12045,#12048,#7638,.T.);
#15126=EDGE_CURVE('',#12048,#12043,#6146,.T.);
#15127=EDGE_CURVE('',#12049,#12050,#7639,.T.);
#15128=EDGE_CURVE('',#12049,#12051,#7640,.T.);
#15129=EDGE_CURVE('',#12052,#12051,#7641,.T.);
#15130=EDGE_CURVE('',#12050,#12052,#7642,.T.);
#15131=EDGE_CURVE('',#12050,#12053,#6147,.T.);
#15132=EDGE_CURVE('',#12052,#12053,#7643,.T.);
#15133=EDGE_CURVE('',#12053,#12054,#7644,.T.);
#15134=EDGE_CURVE('',#12051,#12054,#7645,.T.);
#15135=EDGE_CURVE('',#12054,#12049,#6148,.T.);
#15136=EDGE_CURVE('',#12055,#12056,#7646,.T.);
#15137=EDGE_CURVE('',#12055,#12057,#7647,.T.);
#15138=EDGE_CURVE('',#12058,#12057,#7648,.T.);
#15139=EDGE_CURVE('',#12056,#12058,#7649,.T.);
#15140=EDGE_CURVE('',#12056,#12059,#6149,.T.);
#15141=EDGE_CURVE('',#12058,#12059,#7650,.T.);
#15142=EDGE_CURVE('',#12059,#12060,#7651,.T.);
#15143=EDGE_CURVE('',#12057,#12060,#7652,.T.);
#15144=EDGE_CURVE('',#12060,#12055,#6150,.T.);
#15145=EDGE_CURVE('',#12061,#12062,#7653,.T.);
#15146=EDGE_CURVE('',#12061,#12063,#7654,.T.);
#15147=EDGE_CURVE('',#12064,#12063,#7655,.T.);
#15148=EDGE_CURVE('',#12062,#12064,#7656,.T.);
#15149=EDGE_CURVE('',#12062,#12065,#6151,.T.);
#15150=EDGE_CURVE('',#12064,#12065,#7657,.T.);
#15151=EDGE_CURVE('',#12065,#12066,#7658,.T.);
#15152=EDGE_CURVE('',#12063,#12066,#7659,.T.);
#15153=EDGE_CURVE('',#12066,#12061,#6152,.T.);
#15154=EDGE_CURVE('',#12067,#12068,#7660,.T.);
#15155=EDGE_CURVE('',#12067,#12069,#7661,.T.);
#15156=EDGE_CURVE('',#12070,#12069,#7662,.T.);
#15157=EDGE_CURVE('',#12068,#12070,#7663,.T.);
#15158=EDGE_CURVE('',#12068,#12071,#6153,.T.);
#15159=EDGE_CURVE('',#12070,#12071,#7664,.T.);
#15160=EDGE_CURVE('',#12071,#12072,#7665,.T.);
#15161=EDGE_CURVE('',#12069,#12072,#7666,.T.);
#15162=EDGE_CURVE('',#12072,#12067,#6154,.T.);
#15163=EDGE_CURVE('',#12073,#12074,#7667,.T.);
#15164=EDGE_CURVE('',#12073,#12075,#7668,.T.);
#15165=EDGE_CURVE('',#12076,#12075,#7669,.T.);
#15166=EDGE_CURVE('',#12074,#12076,#7670,.T.);
#15167=EDGE_CURVE('',#12074,#12077,#6155,.T.);
#15168=EDGE_CURVE('',#12076,#12077,#7671,.T.);
#15169=EDGE_CURVE('',#12077,#12078,#7672,.T.);
#15170=EDGE_CURVE('',#12075,#12078,#7673,.T.);
#15171=EDGE_CURVE('',#12078,#12073,#6156,.T.);
#15172=EDGE_CURVE('',#12079,#12080,#7674,.T.);
#15173=EDGE_CURVE('',#12079,#12081,#7675,.T.);
#15174=EDGE_CURVE('',#12082,#12081,#7676,.T.);
#15175=EDGE_CURVE('',#12080,#12082,#7677,.T.);
#15176=EDGE_CURVE('',#12080,#12083,#6157,.T.);
#15177=EDGE_CURVE('',#12082,#12083,#7678,.T.);
#15178=EDGE_CURVE('',#12083,#12084,#7679,.T.);
#15179=EDGE_CURVE('',#12081,#12084,#7680,.T.);
#15180=EDGE_CURVE('',#12084,#12079,#6158,.T.);
#15181=EDGE_CURVE('',#12085,#12086,#7681,.T.);
#15182=EDGE_CURVE('',#12085,#12087,#7682,.T.);
#15183=EDGE_CURVE('',#12088,#12087,#7683,.T.);
#15184=EDGE_CURVE('',#12086,#12088,#7684,.T.);
#15185=EDGE_CURVE('',#12086,#12089,#6159,.T.);
#15186=EDGE_CURVE('',#12088,#12089,#7685,.T.);
#15187=EDGE_CURVE('',#12089,#12090,#7686,.T.);
#15188=EDGE_CURVE('',#12087,#12090,#7687,.T.);
#15189=EDGE_CURVE('',#12090,#12085,#6160,.T.);
#15190=EDGE_CURVE('',#12091,#12092,#6161,.T.);
#15191=EDGE_CURVE('',#12091,#12093,#7688,.T.);
#15192=EDGE_CURVE('',#12093,#12092,#7689,.T.);
#15193=EDGE_CURVE('',#12094,#12091,#7690,.T.);
#15194=EDGE_CURVE('',#12094,#12095,#7691,.T.);
#15195=EDGE_CURVE('',#12093,#12095,#7692,.T.);
#15196=EDGE_CURVE('',#12092,#12096,#7693,.T.);
#15197=EDGE_CURVE('',#12095,#12096,#7694,.T.);
#15198=EDGE_CURVE('',#12096,#12094,#6162,.T.);
#15199=EDGE_CURVE('',#12097,#12098,#7695,.T.);
#15200=EDGE_CURVE('',#12097,#12099,#7696,.T.);
#15201=EDGE_CURVE('',#12100,#12099,#7697,.T.);
#15202=EDGE_CURVE('',#12098,#12100,#7698,.T.);
#15203=EDGE_CURVE('',#12098,#12101,#6163,.T.);
#15204=EDGE_CURVE('',#12100,#12101,#7699,.T.);
#15205=EDGE_CURVE('',#12101,#12102,#7700,.T.);
#15206=EDGE_CURVE('',#12099,#12102,#7701,.T.);
#15207=EDGE_CURVE('',#12102,#12097,#6164,.T.);
#15208=EDGE_CURVE('',#12103,#12104,#7702,.T.);
#15209=EDGE_CURVE('',#12103,#12105,#7703,.T.);
#15210=EDGE_CURVE('',#12106,#12105,#7704,.T.);
#15211=EDGE_CURVE('',#12104,#12106,#7705,.T.);
#15212=EDGE_CURVE('',#12104,#12107,#6165,.T.);
#15213=EDGE_CURVE('',#12106,#12107,#7706,.T.);
#15214=EDGE_CURVE('',#12107,#12108,#7707,.T.);
#15215=EDGE_CURVE('',#12105,#12108,#7708,.T.);
#15216=EDGE_CURVE('',#12108,#12103,#6166,.T.);
#15217=EDGE_CURVE('',#12109,#12110,#7709,.T.);
#15218=EDGE_CURVE('',#12109,#12111,#7710,.T.);
#15219=EDGE_CURVE('',#12112,#12111,#7711,.T.);
#15220=EDGE_CURVE('',#12110,#12112,#7712,.T.);
#15221=EDGE_CURVE('',#12110,#12113,#6167,.T.);
#15222=EDGE_CURVE('',#12112,#12113,#7713,.T.);
#15223=EDGE_CURVE('',#12113,#12114,#7714,.T.);
#15224=EDGE_CURVE('',#12111,#12114,#7715,.T.);
#15225=EDGE_CURVE('',#12114,#12109,#6168,.T.);
#15226=EDGE_CURVE('',#12115,#12116,#7716,.T.);
#15227=EDGE_CURVE('',#12115,#12117,#7717,.T.);
#15228=EDGE_CURVE('',#12118,#12117,#7718,.T.);
#15229=EDGE_CURVE('',#12116,#12118,#7719,.T.);
#15230=EDGE_CURVE('',#12116,#12119,#6169,.T.);
#15231=EDGE_CURVE('',#12118,#12119,#7720,.T.);
#15232=EDGE_CURVE('',#12119,#12120,#7721,.T.);
#15233=EDGE_CURVE('',#12117,#12120,#7722,.T.);
#15234=EDGE_CURVE('',#12120,#12115,#6170,.T.);
#15235=EDGE_CURVE('',#12121,#12122,#7723,.T.);
#15236=EDGE_CURVE('',#12121,#12123,#7724,.T.);
#15237=EDGE_CURVE('',#12124,#12123,#7725,.T.);
#15238=EDGE_CURVE('',#12122,#12124,#7726,.T.);
#15239=EDGE_CURVE('',#12122,#12125,#6171,.T.);
#15240=EDGE_CURVE('',#12124,#12125,#7727,.T.);
#15241=EDGE_CURVE('',#12125,#12126,#7728,.T.);
#15242=EDGE_CURVE('',#12123,#12126,#7729,.T.);
#15243=EDGE_CURVE('',#12126,#12121,#6172,.T.);
#15244=EDGE_CURVE('',#12127,#12128,#7730,.T.);
#15245=EDGE_CURVE('',#12127,#12129,#7731,.T.);
#15246=EDGE_CURVE('',#12130,#12129,#7732,.T.);
#15247=EDGE_CURVE('',#12128,#12130,#7733,.T.);
#15248=EDGE_CURVE('',#12128,#12131,#6173,.T.);
#15249=EDGE_CURVE('',#12130,#12131,#7734,.T.);
#15250=EDGE_CURVE('',#12131,#12132,#7735,.T.);
#15251=EDGE_CURVE('',#12129,#12132,#7736,.T.);
#15252=EDGE_CURVE('',#12132,#12127,#6174,.T.);
#15253=EDGE_CURVE('',#12133,#12134,#7737,.T.);
#15254=EDGE_CURVE('',#12133,#12135,#7738,.T.);
#15255=EDGE_CURVE('',#12136,#12135,#7739,.T.);
#15256=EDGE_CURVE('',#12134,#12136,#7740,.T.);
#15257=EDGE_CURVE('',#12134,#12137,#6175,.T.);
#15258=EDGE_CURVE('',#12136,#12137,#7741,.T.);
#15259=EDGE_CURVE('',#12137,#12138,#7742,.T.);
#15260=EDGE_CURVE('',#12135,#12138,#7743,.T.);
#15261=EDGE_CURVE('',#12138,#12133,#6176,.T.);
#15262=EDGE_CURVE('',#12139,#12140,#7744,.T.);
#15263=EDGE_CURVE('',#12139,#12141,#7745,.T.);
#15264=EDGE_CURVE('',#12142,#12141,#7746,.T.);
#15265=EDGE_CURVE('',#12140,#12142,#7747,.T.);
#15266=EDGE_CURVE('',#12140,#12143,#6177,.T.);
#15267=EDGE_CURVE('',#12142,#12143,#7748,.T.);
#15268=EDGE_CURVE('',#12143,#12144,#7749,.T.);
#15269=EDGE_CURVE('',#12141,#12144,#7750,.T.);
#15270=EDGE_CURVE('',#12144,#12139,#6178,.T.);
#15271=EDGE_CURVE('',#12145,#12146,#7751,.T.);
#15272=EDGE_CURVE('',#12145,#12147,#7752,.T.);
#15273=EDGE_CURVE('',#12148,#12147,#7753,.T.);
#15274=EDGE_CURVE('',#12146,#12148,#7754,.T.);
#15275=EDGE_CURVE('',#12146,#12149,#6179,.T.);
#15276=EDGE_CURVE('',#12148,#12149,#7755,.T.);
#15277=EDGE_CURVE('',#12149,#12150,#7756,.T.);
#15278=EDGE_CURVE('',#12147,#12150,#7757,.T.);
#15279=EDGE_CURVE('',#12150,#12145,#6180,.T.);
#15280=EDGE_CURVE('',#12151,#12151,#6181,.T.);
#15281=EDGE_CURVE('',#11916,#12151,#7758,.T.);
#15282=EDGE_CURVE('',#12152,#12152,#6182,.T.);
#15283=EDGE_CURVE('',#12152,#11919,#7759,.T.);
#15284=EDGE_CURVE('',#12143,#11934,#6183,.T.);
#15285=EDGE_CURVE('',#11943,#12140,#6184,.T.);
#15286=EDGE_CURVE('',#12137,#11940,#6185,.T.);
#15287=EDGE_CURVE('',#11949,#12134,#6186,.T.);
#15288=EDGE_CURVE('',#12131,#11946,#6187,.T.);
#15289=EDGE_CURVE('',#11955,#12128,#6188,.T.);
#15290=EDGE_CURVE('',#12125,#11952,#6189,.T.);
#15291=EDGE_CURVE('',#11961,#12122,#6190,.T.);
#15292=EDGE_CURVE('',#12119,#11958,#6191,.T.);
#15293=EDGE_CURVE('',#11967,#12116,#6192,.T.);
#15294=EDGE_CURVE('',#12113,#11964,#6193,.T.);
#15295=EDGE_CURVE('',#11973,#12110,#6194,.T.);
#15296=EDGE_CURVE('',#12107,#11970,#6195,.T.);
#15297=EDGE_CURVE('',#11979,#12104,#6196,.T.);
#15298=EDGE_CURVE('',#12101,#11976,#6197,.T.);
#15299=EDGE_CURVE('',#11986,#12098,#6198,.T.);
#15300=EDGE_CURVE('',#11988,#12152,#7760,.T.);
#15301=EDGE_CURVE('',#11993,#11982,#6199,.T.);
#15302=EDGE_CURVE('',#12089,#11990,#6200,.T.);
#15303=EDGE_CURVE('',#11999,#12086,#6201,.T.);
#15304=EDGE_CURVE('',#12083,#11996,#6202,.T.);
#15305=EDGE_CURVE('',#12005,#12080,#6203,.T.);
#15306=EDGE_CURVE('',#12077,#12002,#6204,.T.);
#15307=EDGE_CURVE('',#12011,#12074,#6205,.T.);
#15308=EDGE_CURVE('',#12071,#12008,#6206,.T.);
#15309=EDGE_CURVE('',#12017,#12068,#6207,.T.);
#15310=EDGE_CURVE('',#12065,#12014,#6208,.T.);
#15311=EDGE_CURVE('',#12023,#12062,#6209,.T.);
#15312=EDGE_CURVE('',#12059,#12020,#6210,.T.);
#15313=EDGE_CURVE('',#12029,#12056,#6211,.T.);
#15314=EDGE_CURVE('',#12053,#12026,#6212,.T.);
#15315=EDGE_CURVE('',#12035,#12050,#6213,.T.);
#15316=EDGE_CURVE('',#12047,#12032,#6214,.T.);
#15317=EDGE_CURVE('',#12041,#12044,#6215,.T.);
#15318=EDGE_CURVE('',#12092,#12038,#6216,.T.);
#15319=EDGE_CURVE('',#12149,#12091,#6217,.T.);
#15320=EDGE_CURVE('',#11937,#12146,#6218,.T.);
#15321=EDGE_CURVE('',#12153,#12153,#6219,.T.);
#15322=EDGE_CURVE('',#12153,#11985,#7761,.T.);
#20189=ORIENTED_EDGE('',*,*,#14817,.F.);
#20190=ORIENTED_EDGE('',*,*,#14818,.T.);
#20191=ORIENTED_EDGE('',*,*,#14819,.T.);
#20192=ORIENTED_EDGE('',*,*,#14820,.T.);
#20193=ORIENTED_EDGE('',*,*,#14821,.F.);
#20194=ORIENTED_EDGE('',*,*,#14822,.T.);
#20195=ORIENTED_EDGE('',*,*,#14817,.T.);
#20196=ORIENTED_EDGE('',*,*,#14823,.T.);
#20197=ORIENTED_EDGE('',*,*,#14824,.F.);
#20198=ORIENTED_EDGE('',*,*,#14825,.T.);
#20199=ORIENTED_EDGE('',*,*,#14821,.T.);
#20200=ORIENTED_EDGE('',*,*,#14826,.T.);
#20201=ORIENTED_EDGE('',*,*,#14827,.F.);
#20202=ORIENTED_EDGE('',*,*,#14828,.T.);
#20203=ORIENTED_EDGE('',*,*,#14824,.T.);
#20204=ORIENTED_EDGE('',*,*,#14829,.T.);
#20205=ORIENTED_EDGE('',*,*,#14830,.F.);
#20206=ORIENTED_EDGE('',*,*,#14831,.T.);
#20207=ORIENTED_EDGE('',*,*,#14827,.T.);
#20208=ORIENTED_EDGE('',*,*,#14832,.T.);
#20209=ORIENTED_EDGE('',*,*,#14833,.F.);
#20210=ORIENTED_EDGE('',*,*,#14834,.T.);
#20211=ORIENTED_EDGE('',*,*,#14830,.T.);
#20212=ORIENTED_EDGE('',*,*,#14835,.T.);
#20213=ORIENTED_EDGE('',*,*,#14836,.F.);
#20214=ORIENTED_EDGE('',*,*,#14837,.T.);
#20215=ORIENTED_EDGE('',*,*,#14833,.T.);
#20216=ORIENTED_EDGE('',*,*,#14838,.T.);
#20217=ORIENTED_EDGE('',*,*,#14839,.F.);
#20218=ORIENTED_EDGE('',*,*,#14840,.T.);
#20219=ORIENTED_EDGE('',*,*,#14836,.T.);
#20220=ORIENTED_EDGE('',*,*,#14841,.T.);
#20221=ORIENTED_EDGE('',*,*,#14842,.F.);
#20222=ORIENTED_EDGE('',*,*,#14843,.T.);
#20223=ORIENTED_EDGE('',*,*,#14839,.T.);
#20224=ORIENTED_EDGE('',*,*,#14844,.T.);
#20225=ORIENTED_EDGE('',*,*,#14845,.F.);
#20226=ORIENTED_EDGE('',*,*,#14846,.T.);
#20227=ORIENTED_EDGE('',*,*,#14842,.T.);
#20228=ORIENTED_EDGE('',*,*,#14847,.T.);
#20229=ORIENTED_EDGE('',*,*,#14848,.F.);
#20230=ORIENTED_EDGE('',*,*,#14849,.T.);
#20231=ORIENTED_EDGE('',*,*,#14845,.T.);
#20232=ORIENTED_EDGE('',*,*,#14850,.T.);
#20233=ORIENTED_EDGE('',*,*,#14851,.F.);
#20234=ORIENTED_EDGE('',*,*,#14852,.T.);
#20235=ORIENTED_EDGE('',*,*,#14848,.T.);
#20236=ORIENTED_EDGE('',*,*,#14853,.T.);
#20237=ORIENTED_EDGE('',*,*,#14854,.F.);
#20238=ORIENTED_EDGE('',*,*,#14855,.T.);
#20239=ORIENTED_EDGE('',*,*,#14851,.T.);
#20240=ORIENTED_EDGE('',*,*,#14856,.T.);
#20241=ORIENTED_EDGE('',*,*,#14857,.F.);
#20242=ORIENTED_EDGE('',*,*,#14858,.T.);
#20243=ORIENTED_EDGE('',*,*,#14854,.T.);
#20244=ORIENTED_EDGE('',*,*,#14859,.T.);
#20245=ORIENTED_EDGE('',*,*,#14860,.F.);
#20246=ORIENTED_EDGE('',*,*,#14861,.T.);
#20247=ORIENTED_EDGE('',*,*,#14857,.T.);
#20248=ORIENTED_EDGE('',*,*,#14862,.T.);
#20249=ORIENTED_EDGE('',*,*,#14863,.F.);
#20250=ORIENTED_EDGE('',*,*,#14864,.T.);
#20251=ORIENTED_EDGE('',*,*,#14860,.T.);
#20252=ORIENTED_EDGE('',*,*,#14865,.T.);
#20253=ORIENTED_EDGE('',*,*,#14866,.F.);
#20254=ORIENTED_EDGE('',*,*,#14867,.T.);
#20255=ORIENTED_EDGE('',*,*,#14868,.F.);
#20256=ORIENTED_EDGE('',*,*,#14869,.F.);
#20257=ORIENTED_EDGE('',*,*,#14870,.F.);
#20258=ORIENTED_EDGE('',*,*,#14871,.T.);
#20259=ORIENTED_EDGE('',*,*,#14866,.T.);
#20260=ORIENTED_EDGE('',*,*,#14872,.F.);
#20261=ORIENTED_EDGE('',*,*,#14873,.F.);
#20262=ORIENTED_EDGE('',*,*,#14874,.T.);
#20263=ORIENTED_EDGE('',*,*,#14870,.T.);
#20264=ORIENTED_EDGE('',*,*,#14875,.F.);
#20265=ORIENTED_EDGE('',*,*,#14876,.F.);
#20266=ORIENTED_EDGE('',*,*,#14877,.T.);
#20267=ORIENTED_EDGE('',*,*,#14873,.T.);
#20268=ORIENTED_EDGE('',*,*,#14878,.F.);
#20269=ORIENTED_EDGE('',*,*,#14879,.F.);
#20270=ORIENTED_EDGE('',*,*,#14880,.T.);
#20271=ORIENTED_EDGE('',*,*,#14876,.T.);
#20272=ORIENTED_EDGE('',*,*,#14881,.F.);
#20273=ORIENTED_EDGE('',*,*,#14882,.F.);
#20274=ORIENTED_EDGE('',*,*,#14883,.T.);
#20275=ORIENTED_EDGE('',*,*,#14879,.T.);
#20276=ORIENTED_EDGE('',*,*,#14884,.F.);
#20277=ORIENTED_EDGE('',*,*,#14885,.F.);
#20278=ORIENTED_EDGE('',*,*,#14886,.T.);
#20279=ORIENTED_EDGE('',*,*,#14882,.T.);
#20280=ORIENTED_EDGE('',*,*,#14887,.F.);
#20281=ORIENTED_EDGE('',*,*,#14888,.F.);
#20282=ORIENTED_EDGE('',*,*,#14889,.T.);
#20283=ORIENTED_EDGE('',*,*,#14885,.T.);
#20284=ORIENTED_EDGE('',*,*,#14890,.F.);
#20285=ORIENTED_EDGE('',*,*,#14891,.F.);
#20286=ORIENTED_EDGE('',*,*,#14892,.T.);
#20287=ORIENTED_EDGE('',*,*,#14888,.T.);
#20288=ORIENTED_EDGE('',*,*,#14893,.F.);
#20289=ORIENTED_EDGE('',*,*,#14894,.F.);
#20290=ORIENTED_EDGE('',*,*,#14895,.T.);
#20291=ORIENTED_EDGE('',*,*,#14891,.T.);
#20292=ORIENTED_EDGE('',*,*,#14896,.F.);
#20293=ORIENTED_EDGE('',*,*,#14897,.F.);
#20294=ORIENTED_EDGE('',*,*,#14898,.T.);
#20295=ORIENTED_EDGE('',*,*,#14894,.T.);
#20296=ORIENTED_EDGE('',*,*,#14899,.F.);
#20297=ORIENTED_EDGE('',*,*,#14900,.F.);
#20298=ORIENTED_EDGE('',*,*,#14901,.T.);
#20299=ORIENTED_EDGE('',*,*,#14897,.T.);
#20300=ORIENTED_EDGE('',*,*,#14902,.F.);
#20301=ORIENTED_EDGE('',*,*,#14903,.F.);
#20302=ORIENTED_EDGE('',*,*,#14904,.T.);
#20303=ORIENTED_EDGE('',*,*,#14900,.T.);
#20304=ORIENTED_EDGE('',*,*,#14905,.F.);
#20305=ORIENTED_EDGE('',*,*,#14906,.F.);
#20306=ORIENTED_EDGE('',*,*,#14907,.T.);
#20307=ORIENTED_EDGE('',*,*,#14903,.T.);
#20308=ORIENTED_EDGE('',*,*,#14908,.F.);
#20309=ORIENTED_EDGE('',*,*,#14909,.F.);
#20310=ORIENTED_EDGE('',*,*,#14910,.T.);
#20311=ORIENTED_EDGE('',*,*,#14906,.T.);
#20312=ORIENTED_EDGE('',*,*,#14911,.F.);
#20313=ORIENTED_EDGE('',*,*,#14868,.T.);
#20314=ORIENTED_EDGE('',*,*,#14912,.T.);
#20315=ORIENTED_EDGE('',*,*,#14913,.F.);
#20316=ORIENTED_EDGE('',*,*,#14914,.F.);
#20317=ORIENTED_EDGE('',*,*,#14915,.T.);
#20318=ORIENTED_EDGE('',*,*,#14915,.F.);
#20319=ORIENTED_EDGE('',*,*,#14916,.F.);
#20320=ORIENTED_EDGE('',*,*,#14865,.F.);
#20321=ORIENTED_EDGE('',*,*,#14862,.F.);
#20322=ORIENTED_EDGE('',*,*,#14859,.F.);
#20323=ORIENTED_EDGE('',*,*,#14856,.F.);
#20324=ORIENTED_EDGE('',*,*,#14853,.F.);
#20325=ORIENTED_EDGE('',*,*,#14850,.F.);
#20326=ORIENTED_EDGE('',*,*,#14847,.F.);
#20327=ORIENTED_EDGE('',*,*,#14844,.F.);
#20328=ORIENTED_EDGE('',*,*,#14841,.F.);
#20329=ORIENTED_EDGE('',*,*,#14838,.F.);
#20330=ORIENTED_EDGE('',*,*,#14835,.F.);
#20331=ORIENTED_EDGE('',*,*,#14832,.F.);
#20332=ORIENTED_EDGE('',*,*,#14829,.F.);
#20333=ORIENTED_EDGE('',*,*,#14826,.F.);
#20334=ORIENTED_EDGE('',*,*,#14823,.F.);
#20335=ORIENTED_EDGE('',*,*,#14820,.F.);
#20336=ORIENTED_EDGE('',*,*,#14917,.F.);
#20337=ORIENTED_EDGE('',*,*,#14918,.T.);
#20338=ORIENTED_EDGE('',*,*,#14911,.T.);
#20339=ORIENTED_EDGE('',*,*,#14908,.T.);
#20340=ORIENTED_EDGE('',*,*,#14905,.T.);
#20341=ORIENTED_EDGE('',*,*,#14902,.T.);
#20342=ORIENTED_EDGE('',*,*,#14899,.T.);
#20343=ORIENTED_EDGE('',*,*,#14896,.T.);
#20344=ORIENTED_EDGE('',*,*,#14893,.T.);
#20345=ORIENTED_EDGE('',*,*,#14890,.T.);
#20346=ORIENTED_EDGE('',*,*,#14887,.T.);
#20347=ORIENTED_EDGE('',*,*,#14884,.T.);
#20348=ORIENTED_EDGE('',*,*,#14881,.T.);
#20349=ORIENTED_EDGE('',*,*,#14878,.T.);
#20350=ORIENTED_EDGE('',*,*,#14875,.T.);
#20351=ORIENTED_EDGE('',*,*,#14872,.T.);
#20352=ORIENTED_EDGE('',*,*,#14869,.T.);
#20353=ORIENTED_EDGE('',*,*,#14919,.T.);
#20354=ORIENTED_EDGE('',*,*,#14920,.T.);
#20355=ORIENTED_EDGE('',*,*,#14921,.T.);
#20356=ORIENTED_EDGE('',*,*,#14922,.T.);
#20357=ORIENTED_EDGE('',*,*,#14917,.T.);
#20358=ORIENTED_EDGE('',*,*,#14909,.T.);
#20359=ORIENTED_EDGE('',*,*,#14918,.F.);
#20360=ORIENTED_EDGE('',*,*,#14922,.F.);
#20361=ORIENTED_EDGE('',*,*,#14923,.T.);
#20362=ORIENTED_EDGE('',*,*,#14912,.F.);
#20363=ORIENTED_EDGE('',*,*,#14867,.F.);
#20364=ORIENTED_EDGE('',*,*,#14871,.F.);
#20365=ORIENTED_EDGE('',*,*,#14874,.F.);
#20366=ORIENTED_EDGE('',*,*,#14877,.F.);
#20367=ORIENTED_EDGE('',*,*,#14880,.F.);
#20368=ORIENTED_EDGE('',*,*,#14883,.F.);
#20369=ORIENTED_EDGE('',*,*,#14886,.F.);
#20370=ORIENTED_EDGE('',*,*,#14889,.F.);
#20371=ORIENTED_EDGE('',*,*,#14892,.F.);
#20372=ORIENTED_EDGE('',*,*,#14895,.F.);
#20373=ORIENTED_EDGE('',*,*,#14898,.F.);
#20374=ORIENTED_EDGE('',*,*,#14901,.F.);
#20375=ORIENTED_EDGE('',*,*,#14904,.F.);
#20376=ORIENTED_EDGE('',*,*,#14907,.F.);
#20377=ORIENTED_EDGE('',*,*,#14910,.F.);
#20378=ORIENTED_EDGE('',*,*,#14923,.F.);
#20379=ORIENTED_EDGE('',*,*,#14921,.F.);
#20380=ORIENTED_EDGE('',*,*,#14818,.F.);
#20381=ORIENTED_EDGE('',*,*,#14822,.F.);
#20382=ORIENTED_EDGE('',*,*,#14825,.F.);
#20383=ORIENTED_EDGE('',*,*,#14828,.F.);
#20384=ORIENTED_EDGE('',*,*,#14831,.F.);
#20385=ORIENTED_EDGE('',*,*,#14834,.F.);
#20386=ORIENTED_EDGE('',*,*,#14837,.F.);
#20387=ORIENTED_EDGE('',*,*,#14840,.F.);
#20388=ORIENTED_EDGE('',*,*,#14843,.F.);
#20389=ORIENTED_EDGE('',*,*,#14846,.F.);
#20390=ORIENTED_EDGE('',*,*,#14849,.F.);
#20391=ORIENTED_EDGE('',*,*,#14852,.F.);
#20392=ORIENTED_EDGE('',*,*,#14855,.F.);
#20393=ORIENTED_EDGE('',*,*,#14858,.F.);
#20394=ORIENTED_EDGE('',*,*,#14861,.F.);
#20395=ORIENTED_EDGE('',*,*,#14864,.F.);
#20396=ORIENTED_EDGE('',*,*,#14924,.F.);
#20397=ORIENTED_EDGE('',*,*,#14914,.T.);
#20398=ORIENTED_EDGE('',*,*,#14925,.T.);
#20399=ORIENTED_EDGE('',*,*,#14926,.T.);
#20400=ORIENTED_EDGE('',*,*,#14925,.F.);
#20401=ORIENTED_EDGE('',*,*,#14913,.T.);
#20402=ORIENTED_EDGE('',*,*,#14927,.T.);
#20403=ORIENTED_EDGE('',*,*,#14863,.T.);
#20404=ORIENTED_EDGE('',*,*,#14916,.T.);
#20405=ORIENTED_EDGE('',*,*,#14927,.F.);
#20406=ORIENTED_EDGE('',*,*,#14924,.T.);
#20407=ORIENTED_EDGE('',*,*,#14928,.F.);
#20408=ORIENTED_EDGE('',*,*,#14926,.F.);
#20409=ORIENTED_EDGE('',*,*,#14929,.F.);
#20410=ORIENTED_EDGE('',*,*,#14930,.F.);
#20411=ORIENTED_EDGE('',*,*,#14931,.F.);
#20412=ORIENTED_EDGE('',*,*,#14932,.F.);
#20413=ORIENTED_EDGE('',*,*,#14933,.F.);
#20414=ORIENTED_EDGE('',*,*,#14934,.F.);
#20415=ORIENTED_EDGE('',*,*,#14935,.F.);
#20416=ORIENTED_EDGE('',*,*,#14936,.F.);
#20417=ORIENTED_EDGE('',*,*,#14937,.F.);
#20418=ORIENTED_EDGE('',*,*,#14938,.F.);
#20419=ORIENTED_EDGE('',*,*,#14939,.F.);
#20420=ORIENTED_EDGE('',*,*,#14940,.F.);
#20421=ORIENTED_EDGE('',*,*,#14941,.T.);
#20422=ORIENTED_EDGE('',*,*,#14936,.T.);
#20423=ORIENTED_EDGE('',*,*,#14934,.T.);
#20424=ORIENTED_EDGE('',*,*,#14932,.T.);
#20425=ORIENTED_EDGE('',*,*,#14930,.T.);
#20426=ORIENTED_EDGE('',*,*,#14940,.T.);
#20427=ORIENTED_EDGE('',*,*,#14938,.T.);
#20428=ORIENTED_EDGE('',*,*,#14941,.F.);
#20429=ORIENTED_EDGE('',*,*,#14942,.F.);
#20430=ORIENTED_EDGE('',*,*,#14943,.T.);
#20431=ORIENTED_EDGE('',*,*,#14929,.T.);
#20432=ORIENTED_EDGE('',*,*,#14944,.F.);
#20433=ORIENTED_EDGE('',*,*,#14945,.F.);
#20434=ORIENTED_EDGE('',*,*,#14946,.T.);
#20435=ORIENTED_EDGE('',*,*,#14939,.T.);
#20436=ORIENTED_EDGE('',*,*,#14943,.F.);
#20437=ORIENTED_EDGE('',*,*,#14947,.F.);
#20438=ORIENTED_EDGE('',*,*,#14948,.T.);
#20439=ORIENTED_EDGE('',*,*,#14937,.T.);
#20440=ORIENTED_EDGE('',*,*,#14946,.F.);
#20441=ORIENTED_EDGE('',*,*,#14949,.F.);
#20442=ORIENTED_EDGE('',*,*,#14950,.T.);
#20443=ORIENTED_EDGE('',*,*,#14935,.T.);
#20444=ORIENTED_EDGE('',*,*,#14948,.F.);
#20445=ORIENTED_EDGE('',*,*,#14951,.F.);
#20446=ORIENTED_EDGE('',*,*,#14952,.T.);
#20447=ORIENTED_EDGE('',*,*,#14933,.T.);
#20448=ORIENTED_EDGE('',*,*,#14950,.F.);
#20449=ORIENTED_EDGE('',*,*,#14953,.F.);
#20450=ORIENTED_EDGE('',*,*,#14944,.T.);
#20451=ORIENTED_EDGE('',*,*,#14931,.T.);
#20452=ORIENTED_EDGE('',*,*,#14952,.F.);
#20453=ORIENTED_EDGE('',*,*,#14954,.F.);
#20454=ORIENTED_EDGE('',*,*,#14955,.T.);
#20455=ORIENTED_EDGE('',*,*,#14956,.F.);
#20456=ORIENTED_EDGE('',*,*,#14957,.F.);
#20457=ORIENTED_EDGE('',*,*,#14958,.F.);
#20458=ORIENTED_EDGE('',*,*,#14957,.T.);
#20459=ORIENTED_EDGE('',*,*,#14959,.T.);
#20460=ORIENTED_EDGE('',*,*,#14960,.F.);
#20461=ORIENTED_EDGE('',*,*,#14959,.F.);
#20462=ORIENTED_EDGE('',*,*,#14956,.T.);
#20463=ORIENTED_EDGE('',*,*,#14961,.T.);
#20464=ORIENTED_EDGE('',*,*,#14962,.F.);
#20465=ORIENTED_EDGE('',*,*,#14961,.F.);
#20466=ORIENTED_EDGE('',*,*,#14955,.F.);
#20467=ORIENTED_EDGE('',*,*,#14963,.F.);
#20468=ORIENTED_EDGE('',*,*,#14964,.T.);
#20469=ORIENTED_EDGE('',*,*,#14965,.F.);
#20470=ORIENTED_EDGE('',*,*,#14966,.F.);
#20471=ORIENTED_EDGE('',*,*,#14967,.F.);
#20472=ORIENTED_EDGE('',*,*,#14966,.T.);
#20473=ORIENTED_EDGE('',*,*,#14968,.T.);
#20474=ORIENTED_EDGE('',*,*,#14969,.F.);
#20475=ORIENTED_EDGE('',*,*,#14968,.F.);
#20476=ORIENTED_EDGE('',*,*,#14965,.T.);
#20477=ORIENTED_EDGE('',*,*,#14970,.T.);
#20478=ORIENTED_EDGE('',*,*,#14971,.F.);
#20479=ORIENTED_EDGE('',*,*,#14970,.F.);
#20480=ORIENTED_EDGE('',*,*,#14964,.F.);
#20481=ORIENTED_EDGE('',*,*,#14972,.F.);
#20482=ORIENTED_EDGE('',*,*,#14973,.T.);
#20483=ORIENTED_EDGE('',*,*,#14974,.F.);
#20484=ORIENTED_EDGE('',*,*,#14975,.F.);
#20485=ORIENTED_EDGE('',*,*,#14976,.F.);
#20486=ORIENTED_EDGE('',*,*,#14975,.T.);
#20487=ORIENTED_EDGE('',*,*,#14977,.T.);
#20488=ORIENTED_EDGE('',*,*,#14978,.F.);
#20489=ORIENTED_EDGE('',*,*,#14977,.F.);
#20490=ORIENTED_EDGE('',*,*,#14974,.T.);
#20491=ORIENTED_EDGE('',*,*,#14979,.T.);
#20492=ORIENTED_EDGE('',*,*,#14980,.F.);
#20493=ORIENTED_EDGE('',*,*,#14979,.F.);
#20494=ORIENTED_EDGE('',*,*,#14973,.F.);
#20495=ORIENTED_EDGE('',*,*,#14981,.F.);
#20496=ORIENTED_EDGE('',*,*,#14982,.T.);
#20497=ORIENTED_EDGE('',*,*,#14983,.F.);
#20498=ORIENTED_EDGE('',*,*,#14984,.F.);
#20499=ORIENTED_EDGE('',*,*,#14985,.F.);
#20500=ORIENTED_EDGE('',*,*,#14984,.T.);
#20501=ORIENTED_EDGE('',*,*,#14986,.T.);
#20502=ORIENTED_EDGE('',*,*,#14987,.F.);
#20503=ORIENTED_EDGE('',*,*,#14986,.F.);
#20504=ORIENTED_EDGE('',*,*,#14983,.T.);
#20505=ORIENTED_EDGE('',*,*,#14988,.T.);
#20506=ORIENTED_EDGE('',*,*,#14989,.F.);
#20507=ORIENTED_EDGE('',*,*,#14988,.F.);
#20508=ORIENTED_EDGE('',*,*,#14982,.F.);
#20509=ORIENTED_EDGE('',*,*,#14990,.F.);
#20510=ORIENTED_EDGE('',*,*,#14991,.T.);
#20511=ORIENTED_EDGE('',*,*,#14992,.F.);
#20512=ORIENTED_EDGE('',*,*,#14993,.F.);
#20513=ORIENTED_EDGE('',*,*,#14994,.F.);
#20514=ORIENTED_EDGE('',*,*,#14993,.T.);
#20515=ORIENTED_EDGE('',*,*,#14995,.T.);
#20516=ORIENTED_EDGE('',*,*,#14996,.F.);
#20517=ORIENTED_EDGE('',*,*,#14995,.F.);
#20518=ORIENTED_EDGE('',*,*,#14992,.T.);
#20519=ORIENTED_EDGE('',*,*,#14997,.T.);
#20520=ORIENTED_EDGE('',*,*,#14998,.F.);
#20521=ORIENTED_EDGE('',*,*,#14997,.F.);
#20522=ORIENTED_EDGE('',*,*,#14991,.F.);
#20523=ORIENTED_EDGE('',*,*,#14999,.F.);
#20524=ORIENTED_EDGE('',*,*,#15000,.T.);
#20525=ORIENTED_EDGE('',*,*,#15001,.F.);
#20526=ORIENTED_EDGE('',*,*,#15002,.F.);
#20527=ORIENTED_EDGE('',*,*,#15003,.F.);
#20528=ORIENTED_EDGE('',*,*,#15002,.T.);
#20529=ORIENTED_EDGE('',*,*,#15004,.T.);
#20530=ORIENTED_EDGE('',*,*,#15005,.F.);
#20531=ORIENTED_EDGE('',*,*,#15004,.F.);
#20532=ORIENTED_EDGE('',*,*,#15001,.T.);
#20533=ORIENTED_EDGE('',*,*,#15006,.T.);
#20534=ORIENTED_EDGE('',*,*,#15007,.F.);
#20535=ORIENTED_EDGE('',*,*,#15006,.F.);
#20536=ORIENTED_EDGE('',*,*,#15000,.F.);
#20537=ORIENTED_EDGE('',*,*,#15008,.F.);
#20538=ORIENTED_EDGE('',*,*,#15009,.T.);
#20539=ORIENTED_EDGE('',*,*,#15010,.F.);
#20540=ORIENTED_EDGE('',*,*,#15011,.F.);
#20541=ORIENTED_EDGE('',*,*,#15012,.F.);
#20542=ORIENTED_EDGE('',*,*,#15011,.T.);
#20543=ORIENTED_EDGE('',*,*,#15013,.T.);
#20544=ORIENTED_EDGE('',*,*,#15014,.F.);
#20545=ORIENTED_EDGE('',*,*,#15013,.F.);
#20546=ORIENTED_EDGE('',*,*,#15010,.T.);
#20547=ORIENTED_EDGE('',*,*,#15015,.T.);
#20548=ORIENTED_EDGE('',*,*,#15016,.F.);
#20549=ORIENTED_EDGE('',*,*,#15015,.F.);
#20550=ORIENTED_EDGE('',*,*,#15009,.F.);
#20551=ORIENTED_EDGE('',*,*,#15017,.F.);
#20552=ORIENTED_EDGE('',*,*,#15018,.T.);
#20553=ORIENTED_EDGE('',*,*,#15019,.F.);
#20554=ORIENTED_EDGE('',*,*,#15020,.F.);
#20555=ORIENTED_EDGE('',*,*,#15021,.F.);
#20556=ORIENTED_EDGE('',*,*,#15020,.T.);
#20557=ORIENTED_EDGE('',*,*,#15022,.T.);
#20558=ORIENTED_EDGE('',*,*,#15023,.F.);
#20559=ORIENTED_EDGE('',*,*,#15022,.F.);
#20560=ORIENTED_EDGE('',*,*,#15019,.T.);
#20561=ORIENTED_EDGE('',*,*,#15024,.T.);
#20562=ORIENTED_EDGE('',*,*,#15025,.F.);
#20563=ORIENTED_EDGE('',*,*,#15024,.F.);
#20564=ORIENTED_EDGE('',*,*,#15018,.F.);
#20565=ORIENTED_EDGE('',*,*,#15026,.F.);
#20566=ORIENTED_EDGE('',*,*,#15027,.T.);
#20567=ORIENTED_EDGE('',*,*,#15028,.F.);
#20568=ORIENTED_EDGE('',*,*,#15029,.F.);
#20569=ORIENTED_EDGE('',*,*,#15030,.F.);
#20570=ORIENTED_EDGE('',*,*,#15029,.T.);
#20571=ORIENTED_EDGE('',*,*,#15031,.T.);
#20572=ORIENTED_EDGE('',*,*,#15032,.F.);
#20573=ORIENTED_EDGE('',*,*,#15033,.F.);
#20574=ORIENTED_EDGE('',*,*,#15031,.F.);
#20575=ORIENTED_EDGE('',*,*,#15028,.T.);
#20576=ORIENTED_EDGE('',*,*,#15034,.T.);
#20577=ORIENTED_EDGE('',*,*,#15035,.F.);
#20578=ORIENTED_EDGE('',*,*,#15034,.F.);
#20579=ORIENTED_EDGE('',*,*,#15027,.F.);
#20580=ORIENTED_EDGE('',*,*,#15036,.F.);
#20581=ORIENTED_EDGE('',*,*,#15037,.F.);
#20582=ORIENTED_EDGE('',*,*,#15038,.T.);
#20583=ORIENTED_EDGE('',*,*,#15039,.F.);
#20584=ORIENTED_EDGE('',*,*,#15040,.F.);
#20585=ORIENTED_EDGE('',*,*,#15041,.F.);
#20586=ORIENTED_EDGE('',*,*,#15040,.T.);
#20587=ORIENTED_EDGE('',*,*,#15042,.T.);
#20588=ORIENTED_EDGE('',*,*,#15043,.F.);
#20589=ORIENTED_EDGE('',*,*,#15042,.F.);
#20590=ORIENTED_EDGE('',*,*,#15039,.T.);
#20591=ORIENTED_EDGE('',*,*,#15044,.T.);
#20592=ORIENTED_EDGE('',*,*,#15045,.F.);
#20593=ORIENTED_EDGE('',*,*,#15044,.F.);
#20594=ORIENTED_EDGE('',*,*,#15038,.F.);
#20595=ORIENTED_EDGE('',*,*,#15046,.F.);
#20596=ORIENTED_EDGE('',*,*,#15047,.T.);
#20597=ORIENTED_EDGE('',*,*,#15048,.F.);
#20598=ORIENTED_EDGE('',*,*,#15049,.F.);
#20599=ORIENTED_EDGE('',*,*,#15050,.F.);
#20600=ORIENTED_EDGE('',*,*,#15049,.T.);
#20601=ORIENTED_EDGE('',*,*,#15051,.T.);
#20602=ORIENTED_EDGE('',*,*,#15052,.F.);
#20603=ORIENTED_EDGE('',*,*,#15051,.F.);
#20604=ORIENTED_EDGE('',*,*,#15048,.T.);
#20605=ORIENTED_EDGE('',*,*,#15053,.T.);
#20606=ORIENTED_EDGE('',*,*,#15054,.F.);
#20607=ORIENTED_EDGE('',*,*,#15053,.F.);
#20608=ORIENTED_EDGE('',*,*,#15047,.F.);
#20609=ORIENTED_EDGE('',*,*,#15055,.F.);
#20610=ORIENTED_EDGE('',*,*,#15056,.T.);
#20611=ORIENTED_EDGE('',*,*,#15057,.F.);
#20612=ORIENTED_EDGE('',*,*,#15058,.F.);
#20613=ORIENTED_EDGE('',*,*,#15059,.F.);
#20614=ORIENTED_EDGE('',*,*,#15058,.T.);
#20615=ORIENTED_EDGE('',*,*,#15060,.T.);
#20616=ORIENTED_EDGE('',*,*,#15061,.F.);
#20617=ORIENTED_EDGE('',*,*,#15060,.F.);
#20618=ORIENTED_EDGE('',*,*,#15057,.T.);
#20619=ORIENTED_EDGE('',*,*,#15062,.T.);
#20620=ORIENTED_EDGE('',*,*,#15063,.F.);
#20621=ORIENTED_EDGE('',*,*,#15062,.F.);
#20622=ORIENTED_EDGE('',*,*,#15056,.F.);
#20623=ORIENTED_EDGE('',*,*,#15064,.F.);
#20624=ORIENTED_EDGE('',*,*,#15065,.T.);
#20625=ORIENTED_EDGE('',*,*,#15066,.F.);
#20626=ORIENTED_EDGE('',*,*,#15067,.F.);
#20627=ORIENTED_EDGE('',*,*,#15068,.F.);
#20628=ORIENTED_EDGE('',*,*,#15067,.T.);
#20629=ORIENTED_EDGE('',*,*,#15069,.T.);
#20630=ORIENTED_EDGE('',*,*,#15070,.F.);
#20631=ORIENTED_EDGE('',*,*,#15069,.F.);
#20632=ORIENTED_EDGE('',*,*,#15066,.T.);
#20633=ORIENTED_EDGE('',*,*,#15071,.T.);
#20634=ORIENTED_EDGE('',*,*,#15072,.F.);
#20635=ORIENTED_EDGE('',*,*,#15071,.F.);
#20636=ORIENTED_EDGE('',*,*,#15065,.F.);
#20637=ORIENTED_EDGE('',*,*,#15073,.F.);
#20638=ORIENTED_EDGE('',*,*,#15074,.T.);
#20639=ORIENTED_EDGE('',*,*,#15075,.F.);
#20640=ORIENTED_EDGE('',*,*,#15076,.F.);
#20641=ORIENTED_EDGE('',*,*,#15077,.F.);
#20642=ORIENTED_EDGE('',*,*,#15076,.T.);
#20643=ORIENTED_EDGE('',*,*,#15078,.T.);
#20644=ORIENTED_EDGE('',*,*,#15079,.F.);
#20645=ORIENTED_EDGE('',*,*,#15078,.F.);
#20646=ORIENTED_EDGE('',*,*,#15075,.T.);
#20647=ORIENTED_EDGE('',*,*,#15080,.T.);
#20648=ORIENTED_EDGE('',*,*,#15081,.F.);
#20649=ORIENTED_EDGE('',*,*,#15080,.F.);
#20650=ORIENTED_EDGE('',*,*,#15074,.F.);
#20651=ORIENTED_EDGE('',*,*,#15082,.F.);
#20652=ORIENTED_EDGE('',*,*,#15083,.T.);
#20653=ORIENTED_EDGE('',*,*,#15084,.F.);
#20654=ORIENTED_EDGE('',*,*,#15085,.F.);
#20655=ORIENTED_EDGE('',*,*,#15086,.F.);
#20656=ORIENTED_EDGE('',*,*,#15085,.T.);
#20657=ORIENTED_EDGE('',*,*,#15087,.T.);
#20658=ORIENTED_EDGE('',*,*,#15088,.F.);
#20659=ORIENTED_EDGE('',*,*,#15087,.F.);
#20660=ORIENTED_EDGE('',*,*,#15084,.T.);
#20661=ORIENTED_EDGE('',*,*,#15089,.T.);
#20662=ORIENTED_EDGE('',*,*,#15090,.F.);
#20663=ORIENTED_EDGE('',*,*,#15089,.F.);
#20664=ORIENTED_EDGE('',*,*,#15083,.F.);
#20665=ORIENTED_EDGE('',*,*,#15091,.F.);
#20666=ORIENTED_EDGE('',*,*,#15092,.T.);
#20667=ORIENTED_EDGE('',*,*,#15093,.F.);
#20668=ORIENTED_EDGE('',*,*,#15094,.F.);
#20669=ORIENTED_EDGE('',*,*,#15095,.F.);
#20670=ORIENTED_EDGE('',*,*,#15094,.T.);
#20671=ORIENTED_EDGE('',*,*,#15096,.T.);
#20672=ORIENTED_EDGE('',*,*,#15097,.F.);
#20673=ORIENTED_EDGE('',*,*,#15096,.F.);
#20674=ORIENTED_EDGE('',*,*,#15093,.T.);
#20675=ORIENTED_EDGE('',*,*,#15098,.T.);
#20676=ORIENTED_EDGE('',*,*,#15099,.F.);
#20677=ORIENTED_EDGE('',*,*,#15098,.F.);
#20678=ORIENTED_EDGE('',*,*,#15092,.F.);
#20679=ORIENTED_EDGE('',*,*,#15100,.F.);
#20680=ORIENTED_EDGE('',*,*,#15101,.T.);
#20681=ORIENTED_EDGE('',*,*,#15102,.F.);
#20682=ORIENTED_EDGE('',*,*,#15103,.F.);
#20683=ORIENTED_EDGE('',*,*,#15104,.F.);
#20684=ORIENTED_EDGE('',*,*,#15103,.T.);
#20685=ORIENTED_EDGE('',*,*,#15105,.T.);
#20686=ORIENTED_EDGE('',*,*,#15106,.F.);
#20687=ORIENTED_EDGE('',*,*,#15105,.F.);
#20688=ORIENTED_EDGE('',*,*,#15102,.T.);
#20689=ORIENTED_EDGE('',*,*,#15107,.T.);
#20690=ORIENTED_EDGE('',*,*,#15108,.F.);
#20691=ORIENTED_EDGE('',*,*,#15107,.F.);
#20692=ORIENTED_EDGE('',*,*,#15101,.F.);
#20693=ORIENTED_EDGE('',*,*,#15109,.F.);
#20694=ORIENTED_EDGE('',*,*,#15110,.T.);
#20695=ORIENTED_EDGE('',*,*,#15111,.F.);
#20696=ORIENTED_EDGE('',*,*,#15112,.F.);
#20697=ORIENTED_EDGE('',*,*,#15113,.F.);
#20698=ORIENTED_EDGE('',*,*,#15112,.T.);
#20699=ORIENTED_EDGE('',*,*,#15114,.T.);
#20700=ORIENTED_EDGE('',*,*,#15115,.F.);
#20701=ORIENTED_EDGE('',*,*,#15114,.F.);
#20702=ORIENTED_EDGE('',*,*,#15111,.T.);
#20703=ORIENTED_EDGE('',*,*,#15116,.T.);
#20704=ORIENTED_EDGE('',*,*,#15117,.F.);
#20705=ORIENTED_EDGE('',*,*,#15116,.F.);
#20706=ORIENTED_EDGE('',*,*,#15110,.F.);
#20707=ORIENTED_EDGE('',*,*,#15118,.F.);
#20708=ORIENTED_EDGE('',*,*,#15119,.T.);
#20709=ORIENTED_EDGE('',*,*,#15120,.F.);
#20710=ORIENTED_EDGE('',*,*,#15121,.F.);
#20711=ORIENTED_EDGE('',*,*,#15122,.F.);
#20712=ORIENTED_EDGE('',*,*,#15121,.T.);
#20713=ORIENTED_EDGE('',*,*,#15123,.T.);
#20714=ORIENTED_EDGE('',*,*,#15124,.F.);
#20715=ORIENTED_EDGE('',*,*,#15123,.F.);
#20716=ORIENTED_EDGE('',*,*,#15120,.T.);
#20717=ORIENTED_EDGE('',*,*,#15125,.T.);
#20718=ORIENTED_EDGE('',*,*,#15126,.F.);
#20719=ORIENTED_EDGE('',*,*,#15125,.F.);
#20720=ORIENTED_EDGE('',*,*,#15119,.F.);
#20721=ORIENTED_EDGE('',*,*,#15127,.F.);
#20722=ORIENTED_EDGE('',*,*,#15128,.T.);
#20723=ORIENTED_EDGE('',*,*,#15129,.F.);
#20724=ORIENTED_EDGE('',*,*,#15130,.F.);
#20725=ORIENTED_EDGE('',*,*,#15131,.F.);
#20726=ORIENTED_EDGE('',*,*,#15130,.T.);
#20727=ORIENTED_EDGE('',*,*,#15132,.T.);
#20728=ORIENTED_EDGE('',*,*,#15133,.F.);
#20729=ORIENTED_EDGE('',*,*,#15132,.F.);
#20730=ORIENTED_EDGE('',*,*,#15129,.T.);
#20731=ORIENTED_EDGE('',*,*,#15134,.T.);
#20732=ORIENTED_EDGE('',*,*,#15135,.F.);
#20733=ORIENTED_EDGE('',*,*,#15134,.F.);
#20734=ORIENTED_EDGE('',*,*,#15128,.F.);
#20735=ORIENTED_EDGE('',*,*,#15136,.F.);
#20736=ORIENTED_EDGE('',*,*,#15137,.T.);
#20737=ORIENTED_EDGE('',*,*,#15138,.F.);
#20738=ORIENTED_EDGE('',*,*,#15139,.F.);
#20739=ORIENTED_EDGE('',*,*,#15140,.F.);
#20740=ORIENTED_EDGE('',*,*,#15139,.T.);
#20741=ORIENTED_EDGE('',*,*,#15141,.T.);
#20742=ORIENTED_EDGE('',*,*,#15142,.F.);
#20743=ORIENTED_EDGE('',*,*,#15141,.F.);
#20744=ORIENTED_EDGE('',*,*,#15138,.T.);
#20745=ORIENTED_EDGE('',*,*,#15143,.T.);
#20746=ORIENTED_EDGE('',*,*,#15144,.F.);
#20747=ORIENTED_EDGE('',*,*,#15143,.F.);
#20748=ORIENTED_EDGE('',*,*,#15137,.F.);
#20749=ORIENTED_EDGE('',*,*,#15145,.F.);
#20750=ORIENTED_EDGE('',*,*,#15146,.T.);
#20751=ORIENTED_EDGE('',*,*,#15147,.F.);
#20752=ORIENTED_EDGE('',*,*,#15148,.F.);
#20753=ORIENTED_EDGE('',*,*,#15149,.F.);
#20754=ORIENTED_EDGE('',*,*,#15148,.T.);
#20755=ORIENTED_EDGE('',*,*,#15150,.T.);
#20756=ORIENTED_EDGE('',*,*,#15151,.F.);
#20757=ORIENTED_EDGE('',*,*,#15150,.F.);
#20758=ORIENTED_EDGE('',*,*,#15147,.T.);
#20759=ORIENTED_EDGE('',*,*,#15152,.T.);
#20760=ORIENTED_EDGE('',*,*,#15153,.F.);
#20761=ORIENTED_EDGE('',*,*,#15152,.F.);
#20762=ORIENTED_EDGE('',*,*,#15146,.F.);
#20763=ORIENTED_EDGE('',*,*,#15154,.F.);
#20764=ORIENTED_EDGE('',*,*,#15155,.T.);
#20765=ORIENTED_EDGE('',*,*,#15156,.F.);
#20766=ORIENTED_EDGE('',*,*,#15157,.F.);
#20767=ORIENTED_EDGE('',*,*,#15158,.F.);
#20768=ORIENTED_EDGE('',*,*,#15157,.T.);
#20769=ORIENTED_EDGE('',*,*,#15159,.T.);
#20770=ORIENTED_EDGE('',*,*,#15160,.F.);
#20771=ORIENTED_EDGE('',*,*,#15159,.F.);
#20772=ORIENTED_EDGE('',*,*,#15156,.T.);
#20773=ORIENTED_EDGE('',*,*,#15161,.T.);
#20774=ORIENTED_EDGE('',*,*,#15162,.F.);
#20775=ORIENTED_EDGE('',*,*,#15161,.F.);
#20776=ORIENTED_EDGE('',*,*,#15155,.F.);
#20777=ORIENTED_EDGE('',*,*,#15163,.F.);
#20778=ORIENTED_EDGE('',*,*,#15164,.T.);
#20779=ORIENTED_EDGE('',*,*,#15165,.F.);
#20780=ORIENTED_EDGE('',*,*,#15166,.F.);
#20781=ORIENTED_EDGE('',*,*,#15167,.F.);
#20782=ORIENTED_EDGE('',*,*,#15166,.T.);
#20783=ORIENTED_EDGE('',*,*,#15168,.T.);
#20784=ORIENTED_EDGE('',*,*,#15169,.F.);
#20785=ORIENTED_EDGE('',*,*,#15168,.F.);
#20786=ORIENTED_EDGE('',*,*,#15165,.T.);
#20787=ORIENTED_EDGE('',*,*,#15170,.T.);
#20788=ORIENTED_EDGE('',*,*,#15171,.F.);
#20789=ORIENTED_EDGE('',*,*,#15170,.F.);
#20790=ORIENTED_EDGE('',*,*,#15164,.F.);
#20791=ORIENTED_EDGE('',*,*,#15172,.F.);
#20792=ORIENTED_EDGE('',*,*,#15173,.T.);
#20793=ORIENTED_EDGE('',*,*,#15174,.F.);
#20794=ORIENTED_EDGE('',*,*,#15175,.F.);
#20795=ORIENTED_EDGE('',*,*,#15176,.F.);
#20796=ORIENTED_EDGE('',*,*,#15175,.T.);
#20797=ORIENTED_EDGE('',*,*,#15177,.T.);
#20798=ORIENTED_EDGE('',*,*,#15178,.F.);
#20799=ORIENTED_EDGE('',*,*,#15177,.F.);
#20800=ORIENTED_EDGE('',*,*,#15174,.T.);
#20801=ORIENTED_EDGE('',*,*,#15179,.T.);
#20802=ORIENTED_EDGE('',*,*,#15180,.F.);
#20803=ORIENTED_EDGE('',*,*,#15179,.F.);
#20804=ORIENTED_EDGE('',*,*,#15173,.F.);
#20805=ORIENTED_EDGE('',*,*,#15181,.F.);
#20806=ORIENTED_EDGE('',*,*,#15182,.T.);
#20807=ORIENTED_EDGE('',*,*,#15183,.F.);
#20808=ORIENTED_EDGE('',*,*,#15184,.F.);
#20809=ORIENTED_EDGE('',*,*,#15185,.F.);
#20810=ORIENTED_EDGE('',*,*,#15184,.T.);
#20811=ORIENTED_EDGE('',*,*,#15186,.T.);
#20812=ORIENTED_EDGE('',*,*,#15187,.F.);
#20813=ORIENTED_EDGE('',*,*,#15186,.F.);
#20814=ORIENTED_EDGE('',*,*,#15183,.T.);
#20815=ORIENTED_EDGE('',*,*,#15188,.T.);
#20816=ORIENTED_EDGE('',*,*,#15189,.F.);
#20817=ORIENTED_EDGE('',*,*,#15188,.F.);
#20818=ORIENTED_EDGE('',*,*,#15182,.F.);
#20819=ORIENTED_EDGE('',*,*,#15190,.F.);
#20820=ORIENTED_EDGE('',*,*,#15191,.T.);
#20821=ORIENTED_EDGE('',*,*,#15192,.T.);
#20822=ORIENTED_EDGE('',*,*,#15193,.F.);
#20823=ORIENTED_EDGE('',*,*,#15194,.T.);
#20824=ORIENTED_EDGE('',*,*,#15195,.F.);
#20825=ORIENTED_EDGE('',*,*,#15191,.F.);
#20826=ORIENTED_EDGE('',*,*,#15196,.F.);
#20827=ORIENTED_EDGE('',*,*,#15192,.F.);
#20828=ORIENTED_EDGE('',*,*,#15195,.T.);
#20829=ORIENTED_EDGE('',*,*,#15197,.T.);
#20830=ORIENTED_EDGE('',*,*,#15198,.F.);
#20831=ORIENTED_EDGE('',*,*,#15197,.F.);
#20832=ORIENTED_EDGE('',*,*,#15194,.F.);
#20833=ORIENTED_EDGE('',*,*,#15199,.F.);
#20834=ORIENTED_EDGE('',*,*,#15200,.T.);
#20835=ORIENTED_EDGE('',*,*,#15201,.F.);
#20836=ORIENTED_EDGE('',*,*,#15202,.F.);
#20837=ORIENTED_EDGE('',*,*,#15203,.F.);
#20838=ORIENTED_EDGE('',*,*,#15202,.T.);
#20839=ORIENTED_EDGE('',*,*,#15204,.T.);
#20840=ORIENTED_EDGE('',*,*,#15205,.F.);
#20841=ORIENTED_EDGE('',*,*,#15204,.F.);
#20842=ORIENTED_EDGE('',*,*,#15201,.T.);
#20843=ORIENTED_EDGE('',*,*,#15206,.T.);
#20844=ORIENTED_EDGE('',*,*,#15207,.F.);
#20845=ORIENTED_EDGE('',*,*,#15206,.F.);
#20846=ORIENTED_EDGE('',*,*,#15200,.F.);
#20847=ORIENTED_EDGE('',*,*,#15208,.F.);
#20848=ORIENTED_EDGE('',*,*,#15209,.T.);
#20849=ORIENTED_EDGE('',*,*,#15210,.F.);
#20850=ORIENTED_EDGE('',*,*,#15211,.F.);
#20851=ORIENTED_EDGE('',*,*,#15212,.F.);
#20852=ORIENTED_EDGE('',*,*,#15211,.T.);
#20853=ORIENTED_EDGE('',*,*,#15213,.T.);
#20854=ORIENTED_EDGE('',*,*,#15214,.F.);
#20855=ORIENTED_EDGE('',*,*,#15213,.F.);
#20856=ORIENTED_EDGE('',*,*,#15210,.T.);
#20857=ORIENTED_EDGE('',*,*,#15215,.T.);
#20858=ORIENTED_EDGE('',*,*,#15216,.F.);
#20859=ORIENTED_EDGE('',*,*,#15215,.F.);
#20860=ORIENTED_EDGE('',*,*,#15209,.F.);
#20861=ORIENTED_EDGE('',*,*,#15217,.F.);
#20862=ORIENTED_EDGE('',*,*,#15218,.T.);
#20863=ORIENTED_EDGE('',*,*,#15219,.F.);
#20864=ORIENTED_EDGE('',*,*,#15220,.F.);
#20865=ORIENTED_EDGE('',*,*,#15221,.F.);
#20866=ORIENTED_EDGE('',*,*,#15220,.T.);
#20867=ORIENTED_EDGE('',*,*,#15222,.T.);
#20868=ORIENTED_EDGE('',*,*,#15223,.F.);
#20869=ORIENTED_EDGE('',*,*,#15222,.F.);
#20870=ORIENTED_EDGE('',*,*,#15219,.T.);
#20871=ORIENTED_EDGE('',*,*,#15224,.T.);
#20872=ORIENTED_EDGE('',*,*,#15225,.F.);
#20873=ORIENTED_EDGE('',*,*,#15224,.F.);
#20874=ORIENTED_EDGE('',*,*,#15218,.F.);
#20875=ORIENTED_EDGE('',*,*,#15226,.F.);
#20876=ORIENTED_EDGE('',*,*,#15227,.T.);
#20877=ORIENTED_EDGE('',*,*,#15228,.F.);
#20878=ORIENTED_EDGE('',*,*,#15229,.F.);
#20879=ORIENTED_EDGE('',*,*,#15230,.F.);
#20880=ORIENTED_EDGE('',*,*,#15229,.T.);
#20881=ORIENTED_EDGE('',*,*,#15231,.T.);
#20882=ORIENTED_EDGE('',*,*,#15232,.F.);
#20883=ORIENTED_EDGE('',*,*,#15231,.F.);
#20884=ORIENTED_EDGE('',*,*,#15228,.T.);
#20885=ORIENTED_EDGE('',*,*,#15233,.T.);
#20886=ORIENTED_EDGE('',*,*,#15234,.F.);
#20887=ORIENTED_EDGE('',*,*,#15233,.F.);
#20888=ORIENTED_EDGE('',*,*,#15227,.F.);
#20889=ORIENTED_EDGE('',*,*,#15235,.F.);
#20890=ORIENTED_EDGE('',*,*,#15236,.T.);
#20891=ORIENTED_EDGE('',*,*,#15237,.F.);
#20892=ORIENTED_EDGE('',*,*,#15238,.F.);
#20893=ORIENTED_EDGE('',*,*,#15239,.F.);
#20894=ORIENTED_EDGE('',*,*,#15238,.T.);
#20895=ORIENTED_EDGE('',*,*,#15240,.T.);
#20896=ORIENTED_EDGE('',*,*,#15241,.F.);
#20897=ORIENTED_EDGE('',*,*,#15240,.F.);
#20898=ORIENTED_EDGE('',*,*,#15237,.T.);
#20899=ORIENTED_EDGE('',*,*,#15242,.T.);
#20900=ORIENTED_EDGE('',*,*,#15243,.F.);
#20901=ORIENTED_EDGE('',*,*,#15242,.F.);
#20902=ORIENTED_EDGE('',*,*,#15236,.F.);
#20903=ORIENTED_EDGE('',*,*,#15244,.F.);
#20904=ORIENTED_EDGE('',*,*,#15245,.T.);
#20905=ORIENTED_EDGE('',*,*,#15246,.F.);
#20906=ORIENTED_EDGE('',*,*,#15247,.F.);
#20907=ORIENTED_EDGE('',*,*,#15248,.F.);
#20908=ORIENTED_EDGE('',*,*,#15247,.T.);
#20909=ORIENTED_EDGE('',*,*,#15249,.T.);
#20910=ORIENTED_EDGE('',*,*,#15250,.F.);
#20911=ORIENTED_EDGE('',*,*,#15249,.F.);
#20912=ORIENTED_EDGE('',*,*,#15246,.T.);
#20913=ORIENTED_EDGE('',*,*,#15251,.T.);
#20914=ORIENTED_EDGE('',*,*,#15252,.F.);
#20915=ORIENTED_EDGE('',*,*,#15251,.F.);
#20916=ORIENTED_EDGE('',*,*,#15245,.F.);
#20917=ORIENTED_EDGE('',*,*,#15253,.F.);
#20918=ORIENTED_EDGE('',*,*,#15254,.T.);
#20919=ORIENTED_EDGE('',*,*,#15255,.F.);
#20920=ORIENTED_EDGE('',*,*,#15256,.F.);
#20921=ORIENTED_EDGE('',*,*,#15257,.F.);
#20922=ORIENTED_EDGE('',*,*,#15256,.T.);
#20923=ORIENTED_EDGE('',*,*,#15258,.T.);
#20924=ORIENTED_EDGE('',*,*,#15259,.F.);
#20925=ORIENTED_EDGE('',*,*,#15258,.F.);
#20926=ORIENTED_EDGE('',*,*,#15255,.T.);
#20927=ORIENTED_EDGE('',*,*,#15260,.T.);
#20928=ORIENTED_EDGE('',*,*,#15261,.F.);
#20929=ORIENTED_EDGE('',*,*,#15260,.F.);
#20930=ORIENTED_EDGE('',*,*,#15254,.F.);
#20931=ORIENTED_EDGE('',*,*,#15262,.F.);
#20932=ORIENTED_EDGE('',*,*,#15263,.T.);
#20933=ORIENTED_EDGE('',*,*,#15264,.F.);
#20934=ORIENTED_EDGE('',*,*,#15265,.F.);
#20935=ORIENTED_EDGE('',*,*,#15266,.F.);
#20936=ORIENTED_EDGE('',*,*,#15265,.T.);
#20937=ORIENTED_EDGE('',*,*,#15267,.T.);
#20938=ORIENTED_EDGE('',*,*,#15268,.F.);
#20939=ORIENTED_EDGE('',*,*,#15267,.F.);
#20940=ORIENTED_EDGE('',*,*,#15264,.T.);
#20941=ORIENTED_EDGE('',*,*,#15269,.T.);
#20942=ORIENTED_EDGE('',*,*,#15270,.F.);
#20943=ORIENTED_EDGE('',*,*,#15269,.F.);
#20944=ORIENTED_EDGE('',*,*,#15263,.F.);
#20945=ORIENTED_EDGE('',*,*,#15271,.F.);
#20946=ORIENTED_EDGE('',*,*,#15272,.T.);
#20947=ORIENTED_EDGE('',*,*,#15273,.F.);
#20948=ORIENTED_EDGE('',*,*,#15274,.F.);
#20949=ORIENTED_EDGE('',*,*,#15275,.F.);
#20950=ORIENTED_EDGE('',*,*,#15274,.T.);
#20951=ORIENTED_EDGE('',*,*,#15276,.T.);
#20952=ORIENTED_EDGE('',*,*,#15277,.F.);
#20953=ORIENTED_EDGE('',*,*,#15276,.F.);
#20954=ORIENTED_EDGE('',*,*,#15273,.T.);
#20955=ORIENTED_EDGE('',*,*,#15278,.T.);
#20956=ORIENTED_EDGE('',*,*,#15279,.F.);
#20957=ORIENTED_EDGE('',*,*,#15278,.F.);
#20958=ORIENTED_EDGE('',*,*,#15272,.F.);
#20959=ORIENTED_EDGE('',*,*,#15280,.F.);
#20960=ORIENTED_EDGE('',*,*,#14919,.F.);
#20961=ORIENTED_EDGE('',*,*,#14819,.F.);
#20962=ORIENTED_EDGE('',*,*,#14920,.F.);
#20963=ORIENTED_EDGE('',*,*,#15281,.T.);
#20964=ORIENTED_EDGE('',*,*,#15280,.T.);
#20965=ORIENTED_EDGE('',*,*,#15281,.F.);
#20966=ORIENTED_EDGE('',*,*,#15282,.F.);
#20967=ORIENTED_EDGE('',*,*,#15283,.T.);
#20968=ORIENTED_EDGE('',*,*,#14928,.T.);
#20969=ORIENTED_EDGE('',*,*,#15283,.F.);
#20970=ORIENTED_EDGE('',*,*,#14954,.T.);
#20971=ORIENTED_EDGE('',*,*,#15284,.F.);
#20972=ORIENTED_EDGE('',*,*,#15268,.T.);
#20973=ORIENTED_EDGE('',*,*,#15270,.T.);
#20974=ORIENTED_EDGE('',*,*,#15262,.T.);
#20975=ORIENTED_EDGE('',*,*,#15285,.F.);
#20976=ORIENTED_EDGE('',*,*,#14969,.T.);
#20977=ORIENTED_EDGE('',*,*,#14971,.T.);
#20978=ORIENTED_EDGE('',*,*,#14963,.T.);
#20979=ORIENTED_EDGE('',*,*,#15286,.F.);
#20980=ORIENTED_EDGE('',*,*,#15259,.T.);
#20981=ORIENTED_EDGE('',*,*,#15261,.T.);
#20982=ORIENTED_EDGE('',*,*,#15253,.T.);
#20983=ORIENTED_EDGE('',*,*,#15287,.F.);
#20984=ORIENTED_EDGE('',*,*,#14978,.T.);
#20985=ORIENTED_EDGE('',*,*,#14980,.T.);
#20986=ORIENTED_EDGE('',*,*,#14972,.T.);
#20987=ORIENTED_EDGE('',*,*,#15288,.F.);
#20988=ORIENTED_EDGE('',*,*,#15250,.T.);
#20989=ORIENTED_EDGE('',*,*,#15252,.T.);
#20990=ORIENTED_EDGE('',*,*,#15244,.T.);
#20991=ORIENTED_EDGE('',*,*,#15289,.F.);
#20992=ORIENTED_EDGE('',*,*,#14987,.T.);
#20993=ORIENTED_EDGE('',*,*,#14989,.T.);
#20994=ORIENTED_EDGE('',*,*,#14981,.T.);
#20995=ORIENTED_EDGE('',*,*,#15290,.F.);
#20996=ORIENTED_EDGE('',*,*,#15241,.T.);
#20997=ORIENTED_EDGE('',*,*,#15243,.T.);
#20998=ORIENTED_EDGE('',*,*,#15235,.T.);
#20999=ORIENTED_EDGE('',*,*,#15291,.F.);
#21000=ORIENTED_EDGE('',*,*,#14996,.T.);
#21001=ORIENTED_EDGE('',*,*,#14998,.T.);
#21002=ORIENTED_EDGE('',*,*,#14990,.T.);
#21003=ORIENTED_EDGE('',*,*,#15292,.F.);
#21004=ORIENTED_EDGE('',*,*,#15232,.T.);
#21005=ORIENTED_EDGE('',*,*,#15234,.T.);
#21006=ORIENTED_EDGE('',*,*,#15226,.T.);
#21007=ORIENTED_EDGE('',*,*,#15293,.F.);
#21008=ORIENTED_EDGE('',*,*,#15005,.T.);
#21009=ORIENTED_EDGE('',*,*,#15007,.T.);
#21010=ORIENTED_EDGE('',*,*,#14999,.T.);
#21011=ORIENTED_EDGE('',*,*,#15294,.F.);
#21012=ORIENTED_EDGE('',*,*,#15223,.T.);
#21013=ORIENTED_EDGE('',*,*,#15225,.T.);
#21014=ORIENTED_EDGE('',*,*,#15217,.T.);
#21015=ORIENTED_EDGE('',*,*,#15295,.F.);
#21016=ORIENTED_EDGE('',*,*,#15014,.T.);
#21017=ORIENTED_EDGE('',*,*,#15016,.T.);
#21018=ORIENTED_EDGE('',*,*,#15008,.T.);
#21019=ORIENTED_EDGE('',*,*,#15296,.F.);
#21020=ORIENTED_EDGE('',*,*,#15214,.T.);
#21021=ORIENTED_EDGE('',*,*,#15216,.T.);
#21022=ORIENTED_EDGE('',*,*,#15208,.T.);
#21023=ORIENTED_EDGE('',*,*,#15297,.F.);
#21024=ORIENTED_EDGE('',*,*,#15023,.T.);
#21025=ORIENTED_EDGE('',*,*,#15025,.T.);
#21026=ORIENTED_EDGE('',*,*,#15017,.T.);
#21027=ORIENTED_EDGE('',*,*,#15298,.F.);
#21028=ORIENTED_EDGE('',*,*,#15205,.T.);
#21029=ORIENTED_EDGE('',*,*,#15207,.T.);
#21030=ORIENTED_EDGE('',*,*,#15199,.T.);
#21031=ORIENTED_EDGE('',*,*,#15299,.F.);
#21032=ORIENTED_EDGE('',*,*,#15033,.T.);
#21033=ORIENTED_EDGE('',*,*,#15035,.T.);
#21034=ORIENTED_EDGE('',*,*,#15300,.T.);
#21035=ORIENTED_EDGE('',*,*,#15282,.T.);
#21036=ORIENTED_EDGE('',*,*,#15300,.F.);
#21037=ORIENTED_EDGE('',*,*,#15036,.T.);
#21038=ORIENTED_EDGE('',*,*,#15026,.T.);
#21039=ORIENTED_EDGE('',*,*,#15301,.F.);
#21040=ORIENTED_EDGE('',*,*,#15043,.T.);
#21041=ORIENTED_EDGE('',*,*,#15045,.T.);
#21042=ORIENTED_EDGE('',*,*,#15037,.T.);
#21043=ORIENTED_EDGE('',*,*,#15302,.F.);
#21044=ORIENTED_EDGE('',*,*,#15187,.T.);
#21045=ORIENTED_EDGE('',*,*,#15189,.T.);
#21046=ORIENTED_EDGE('',*,*,#15181,.T.);
#21047=ORIENTED_EDGE('',*,*,#15303,.F.);
#21048=ORIENTED_EDGE('',*,*,#15052,.T.);
#21049=ORIENTED_EDGE('',*,*,#15054,.T.);
#21050=ORIENTED_EDGE('',*,*,#15046,.T.);
#21051=ORIENTED_EDGE('',*,*,#15304,.F.);
#21052=ORIENTED_EDGE('',*,*,#15178,.T.);
#21053=ORIENTED_EDGE('',*,*,#15180,.T.);
#21054=ORIENTED_EDGE('',*,*,#15172,.T.);
#21055=ORIENTED_EDGE('',*,*,#15305,.F.);
#21056=ORIENTED_EDGE('',*,*,#15061,.T.);
#21057=ORIENTED_EDGE('',*,*,#15063,.T.);
#21058=ORIENTED_EDGE('',*,*,#15055,.T.);
#21059=ORIENTED_EDGE('',*,*,#15306,.F.);
#21060=ORIENTED_EDGE('',*,*,#15169,.T.);
#21061=ORIENTED_EDGE('',*,*,#15171,.T.);
#21062=ORIENTED_EDGE('',*,*,#15163,.T.);
#21063=ORIENTED_EDGE('',*,*,#15307,.F.);
#21064=ORIENTED_EDGE('',*,*,#15070,.T.);
#21065=ORIENTED_EDGE('',*,*,#15072,.T.);
#21066=ORIENTED_EDGE('',*,*,#15064,.T.);
#21067=ORIENTED_EDGE('',*,*,#15308,.F.);
#21068=ORIENTED_EDGE('',*,*,#15160,.T.);
#21069=ORIENTED_EDGE('',*,*,#15162,.T.);
#21070=ORIENTED_EDGE('',*,*,#15154,.T.);
#21071=ORIENTED_EDGE('',*,*,#15309,.F.);
#21072=ORIENTED_EDGE('',*,*,#15079,.T.);
#21073=ORIENTED_EDGE('',*,*,#15081,.T.);
#21074=ORIENTED_EDGE('',*,*,#15073,.T.);
#21075=ORIENTED_EDGE('',*,*,#15310,.F.);
#21076=ORIENTED_EDGE('',*,*,#15151,.T.);
#21077=ORIENTED_EDGE('',*,*,#15153,.T.);
#21078=ORIENTED_EDGE('',*,*,#15145,.T.);
#21079=ORIENTED_EDGE('',*,*,#15311,.F.);
#21080=ORIENTED_EDGE('',*,*,#15088,.T.);
#21081=ORIENTED_EDGE('',*,*,#15090,.T.);
#21082=ORIENTED_EDGE('',*,*,#15082,.T.);
#21083=ORIENTED_EDGE('',*,*,#15312,.F.);
#21084=ORIENTED_EDGE('',*,*,#15142,.T.);
#21085=ORIENTED_EDGE('',*,*,#15144,.T.);
#21086=ORIENTED_EDGE('',*,*,#15136,.T.);
#21087=ORIENTED_EDGE('',*,*,#15313,.F.);
#21088=ORIENTED_EDGE('',*,*,#15097,.T.);
#21089=ORIENTED_EDGE('',*,*,#15099,.T.);
#21090=ORIENTED_EDGE('',*,*,#15091,.T.);
#21091=ORIENTED_EDGE('',*,*,#15314,.F.);
#21092=ORIENTED_EDGE('',*,*,#15133,.T.);
#21093=ORIENTED_EDGE('',*,*,#15135,.T.);
#21094=ORIENTED_EDGE('',*,*,#15127,.T.);
#21095=ORIENTED_EDGE('',*,*,#15315,.F.);
#21096=ORIENTED_EDGE('',*,*,#15106,.T.);
#21097=ORIENTED_EDGE('',*,*,#15108,.T.);
#21098=ORIENTED_EDGE('',*,*,#15100,.T.);
#21099=ORIENTED_EDGE('',*,*,#15316,.F.);
#21100=ORIENTED_EDGE('',*,*,#15124,.T.);
#21101=ORIENTED_EDGE('',*,*,#15126,.T.);
#21102=ORIENTED_EDGE('',*,*,#15118,.T.);
#21103=ORIENTED_EDGE('',*,*,#15317,.F.);
#21104=ORIENTED_EDGE('',*,*,#15115,.T.);
#21105=ORIENTED_EDGE('',*,*,#15117,.T.);
#21106=ORIENTED_EDGE('',*,*,#15109,.T.);
#21107=ORIENTED_EDGE('',*,*,#15318,.F.);
#21108=ORIENTED_EDGE('',*,*,#15196,.T.);
#21109=ORIENTED_EDGE('',*,*,#15198,.T.);
#21110=ORIENTED_EDGE('',*,*,#15193,.T.);
#21111=ORIENTED_EDGE('',*,*,#15319,.F.);
#21112=ORIENTED_EDGE('',*,*,#15277,.T.);
#21113=ORIENTED_EDGE('',*,*,#15279,.T.);
#21114=ORIENTED_EDGE('',*,*,#15271,.T.);
#21115=ORIENTED_EDGE('',*,*,#15320,.F.);
#21116=ORIENTED_EDGE('',*,*,#14960,.T.);
#21117=ORIENTED_EDGE('',*,*,#14962,.T.);
#21118=ORIENTED_EDGE('',*,*,#15321,.F.);
#21119=ORIENTED_EDGE('',*,*,#15322,.T.);
#21120=ORIENTED_EDGE('',*,*,#15032,.T.);
#21121=ORIENTED_EDGE('',*,*,#15299,.T.);
#21122=ORIENTED_EDGE('',*,*,#15203,.T.);
#21123=ORIENTED_EDGE('',*,*,#15298,.T.);
#21124=ORIENTED_EDGE('',*,*,#15021,.T.);
#21125=ORIENTED_EDGE('',*,*,#15297,.T.);
#21126=ORIENTED_EDGE('',*,*,#15212,.T.);
#21127=ORIENTED_EDGE('',*,*,#15296,.T.);
#21128=ORIENTED_EDGE('',*,*,#15012,.T.);
#21129=ORIENTED_EDGE('',*,*,#15295,.T.);
#21130=ORIENTED_EDGE('',*,*,#15221,.T.);
#21131=ORIENTED_EDGE('',*,*,#15294,.T.);
#21132=ORIENTED_EDGE('',*,*,#15003,.T.);
#21133=ORIENTED_EDGE('',*,*,#15293,.T.);
#21134=ORIENTED_EDGE('',*,*,#15230,.T.);
#21135=ORIENTED_EDGE('',*,*,#15292,.T.);
#21136=ORIENTED_EDGE('',*,*,#14994,.T.);
#21137=ORIENTED_EDGE('',*,*,#15291,.T.);
#21138=ORIENTED_EDGE('',*,*,#15239,.T.);
#21139=ORIENTED_EDGE('',*,*,#15290,.T.);
#21140=ORIENTED_EDGE('',*,*,#14985,.T.);
#21141=ORIENTED_EDGE('',*,*,#15289,.T.);
#21142=ORIENTED_EDGE('',*,*,#15248,.T.);
#21143=ORIENTED_EDGE('',*,*,#15288,.T.);
#21144=ORIENTED_EDGE('',*,*,#14976,.T.);
#21145=ORIENTED_EDGE('',*,*,#15287,.T.);
#21146=ORIENTED_EDGE('',*,*,#15257,.T.);
#21147=ORIENTED_EDGE('',*,*,#15286,.T.);
#21148=ORIENTED_EDGE('',*,*,#14967,.T.);
#21149=ORIENTED_EDGE('',*,*,#15285,.T.);
#21150=ORIENTED_EDGE('',*,*,#15266,.T.);
#21151=ORIENTED_EDGE('',*,*,#15284,.T.);
#21152=ORIENTED_EDGE('',*,*,#14958,.T.);
#21153=ORIENTED_EDGE('',*,*,#15320,.T.);
#21154=ORIENTED_EDGE('',*,*,#15275,.T.);
#21155=ORIENTED_EDGE('',*,*,#15319,.T.);
#21156=ORIENTED_EDGE('',*,*,#15190,.T.);
#21157=ORIENTED_EDGE('',*,*,#15318,.T.);
#21158=ORIENTED_EDGE('',*,*,#15113,.T.);
#21159=ORIENTED_EDGE('',*,*,#15317,.T.);
#21160=ORIENTED_EDGE('',*,*,#15122,.T.);
#21161=ORIENTED_EDGE('',*,*,#15316,.T.);
#21162=ORIENTED_EDGE('',*,*,#15104,.T.);
#21163=ORIENTED_EDGE('',*,*,#15315,.T.);
#21164=ORIENTED_EDGE('',*,*,#15131,.T.);
#21165=ORIENTED_EDGE('',*,*,#15314,.T.);
#21166=ORIENTED_EDGE('',*,*,#15095,.T.);
#21167=ORIENTED_EDGE('',*,*,#15313,.T.);
#21168=ORIENTED_EDGE('',*,*,#15140,.T.);
#21169=ORIENTED_EDGE('',*,*,#15312,.T.);
#21170=ORIENTED_EDGE('',*,*,#15086,.T.);
#21171=ORIENTED_EDGE('',*,*,#15311,.T.);
#21172=ORIENTED_EDGE('',*,*,#15149,.T.);
#21173=ORIENTED_EDGE('',*,*,#15310,.T.);
#21174=ORIENTED_EDGE('',*,*,#15077,.T.);
#21175=ORIENTED_EDGE('',*,*,#15309,.T.);
#21176=ORIENTED_EDGE('',*,*,#15158,.T.);
#21177=ORIENTED_EDGE('',*,*,#15308,.T.);
#21178=ORIENTED_EDGE('',*,*,#15068,.T.);
#21179=ORIENTED_EDGE('',*,*,#15307,.T.);
#21180=ORIENTED_EDGE('',*,*,#15167,.T.);
#21181=ORIENTED_EDGE('',*,*,#15306,.T.);
#21182=ORIENTED_EDGE('',*,*,#15059,.T.);
#21183=ORIENTED_EDGE('',*,*,#15305,.T.);
#21184=ORIENTED_EDGE('',*,*,#15176,.T.);
#21185=ORIENTED_EDGE('',*,*,#15304,.T.);
#21186=ORIENTED_EDGE('',*,*,#15050,.T.);
#21187=ORIENTED_EDGE('',*,*,#15303,.T.);
#21188=ORIENTED_EDGE('',*,*,#15185,.T.);
#21189=ORIENTED_EDGE('',*,*,#15302,.T.);
#21190=ORIENTED_EDGE('',*,*,#15041,.T.);
#21191=ORIENTED_EDGE('',*,*,#15301,.T.);
#21192=ORIENTED_EDGE('',*,*,#15030,.T.);
#21193=ORIENTED_EDGE('',*,*,#15322,.F.);
#21194=ORIENTED_EDGE('',*,*,#15321,.T.);
#21195=ORIENTED_EDGE('',*,*,#14942,.T.);
#21196=ORIENTED_EDGE('',*,*,#14953,.T.);
#21197=ORIENTED_EDGE('',*,*,#14951,.T.);
#21198=ORIENTED_EDGE('',*,*,#14949,.T.);
#21199=ORIENTED_EDGE('',*,*,#14947,.T.);
#21200=ORIENTED_EDGE('',*,*,#14945,.T.);
#25055=CONICAL_SURFACE('',#27936,0.173205080756888,1.03037682652431);
#25056=CONICAL_SURFACE('',#28163,0.375,0.785398163397448);
#25057=CONICAL_SURFACE('',#28164,0.635,0.785398163397449);
#25058=CONICAL_SURFACE('',#28203,0.625,0.785398163397448);
#25724=ADVANCED_FACE('',(#3136),#1268,.T.);
#25725=ADVANCED_FACE('',(#3137),#1269,.T.);
#25726=ADVANCED_FACE('',(#3138),#1270,.T.);
#25727=ADVANCED_FACE('',(#3139),#1271,.T.);
#25728=ADVANCED_FACE('',(#3140),#1272,.T.);
#25729=ADVANCED_FACE('',(#3141),#1273,.T.);
#25730=ADVANCED_FACE('',(#3142),#1274,.T.);
#25731=ADVANCED_FACE('',(#3143),#1275,.T.);
#25732=ADVANCED_FACE('',(#3144),#1276,.T.);
#25733=ADVANCED_FACE('',(#3145),#1277,.T.);
#25734=ADVANCED_FACE('',(#3146),#1278,.T.);
#25735=ADVANCED_FACE('',(#3147),#1279,.T.);
#25736=ADVANCED_FACE('',(#3148),#1280,.T.);
#25737=ADVANCED_FACE('',(#3149),#1281,.T.);
#25738=ADVANCED_FACE('',(#3150),#1282,.T.);
#25739=ADVANCED_FACE('',(#3151),#1283,.T.);
#25740=ADVANCED_FACE('',(#3152),#1284,.T.);
#25741=ADVANCED_FACE('',(#3153),#1285,.T.);
#25742=ADVANCED_FACE('',(#3154),#1286,.T.);
#25743=ADVANCED_FACE('',(#3155),#1287,.T.);
#25744=ADVANCED_FACE('',(#3156),#1288,.T.);
#25745=ADVANCED_FACE('',(#3157),#1289,.T.);
#25746=ADVANCED_FACE('',(#3158),#1290,.T.);
#25747=ADVANCED_FACE('',(#3159),#1291,.T.);
#25748=ADVANCED_FACE('',(#3160),#1292,.T.);
#25749=ADVANCED_FACE('',(#3161),#1293,.T.);
#25750=ADVANCED_FACE('',(#3162),#1294,.T.);
#25751=ADVANCED_FACE('',(#3163),#1295,.T.);
#25752=ADVANCED_FACE('',(#3164),#1296,.T.);
#25753=ADVANCED_FACE('',(#3165),#1297,.T.);
#25754=ADVANCED_FACE('',(#3166),#1298,.T.);
#25755=ADVANCED_FACE('',(#3167),#1944,.F.);
#25756=ADVANCED_FACE('',(#3168),#160,.F.);
#25757=ADVANCED_FACE('',(#3169),#1945,.T.);
#25758=ADVANCED_FACE('',(#3170),#1299,.T.);
#25759=ADVANCED_FACE('',(#3171),#161,.F.);
#25760=ADVANCED_FACE('',(#3172),#1086,.F.);
#25761=ADVANCED_FACE('',(#3173),#1300,.T.);
#25762=ADVANCED_FACE('',(#3174,#1635),#1946,.T.);
#25763=ADVANCED_FACE('',(#3175),#1947,.F.);
#25764=ADVANCED_FACE('',(#3176),#1948,.F.);
#25765=ADVANCED_FACE('',(#3177),#1949,.F.);
#25766=ADVANCED_FACE('',(#3178),#1950,.F.);
#25767=ADVANCED_FACE('',(#3179),#1951,.F.);
#25768=ADVANCED_FACE('',(#3180),#1952,.F.);
#25769=ADVANCED_FACE('',(#3181),#25055,.F.);
#25770=ADVANCED_FACE('',(#3182),#1953,.F.);
#25771=ADVANCED_FACE('',(#3183),#1954,.F.);
#25772=ADVANCED_FACE('',(#3184),#1955,.F.);
#25773=ADVANCED_FACE('',(#3185),#1956,.F.);
#25774=ADVANCED_FACE('',(#3186),#1957,.F.);
#25775=ADVANCED_FACE('',(#3187),#1958,.F.);
#25776=ADVANCED_FACE('',(#3188),#1959,.F.);
#25777=ADVANCED_FACE('',(#3189),#1960,.F.);
#25778=ADVANCED_FACE('',(#3190),#1961,.F.);
#25779=ADVANCED_FACE('',(#3191),#1962,.F.);
#25780=ADVANCED_FACE('',(#3192),#1963,.F.);
#25781=ADVANCED_FACE('',(#3193),#1964,.F.);
#25782=ADVANCED_FACE('',(#3194),#1965,.F.);
#25783=ADVANCED_FACE('',(#3195),#1966,.F.);
#25784=ADVANCED_FACE('',(#3196),#1967,.F.);
#25785=ADVANCED_FACE('',(#3197),#1968,.F.);
#25786=ADVANCED_FACE('',(#3198),#1969,.F.);
#25787=ADVANCED_FACE('',(#3199),#1970,.F.);
#25788=ADVANCED_FACE('',(#3200),#1971,.F.);
#25789=ADVANCED_FACE('',(#3201),#1972,.F.);
#25790=ADVANCED_FACE('',(#3202),#1973,.F.);
#25791=ADVANCED_FACE('',(#3203),#1974,.F.);
#25792=ADVANCED_FACE('',(#3204),#1975,.F.);
#25793=ADVANCED_FACE('',(#3205),#1976,.F.);
#25794=ADVANCED_FACE('',(#3206),#1977,.F.);
#25795=ADVANCED_FACE('',(#3207),#1978,.F.);
#25796=ADVANCED_FACE('',(#3208),#1979,.F.);
#25797=ADVANCED_FACE('',(#3209),#1980,.F.);
#25798=ADVANCED_FACE('',(#3210),#1981,.F.);
#25799=ADVANCED_FACE('',(#3211),#1982,.F.);
#25800=ADVANCED_FACE('',(#3212),#1983,.F.);
#25801=ADVANCED_FACE('',(#3213),#1984,.F.);
#25802=ADVANCED_FACE('',(#3214),#1985,.F.);
#25803=ADVANCED_FACE('',(#3215),#1986,.F.);
#25804=ADVANCED_FACE('',(#3216),#1987,.F.);
#25805=ADVANCED_FACE('',(#3217),#1988,.F.);
#25806=ADVANCED_FACE('',(#3218),#1989,.F.);
#25807=ADVANCED_FACE('',(#3219),#1990,.F.);
#25808=ADVANCED_FACE('',(#3220),#1991,.F.);
#25809=ADVANCED_FACE('',(#3221),#1992,.F.);
#25810=ADVANCED_FACE('',(#3222),#1993,.F.);
#25811=ADVANCED_FACE('',(#3223),#1994,.F.);
#25812=ADVANCED_FACE('',(#3224),#1995,.F.);
#25813=ADVANCED_FACE('',(#3225),#1996,.F.);
#25814=ADVANCED_FACE('',(#3226),#1997,.F.);
#25815=ADVANCED_FACE('',(#3227),#1998,.F.);
#25816=ADVANCED_FACE('',(#3228),#1999,.F.);
#25817=ADVANCED_FACE('',(#3229),#2000,.F.);
#25818=ADVANCED_FACE('',(#3230),#2001,.F.);
#25819=ADVANCED_FACE('',(#3231),#2002,.F.);
#25820=ADVANCED_FACE('',(#3232),#2003,.F.);
#25821=ADVANCED_FACE('',(#3233),#2004,.F.);
#25822=ADVANCED_FACE('',(#3234),#2005,.F.);
#25823=ADVANCED_FACE('',(#3235),#2006,.F.);
#25824=ADVANCED_FACE('',(#3236),#2007,.F.);
#25825=ADVANCED_FACE('',(#3237),#2008,.F.);
#25826=ADVANCED_FACE('',(#3238),#2009,.F.);
#25827=ADVANCED_FACE('',(#3239),#2010,.F.);
#25828=ADVANCED_FACE('',(#3240),#2011,.F.);
#25829=ADVANCED_FACE('',(#3241),#2012,.F.);
#25830=ADVANCED_FACE('',(#3242),#2013,.F.);
#25831=ADVANCED_FACE('',(#3243),#2014,.F.);
#25832=ADVANCED_FACE('',(#3244),#2015,.F.);
#25833=ADVANCED_FACE('',(#3245),#2016,.F.);
#25834=ADVANCED_FACE('',(#3246),#2017,.F.);
#25835=ADVANCED_FACE('',(#3247),#2018,.F.);
#25836=ADVANCED_FACE('',(#3248),#2019,.F.);
#25837=ADVANCED_FACE('',(#3249),#2020,.F.);
#25838=ADVANCED_FACE('',(#3250),#2021,.F.);
#25839=ADVANCED_FACE('',(#3251),#2022,.F.);
#25840=ADVANCED_FACE('',(#3252),#2023,.F.);
#25841=ADVANCED_FACE('',(#3253),#2024,.F.);
#25842=ADVANCED_FACE('',(#3254),#2025,.F.);
#25843=ADVANCED_FACE('',(#3255),#2026,.F.);
#25844=ADVANCED_FACE('',(#3256),#2027,.F.);
#25845=ADVANCED_FACE('',(#3257),#2028,.F.);
#25846=ADVANCED_FACE('',(#3258),#2029,.F.);
#25847=ADVANCED_FACE('',(#3259),#2030,.F.);
#25848=ADVANCED_FACE('',(#3260),#2031,.F.);
#25849=ADVANCED_FACE('',(#3261),#2032,.F.);
#25850=ADVANCED_FACE('',(#3262),#2033,.F.);
#25851=ADVANCED_FACE('',(#3263),#2034,.F.);
#25852=ADVANCED_FACE('',(#3264),#2035,.F.);
#25853=ADVANCED_FACE('',(#3265),#2036,.F.);
#25854=ADVANCED_FACE('',(#3266),#2037,.F.);
#25855=ADVANCED_FACE('',(#3267),#2038,.F.);
#25856=ADVANCED_FACE('',(#3268),#2039,.F.);
#25857=ADVANCED_FACE('',(#3269),#2040,.F.);
#25858=ADVANCED_FACE('',(#3270),#2041,.F.);
#25859=ADVANCED_FACE('',(#3271),#2042,.F.);
#25860=ADVANCED_FACE('',(#3272),#2043,.F.);
#25861=ADVANCED_FACE('',(#3273),#2044,.F.);
#25862=ADVANCED_FACE('',(#3274),#2045,.F.);
#25863=ADVANCED_FACE('',(#3275),#2046,.F.);
#25864=ADVANCED_FACE('',(#3276),#2047,.F.);
#25865=ADVANCED_FACE('',(#3277),#2048,.F.);
#25866=ADVANCED_FACE('',(#3278),#2049,.F.);
#25867=ADVANCED_FACE('',(#3279),#2050,.F.);
#25868=ADVANCED_FACE('',(#3280),#2051,.F.);
#25869=ADVANCED_FACE('',(#3281),#2052,.F.);
#25870=ADVANCED_FACE('',(#3282),#2053,.F.);
#25871=ADVANCED_FACE('',(#3283),#2054,.F.);
#25872=ADVANCED_FACE('',(#3284),#2055,.F.);
#25873=ADVANCED_FACE('',(#3285),#2056,.F.);
#25874=ADVANCED_FACE('',(#3286),#2057,.F.);
#25875=ADVANCED_FACE('',(#3287),#2058,.F.);
#25876=ADVANCED_FACE('',(#3288),#2059,.F.);
#25877=ADVANCED_FACE('',(#3289),#2060,.F.);
#25878=ADVANCED_FACE('',(#3290),#2061,.F.);
#25879=ADVANCED_FACE('',(#3291),#2062,.F.);
#25880=ADVANCED_FACE('',(#3292),#2063,.F.);
#25881=ADVANCED_FACE('',(#3293),#2064,.F.);
#25882=ADVANCED_FACE('',(#3294),#2065,.F.);
#25883=ADVANCED_FACE('',(#3295),#2066,.F.);
#25884=ADVANCED_FACE('',(#3296),#2067,.F.);
#25885=ADVANCED_FACE('',(#3297),#2068,.F.);
#25886=ADVANCED_FACE('',(#3298),#2069,.F.);
#25887=ADVANCED_FACE('',(#3299),#2070,.F.);
#25888=ADVANCED_FACE('',(#3300),#2071,.F.);
#25889=ADVANCED_FACE('',(#3301),#2072,.F.);
#25890=ADVANCED_FACE('',(#3302),#2073,.F.);
#25891=ADVANCED_FACE('',(#3303),#2074,.F.);
#25892=ADVANCED_FACE('',(#3304),#2075,.F.);
#25893=ADVANCED_FACE('',(#3305),#2076,.F.);
#25894=ADVANCED_FACE('',(#3306),#2077,.F.);
#25895=ADVANCED_FACE('',(#3307),#2078,.F.);
#25896=ADVANCED_FACE('',(#3308),#2079,.F.);
#25897=ADVANCED_FACE('',(#3309),#2080,.F.);
#25898=ADVANCED_FACE('',(#3310),#2081,.F.);
#25899=ADVANCED_FACE('',(#3311),#2082,.F.);
#25900=ADVANCED_FACE('',(#3312),#2083,.F.);
#25901=ADVANCED_FACE('',(#3313),#2084,.F.);
#25902=ADVANCED_FACE('',(#3314),#2085,.F.);
#25903=ADVANCED_FACE('',(#3315),#2086,.F.);
#25904=ADVANCED_FACE('',(#3316),#2087,.F.);
#25905=ADVANCED_FACE('',(#3317),#2088,.F.);
#25906=ADVANCED_FACE('',(#3318),#2089,.F.);
#25907=ADVANCED_FACE('',(#3319),#2090,.F.);
#25908=ADVANCED_FACE('',(#3320),#2091,.F.);
#25909=ADVANCED_FACE('',(#3321),#2092,.F.);
#25910=ADVANCED_FACE('',(#3322),#2093,.F.);
#25911=ADVANCED_FACE('',(#3323),#2094,.F.);
#25912=ADVANCED_FACE('',(#3324),#2095,.F.);
#25913=ADVANCED_FACE('',(#3325),#2096,.F.);
#25914=ADVANCED_FACE('',(#3326),#2097,.F.);
#25915=ADVANCED_FACE('',(#3327),#2098,.F.);
#25916=ADVANCED_FACE('',(#3328),#2099,.F.);
#25917=ADVANCED_FACE('',(#3329),#2100,.F.);
#25918=ADVANCED_FACE('',(#3330),#2101,.F.);
#25919=ADVANCED_FACE('',(#3331),#2102,.F.);
#25920=ADVANCED_FACE('',(#3332),#2103,.T.);
#25921=ADVANCED_FACE('',(#3333),#25056,.T.);
#25922=ADVANCED_FACE('',(#3334),#25057,.T.);
#25923=ADVANCED_FACE('',(#3335),#1301,.T.);
#25924=ADVANCED_FACE('',(#3336),#25058,.T.);
#25925=ADVANCED_FACE('',(#3337,#1636),#2104,.T.);
#26672=CLOSED_SHELL('',(#25724,#25725,#25726,#25727,#25728,#25729,#25730,
#25731,#25732,#25733,#25734,#25735,#25736,#25737,#25738,#25739,#25740,#25741,
#25742,#25743,#25744,#25745,#25746,#25747,#25748,#25749,#25750,#25751,#25752,
#25753,#25754,#25755,#25756,#25757,#25758,#25759,#25760,#25761,#25762,#25763,
#25764,#25765,#25766,#25767,#25768,#25769,#25770,#25771,#25772,#25773,#25774,
#25775,#25776,#25777,#25778,#25779,#25780,#25781,#25782,#25783,#25784,#25785,
#25786,#25787,#25788,#25789,#25790,#25791,#25792,#25793,#25794,#25795,#25796,
#25797,#25798,#25799,#25800,#25801,#25802,#25803,#25804,#25805,#25806,#25807,
#25808,#25809,#25810,#25811,#25812,#25813,#25814,#25815,#25816,#25817,#25818,
#25819,#25820,#25821,#25822,#25823,#25824,#25825,#25826,#25827,#25828,#25829,
#25830,#25831,#25832,#25833,#25834,#25835,#25836,#25837,#25838,#25839,#25840,
#25841,#25842,#25843,#25844,#25845,#25846,#25847,#25848,#25849,#25850,#25851,
#25852,#25853,#25854,#25855,#25856,#25857,#25858,#25859,#25860,#25861,#25862,
#25863,#25864,#25865,#25866,#25867,#25868,#25869,#25870,#25871,#25872,#25873,
#25874,#25875,#25876,#25877,#25878,#25879,#25880,#25881,#25882,#25883,#25884,
#25885,#25886,#25887,#25888,#25889,#25890,#25891,#25892,#25893,#25894,#25895,
#25896,#25897,#25898,#25899,#25900,#25901,#25902,#25903,#25904,#25905,#25906,
#25907,#25908,#25909,#25910,#25911,#25912,#25913,#25914,#25915,#25916,#25917,
#25918,#25919,#25920,#25921,#25922,#25923,#25924,#25925));
#27875=AXIS2_PLACEMENT_3D('',#50311,#32149,#32150);
#27876=AXIS2_PLACEMENT_3D('',#50312,#32151,#32152);
#27877=AXIS2_PLACEMENT_3D('',#50328,#32154,#32155);
#27878=AXIS2_PLACEMENT_3D('',#50336,#32156,#32157);
#27879=AXIS2_PLACEMENT_3D('',#50384,#32159,#32160);
#27880=AXIS2_PLACEMENT_3D('',#50432,#32162,#32163);
#27881=AXIS2_PLACEMENT_3D('',#50486,#32165,#32166);
#27882=AXIS2_PLACEMENT_3D('',#50534,#32168,#32169);
#27883=AXIS2_PLACEMENT_3D('',#50582,#32171,#32172);
#27884=AXIS2_PLACEMENT_3D('',#50636,#32174,#32175);
#27885=AXIS2_PLACEMENT_3D('',#50684,#32177,#32178);
#27886=AXIS2_PLACEMENT_3D('',#50732,#32180,#32181);
#27887=AXIS2_PLACEMENT_3D('',#50786,#32183,#32184);
#27888=AXIS2_PLACEMENT_3D('',#50834,#32186,#32187);
#27889=AXIS2_PLACEMENT_3D('',#50882,#32189,#32190);
#27890=AXIS2_PLACEMENT_3D('',#50936,#32192,#32193);
#27891=AXIS2_PLACEMENT_3D('',#50984,#32195,#32196);
#27892=AXIS2_PLACEMENT_3D('',#51032,#32198,#32199);
#27893=AXIS2_PLACEMENT_3D('',#51086,#32201,#32202);
#27894=AXIS2_PLACEMENT_3D('',#51101,#32204,#32205);
#27895=AXIS2_PLACEMENT_3D('',#51109,#32206,#32207);
#27896=AXIS2_PLACEMENT_3D('',#51134,#32209,#32210);
#27897=AXIS2_PLACEMENT_3D('',#51158,#32212,#32213);
#27898=AXIS2_PLACEMENT_3D('',#51183,#32215,#32216);
#27899=AXIS2_PLACEMENT_3D('',#51208,#32218,#32219);
#27900=AXIS2_PLACEMENT_3D('',#51232,#32221,#32222);
#27901=AXIS2_PLACEMENT_3D('',#51257,#32224,#32225);
#27902=AXIS2_PLACEMENT_3D('',#51282,#32227,#32228);
#27903=AXIS2_PLACEMENT_3D('',#51306,#32230,#32231);
#27904=AXIS2_PLACEMENT_3D('',#51331,#32233,#32234);
#27905=AXIS2_PLACEMENT_3D('',#51356,#32236,#32237);
#27906=AXIS2_PLACEMENT_3D('',#51380,#32239,#32240);
#27907=AXIS2_PLACEMENT_3D('',#51405,#32242,#32243);
#27908=AXIS2_PLACEMENT_3D('',#51430,#32245,#32246);
#27909=AXIS2_PLACEMENT_3D('',#51454,#32248,#32249);
#27910=AXIS2_PLACEMENT_3D('',#51518,#32250,#32251);
#27911=AXIS2_PLACEMENT_3D('',#51520,#32252,#32253);
#27912=AXIS2_PLACEMENT_3D('',#52072,#32254,#32255);
#27913=AXIS2_PLACEMENT_3D('',#52074,#32256,#32257);
#27914=AXIS2_PLACEMENT_3D('',#52075,#32258,#32259);
#27915=AXIS2_PLACEMENT_3D('',#52138,#32260,#32261);
#27916=AXIS2_PLACEMENT_3D('',#52139,#32262,#32263);
#27917=AXIS2_PLACEMENT_3D('',#52564,#32264,#32265);
#27918=AXIS2_PLACEMENT_3D('',#52566,#32266,#32267);
#27919=AXIS2_PLACEMENT_3D('',#52567,#32268,#32269);
#27920=AXIS2_PLACEMENT_3D('',#52568,#32270,#32271);
#27921=AXIS2_PLACEMENT_3D('',#52569,#32272,#32273);
#27922=AXIS2_PLACEMENT_3D('',#52570,#32274,#32275);
#27923=AXIS2_PLACEMENT_3D('',#52572,#32276,#32277);
#27924=AXIS2_PLACEMENT_3D('',#52573,#32278,#32279);
#27925=AXIS2_PLACEMENT_3D('',#52577,#32281,#32282);
#27926=AXIS2_PLACEMENT_3D('',#52578,#32283,#32284);
#27927=AXIS2_PLACEMENT_3D('',#52581,#32286,#32287);
#27928=AXIS2_PLACEMENT_3D('',#52582,#32288,#32289);
#27929=AXIS2_PLACEMENT_3D('',#52585,#32291,#32292);
#27930=AXIS2_PLACEMENT_3D('',#52586,#32293,#32294);
#27931=AXIS2_PLACEMENT_3D('',#52589,#32296,#32297);
#27932=AXIS2_PLACEMENT_3D('',#52590,#32298,#32299);
#27933=AXIS2_PLACEMENT_3D('',#52593,#32301,#32302);
#27934=AXIS2_PLACEMENT_3D('',#52594,#32303,#32304);
#27935=AXIS2_PLACEMENT_3D('',#52596,#32306,#32307);
#27936=AXIS2_PLACEMENT_3D('',#52597,#32308,#32309);
#27937=AXIS2_PLACEMENT_3D('',#52600,#32311,#32312);
#27938=AXIS2_PLACEMENT_3D('',#52606,#32316,#32317);
#27939=AXIS2_PLACEMENT_3D('',#52610,#32320,#32321);
#27940=AXIS2_PLACEMENT_3D('',#52614,#32324,#32325);
#27941=AXIS2_PLACEMENT_3D('',#52618,#32328,#32329);
#27942=AXIS2_PLACEMENT_3D('',#52622,#32332,#32333);
#27943=AXIS2_PLACEMENT_3D('',#52624,#32335,#32336);
#27944=AXIS2_PLACEMENT_3D('',#52633,#32341,#32342);
#27945=AXIS2_PLACEMENT_3D('',#52635,#32343,#32344);
#27946=AXIS2_PLACEMENT_3D('',#52637,#32346,#32347);
#27947=AXIS2_PLACEMENT_3D('',#52641,#32350,#32351);
#27948=AXIS2_PLACEMENT_3D('',#52642,#32352,#32353);
#27949=AXIS2_PLACEMENT_3D('',#52643,#32354,#32355);
#27950=AXIS2_PLACEMENT_3D('',#52652,#32360,#32361);
#27951=AXIS2_PLACEMENT_3D('',#52654,#32362,#32363);
#27952=AXIS2_PLACEMENT_3D('',#52656,#32365,#32366);
#27953=AXIS2_PLACEMENT_3D('',#52660,#32369,#32370);
#27954=AXIS2_PLACEMENT_3D('',#52661,#32371,#32372);
#27955=AXIS2_PLACEMENT_3D('',#52662,#32373,#32374);
#27956=AXIS2_PLACEMENT_3D('',#52671,#32379,#32380);
#27957=AXIS2_PLACEMENT_3D('',#52673,#32381,#32382);
#27958=AXIS2_PLACEMENT_3D('',#52675,#32384,#32385);
#27959=AXIS2_PLACEMENT_3D('',#52679,#32388,#32389);
#27960=AXIS2_PLACEMENT_3D('',#52680,#32390,#32391);
#27961=AXIS2_PLACEMENT_3D('',#52681,#32392,#32393);
#27962=AXIS2_PLACEMENT_3D('',#52690,#32398,#32399);
#27963=AXIS2_PLACEMENT_3D('',#52692,#32400,#32401);
#27964=AXIS2_PLACEMENT_3D('',#52694,#32403,#32404);
#27965=AXIS2_PLACEMENT_3D('',#52698,#32407,#32408);
#27966=AXIS2_PLACEMENT_3D('',#52699,#32409,#32410);
#27967=AXIS2_PLACEMENT_3D('',#52700,#32411,#32412);
#27968=AXIS2_PLACEMENT_3D('',#52709,#32417,#32418);
#27969=AXIS2_PLACEMENT_3D('',#52711,#32419,#32420);
#27970=AXIS2_PLACEMENT_3D('',#52713,#32422,#32423);
#27971=AXIS2_PLACEMENT_3D('',#52717,#32426,#32427);
#27972=AXIS2_PLACEMENT_3D('',#52718,#32428,#32429);
#27973=AXIS2_PLACEMENT_3D('',#52719,#32430,#32431);
#27974=AXIS2_PLACEMENT_3D('',#52728,#32436,#32437);
#27975=AXIS2_PLACEMENT_3D('',#52730,#32438,#32439);
#27976=AXIS2_PLACEMENT_3D('',#52732,#32441,#32442);
#27977=AXIS2_PLACEMENT_3D('',#52736,#32445,#32446);
#27978=AXIS2_PLACEMENT_3D('',#52737,#32447,#32448);
#27979=AXIS2_PLACEMENT_3D('',#52738,#32449,#32450);
#27980=AXIS2_PLACEMENT_3D('',#52747,#32455,#32456);
#27981=AXIS2_PLACEMENT_3D('',#52749,#32457,#32458);
#27982=AXIS2_PLACEMENT_3D('',#52751,#32460,#32461);
#27983=AXIS2_PLACEMENT_3D('',#52755,#32464,#32465);
#27984=AXIS2_PLACEMENT_3D('',#52756,#32466,#32467);
#27985=AXIS2_PLACEMENT_3D('',#52757,#32468,#32469);
#27986=AXIS2_PLACEMENT_3D('',#52766,#32474,#32475);
#27987=AXIS2_PLACEMENT_3D('',#52768,#32476,#32477);
#27988=AXIS2_PLACEMENT_3D('',#52770,#32479,#32480);
#27989=AXIS2_PLACEMENT_3D('',#52774,#32483,#32484);
#27990=AXIS2_PLACEMENT_3D('',#52775,#32485,#32486);
#27991=AXIS2_PLACEMENT_3D('',#52776,#32487,#32488);
#27992=AXIS2_PLACEMENT_3D('',#52785,#32493,#32494);
#27993=AXIS2_PLACEMENT_3D('',#52787,#32495,#32496);
#27994=AXIS2_PLACEMENT_3D('',#52790,#32498,#32499);
#27995=AXIS2_PLACEMENT_3D('',#52791,#32500,#32501);
#27996=AXIS2_PLACEMENT_3D('',#52795,#32504,#32505);
#27997=AXIS2_PLACEMENT_3D('',#52797,#32506,#32507);
#27998=AXIS2_PLACEMENT_3D('',#52798,#32508,#32509);
#27999=AXIS2_PLACEMENT_3D('',#52799,#32510,#32511);
#28000=AXIS2_PLACEMENT_3D('',#52808,#32516,#32517);
#28001=AXIS2_PLACEMENT_3D('',#52810,#32518,#32519);
#28002=AXIS2_PLACEMENT_3D('',#52812,#32521,#32522);
#28003=AXIS2_PLACEMENT_3D('',#52816,#32525,#32526);
#28004=AXIS2_PLACEMENT_3D('',#52817,#32527,#32528);
#28005=AXIS2_PLACEMENT_3D('',#52818,#32529,#32530);
#28006=AXIS2_PLACEMENT_3D('',#52827,#32535,#32536);
#28007=AXIS2_PLACEMENT_3D('',#52829,#32537,#32538);
#28008=AXIS2_PLACEMENT_3D('',#52831,#32540,#32541);
#28009=AXIS2_PLACEMENT_3D('',#52835,#32544,#32545);
#28010=AXIS2_PLACEMENT_3D('',#52836,#32546,#32547);
#28011=AXIS2_PLACEMENT_3D('',#52837,#32548,#32549);
#28012=AXIS2_PLACEMENT_3D('',#52846,#32554,#32555);
#28013=AXIS2_PLACEMENT_3D('',#52848,#32556,#32557);
#28014=AXIS2_PLACEMENT_3D('',#52850,#32559,#32560);
#28015=AXIS2_PLACEMENT_3D('',#52854,#32563,#32564);
#28016=AXIS2_PLACEMENT_3D('',#52855,#32565,#32566);
#28017=AXIS2_PLACEMENT_3D('',#52856,#32567,#32568);
#28018=AXIS2_PLACEMENT_3D('',#52865,#32573,#32574);
#28019=AXIS2_PLACEMENT_3D('',#52867,#32575,#32576);
#28020=AXIS2_PLACEMENT_3D('',#52869,#32578,#32579);
#28021=AXIS2_PLACEMENT_3D('',#52873,#32582,#32583);
#28022=AXIS2_PLACEMENT_3D('',#52874,#32584,#32585);
#28023=AXIS2_PLACEMENT_3D('',#52875,#32586,#32587);
#28024=AXIS2_PLACEMENT_3D('',#52884,#32592,#32593);
#28025=AXIS2_PLACEMENT_3D('',#52886,#32594,#32595);
#28026=AXIS2_PLACEMENT_3D('',#52888,#32597,#32598);
#28027=AXIS2_PLACEMENT_3D('',#52892,#32601,#32602);
#28028=AXIS2_PLACEMENT_3D('',#52893,#32603,#32604);
#28029=AXIS2_PLACEMENT_3D('',#52894,#32605,#32606);
#28030=AXIS2_PLACEMENT_3D('',#52903,#32611,#32612);
#28031=AXIS2_PLACEMENT_3D('',#52905,#32613,#32614);
#28032=AXIS2_PLACEMENT_3D('',#52907,#32616,#32617);
#28033=AXIS2_PLACEMENT_3D('',#52911,#32620,#32621);
#28034=AXIS2_PLACEMENT_3D('',#52912,#32622,#32623);
#28035=AXIS2_PLACEMENT_3D('',#52913,#32624,#32625);
#28036=AXIS2_PLACEMENT_3D('',#52922,#32630,#32631);
#28037=AXIS2_PLACEMENT_3D('',#52924,#32632,#32633);
#28038=AXIS2_PLACEMENT_3D('',#52926,#32635,#32636);
#28039=AXIS2_PLACEMENT_3D('',#52930,#32639,#32640);
#28040=AXIS2_PLACEMENT_3D('',#52931,#32641,#32642);
#28041=AXIS2_PLACEMENT_3D('',#52932,#32643,#32644);
#28042=AXIS2_PLACEMENT_3D('',#52941,#32649,#32650);
#28043=AXIS2_PLACEMENT_3D('',#52943,#32651,#32652);
#28044=AXIS2_PLACEMENT_3D('',#52945,#32654,#32655);
#28045=AXIS2_PLACEMENT_3D('',#52949,#32658,#32659);
#28046=AXIS2_PLACEMENT_3D('',#52950,#32660,#32661);
#28047=AXIS2_PLACEMENT_3D('',#52951,#32662,#32663);
#28048=AXIS2_PLACEMENT_3D('',#52960,#32668,#32669);
#28049=AXIS2_PLACEMENT_3D('',#52962,#32670,#32671);
#28050=AXIS2_PLACEMENT_3D('',#52964,#32673,#32674);
#28051=AXIS2_PLACEMENT_3D('',#52968,#32677,#32678);
#28052=AXIS2_PLACEMENT_3D('',#52969,#32679,#32680);
#28053=AXIS2_PLACEMENT_3D('',#52970,#32681,#32682);
#28054=AXIS2_PLACEMENT_3D('',#52979,#32687,#32688);
#28055=AXIS2_PLACEMENT_3D('',#52981,#32689,#32690);
#28056=AXIS2_PLACEMENT_3D('',#52983,#32692,#32693);
#28057=AXIS2_PLACEMENT_3D('',#52987,#32696,#32697);
#28058=AXIS2_PLACEMENT_3D('',#52988,#32698,#32699);
#28059=AXIS2_PLACEMENT_3D('',#52989,#32700,#32701);
#28060=AXIS2_PLACEMENT_3D('',#52998,#32706,#32707);
#28061=AXIS2_PLACEMENT_3D('',#53000,#32708,#32709);
#28062=AXIS2_PLACEMENT_3D('',#53002,#32711,#32712);
#28063=AXIS2_PLACEMENT_3D('',#53006,#32715,#32716);
#28064=AXIS2_PLACEMENT_3D('',#53007,#32717,#32718);
#28065=AXIS2_PLACEMENT_3D('',#53008,#32719,#32720);
#28066=AXIS2_PLACEMENT_3D('',#53017,#32725,#32726);
#28067=AXIS2_PLACEMENT_3D('',#53019,#32727,#32728);
#28068=AXIS2_PLACEMENT_3D('',#53021,#32730,#32731);
#28069=AXIS2_PLACEMENT_3D('',#53025,#32734,#32735);
#28070=AXIS2_PLACEMENT_3D('',#53026,#32736,#32737);
#28071=AXIS2_PLACEMENT_3D('',#53027,#32738,#32739);
#28072=AXIS2_PLACEMENT_3D('',#53036,#32744,#32745);
#28073=AXIS2_PLACEMENT_3D('',#53038,#32746,#32747);
#28074=AXIS2_PLACEMENT_3D('',#53040,#32749,#32750);
#28075=AXIS2_PLACEMENT_3D('',#53044,#32753,#32754);
#28076=AXIS2_PLACEMENT_3D('',#53045,#32755,#32756);
#28077=AXIS2_PLACEMENT_3D('',#53046,#32757,#32758);
#28078=AXIS2_PLACEMENT_3D('',#53055,#32763,#32764);
#28079=AXIS2_PLACEMENT_3D('',#53057,#32765,#32766);
#28080=AXIS2_PLACEMENT_3D('',#53059,#32768,#32769);
#28081=AXIS2_PLACEMENT_3D('',#53063,#32772,#32773);
#28082=AXIS2_PLACEMENT_3D('',#53064,#32774,#32775);
#28083=AXIS2_PLACEMENT_3D('',#53065,#32776,#32777);
#28084=AXIS2_PLACEMENT_3D('',#53074,#32782,#32783);
#28085=AXIS2_PLACEMENT_3D('',#53076,#32784,#32785);
#28086=AXIS2_PLACEMENT_3D('',#53078,#32787,#32788);
#28087=AXIS2_PLACEMENT_3D('',#53082,#32791,#32792);
#28088=AXIS2_PLACEMENT_3D('',#53083,#32793,#32794);
#28089=AXIS2_PLACEMENT_3D('',#53084,#32795,#32796);
#28090=AXIS2_PLACEMENT_3D('',#53093,#32801,#32802);
#28091=AXIS2_PLACEMENT_3D('',#53095,#32803,#32804);
#28092=AXIS2_PLACEMENT_3D('',#53097,#32806,#32807);
#28093=AXIS2_PLACEMENT_3D('',#53101,#32810,#32811);
#28094=AXIS2_PLACEMENT_3D('',#53102,#32812,#32813);
#28095=AXIS2_PLACEMENT_3D('',#53103,#32814,#32815);
#28096=AXIS2_PLACEMENT_3D('',#53112,#32820,#32821);
#28097=AXIS2_PLACEMENT_3D('',#53114,#32822,#32823);
#28098=AXIS2_PLACEMENT_3D('',#53116,#32825,#32826);
#28099=AXIS2_PLACEMENT_3D('',#53120,#32829,#32830);
#28100=AXIS2_PLACEMENT_3D('',#53121,#32831,#32832);
#28101=AXIS2_PLACEMENT_3D('',#53122,#32833,#32834);
#28102=AXIS2_PLACEMENT_3D('',#53125,#32835,#32836);
#28103=AXIS2_PLACEMENT_3D('',#53129,#32839,#32840);
#28104=AXIS2_PLACEMENT_3D('',#53135,#32844,#32845);
#28105=AXIS2_PLACEMENT_3D('',#53139,#32848,#32849);
#28106=AXIS2_PLACEMENT_3D('',#53140,#32850,#32851);
#28107=AXIS2_PLACEMENT_3D('',#53141,#32852,#32853);
#28108=AXIS2_PLACEMENT_3D('',#53150,#32858,#32859);
#28109=AXIS2_PLACEMENT_3D('',#53152,#32860,#32861);
#28110=AXIS2_PLACEMENT_3D('',#53154,#32863,#32864);
#28111=AXIS2_PLACEMENT_3D('',#53158,#32867,#32868);
#28112=AXIS2_PLACEMENT_3D('',#53159,#32869,#32870);
#28113=AXIS2_PLACEMENT_3D('',#53160,#32871,#32872);
#28114=AXIS2_PLACEMENT_3D('',#53169,#32877,#32878);
#28115=AXIS2_PLACEMENT_3D('',#53171,#32879,#32880);
#28116=AXIS2_PLACEMENT_3D('',#53173,#32882,#32883);
#28117=AXIS2_PLACEMENT_3D('',#53177,#32886,#32887);
#28118=AXIS2_PLACEMENT_3D('',#53178,#32888,#32889);
#28119=AXIS2_PLACEMENT_3D('',#53179,#32890,#32891);
#28120=AXIS2_PLACEMENT_3D('',#53188,#32896,#32897);
#28121=AXIS2_PLACEMENT_3D('',#53190,#32898,#32899);
#28122=AXIS2_PLACEMENT_3D('',#53192,#32901,#32902);
#28123=AXIS2_PLACEMENT_3D('',#53196,#32905,#32906);
#28124=AXIS2_PLACEMENT_3D('',#53197,#32907,#32908);
#28125=AXIS2_PLACEMENT_3D('',#53198,#32909,#32910);
#28126=AXIS2_PLACEMENT_3D('',#53207,#32915,#32916);
#28127=AXIS2_PLACEMENT_3D('',#53209,#32917,#32918);
#28128=AXIS2_PLACEMENT_3D('',#53211,#32920,#32921);
#28129=AXIS2_PLACEMENT_3D('',#53215,#32924,#32925);
#28130=AXIS2_PLACEMENT_3D('',#53216,#32926,#32927);
#28131=AXIS2_PLACEMENT_3D('',#53217,#32928,#32929);
#28132=AXIS2_PLACEMENT_3D('',#53226,#32934,#32935);
#28133=AXIS2_PLACEMENT_3D('',#53228,#32936,#32937);
#28134=AXIS2_PLACEMENT_3D('',#53230,#32939,#32940);
#28135=AXIS2_PLACEMENT_3D('',#53234,#32943,#32944);
#28136=AXIS2_PLACEMENT_3D('',#53235,#32945,#32946);
#28137=AXIS2_PLACEMENT_3D('',#53236,#32947,#32948);
#28138=AXIS2_PLACEMENT_3D('',#53245,#32953,#32954);
#28139=AXIS2_PLACEMENT_3D('',#53247,#32955,#32956);
#28140=AXIS2_PLACEMENT_3D('',#53249,#32958,#32959);
#28141=AXIS2_PLACEMENT_3D('',#53253,#32962,#32963);
#28142=AXIS2_PLACEMENT_3D('',#53254,#32964,#32965);
#28143=AXIS2_PLACEMENT_3D('',#53255,#32966,#32967);
#28144=AXIS2_PLACEMENT_3D('',#53264,#32972,#32973);
#28145=AXIS2_PLACEMENT_3D('',#53266,#32974,#32975);
#28146=AXIS2_PLACEMENT_3D('',#53268,#32977,#32978);
#28147=AXIS2_PLACEMENT_3D('',#53272,#32981,#32982);
#28148=AXIS2_PLACEMENT_3D('',#53273,#32983,#32984);
#28149=AXIS2_PLACEMENT_3D('',#53274,#32985,#32986);
#28150=AXIS2_PLACEMENT_3D('',#53283,#32991,#32992);
#28151=AXIS2_PLACEMENT_3D('',#53285,#32993,#32994);
#28152=AXIS2_PLACEMENT_3D('',#53287,#32996,#32997);
#28153=AXIS2_PLACEMENT_3D('',#53291,#33000,#33001);
#28154=AXIS2_PLACEMENT_3D('',#53292,#33002,#33003);
#28155=AXIS2_PLACEMENT_3D('',#53293,#33004,#33005);
#28156=AXIS2_PLACEMENT_3D('',#53302,#33010,#33011);
#28157=AXIS2_PLACEMENT_3D('',#53304,#33012,#33013);
#28158=AXIS2_PLACEMENT_3D('',#53306,#33015,#33016);
#28159=AXIS2_PLACEMENT_3D('',#53310,#33019,#33020);
#28160=AXIS2_PLACEMENT_3D('',#53311,#33021,#33022);
#28161=AXIS2_PLACEMENT_3D('',#53312,#33023,#33024);
#28162=AXIS2_PLACEMENT_3D('',#53314,#33025,#33026);
#28163=AXIS2_PLACEMENT_3D('',#53315,#33027,#33028);
#28164=AXIS2_PLACEMENT_3D('',#53317,#33030,#33031);
#28165=AXIS2_PLACEMENT_3D('',#53319,#33032,#33033);
#28166=AXIS2_PLACEMENT_3D('',#53321,#33035,#33036);
#28167=AXIS2_PLACEMENT_3D('',#53322,#33037,#33038);
#28168=AXIS2_PLACEMENT_3D('',#53323,#33039,#33040);
#28169=AXIS2_PLACEMENT_3D('',#53324,#33041,#33042);
#28170=AXIS2_PLACEMENT_3D('',#53325,#33043,#33044);
#28171=AXIS2_PLACEMENT_3D('',#53326,#33045,#33046);
#28172=AXIS2_PLACEMENT_3D('',#53327,#33047,#33048);
#28173=AXIS2_PLACEMENT_3D('',#53328,#33049,#33050);
#28174=AXIS2_PLACEMENT_3D('',#53329,#33051,#33052);
#28175=AXIS2_PLACEMENT_3D('',#53330,#33053,#33054);
#28176=AXIS2_PLACEMENT_3D('',#53331,#33055,#33056);
#28177=AXIS2_PLACEMENT_3D('',#53332,#33057,#33058);
#28178=AXIS2_PLACEMENT_3D('',#53333,#33059,#33060);
#28179=AXIS2_PLACEMENT_3D('',#53334,#33061,#33062);
#28180=AXIS2_PLACEMENT_3D('',#53335,#33063,#33064);
#28181=AXIS2_PLACEMENT_3D('',#53336,#33065,#33066);
#28182=AXIS2_PLACEMENT_3D('',#53337,#33067,#33068);
#28183=AXIS2_PLACEMENT_3D('',#53339,#33070,#33071);
#28184=AXIS2_PLACEMENT_3D('',#53340,#33072,#33073);
#28185=AXIS2_PLACEMENT_3D('',#53341,#33074,#33075);
#28186=AXIS2_PLACEMENT_3D('',#53342,#33076,#33077);
#28187=AXIS2_PLACEMENT_3D('',#53343,#33078,#33079);
#28188=AXIS2_PLACEMENT_3D('',#53344,#33080,#33081);
#28189=AXIS2_PLACEMENT_3D('',#53345,#33082,#33083);
#28190=AXIS2_PLACEMENT_3D('',#53346,#33084,#33085);
#28191=AXIS2_PLACEMENT_3D('',#53347,#33086,#33087);
#28192=AXIS2_PLACEMENT_3D('',#53348,#33088,#33089);
#28193=AXIS2_PLACEMENT_3D('',#53349,#33090,#33091);
#28194=AXIS2_PLACEMENT_3D('',#53350,#33092,#33093);
#28195=AXIS2_PLACEMENT_3D('',#53351,#33094,#33095);
#28196=AXIS2_PLACEMENT_3D('',#53352,#33096,#33097);
#28197=AXIS2_PLACEMENT_3D('',#53353,#33098,#33099);
#28198=AXIS2_PLACEMENT_3D('',#53354,#33100,#33101);
#28199=AXIS2_PLACEMENT_3D('',#53355,#33102,#33103);
#28200=AXIS2_PLACEMENT_3D('',#53356,#33104,#33105);
#28201=AXIS2_PLACEMENT_3D('',#53357,#33106,#33107);
#28202=AXIS2_PLACEMENT_3D('',#53358,#33108,#33109);
#28203=AXIS2_PLACEMENT_3D('',#53359,#33110,#33111);
#28204=AXIS2_PLACEMENT_3D('',#53361,#33112,#33113);
#28205=AXIS2_PLACEMENT_3D('',#53363,#33115,#33116);
#32149=DIRECTION('axis',(0.,0.,1.));
#32150=DIRECTION('refdir',(1.,0.,0.));
#32151=DIRECTION('center_axis',(0.,0.,1.));
#32152=DIRECTION('ref_axis',(1.,0.,0.));
#32153=DIRECTION('',(0.,0.,-1.));
#32154=DIRECTION('center_axis',(0.,0.,1.));
#32155=DIRECTION('ref_axis',(1.,0.,0.));
#32156=DIRECTION('center_axis',(0.,0.,1.));
#32157=DIRECTION('ref_axis',(1.,0.,0.));
#32158=DIRECTION('',(0.,0.,-1.));
#32159=DIRECTION('center_axis',(0.,0.,1.));
#32160=DIRECTION('ref_axis',(1.,0.,0.));
#32161=DIRECTION('',(0.,0.,-1.));
#32162=DIRECTION('center_axis',(0.,0.,1.));
#32163=DIRECTION('ref_axis',(1.,0.,0.));
#32164=DIRECTION('',(0.,0.,-1.));
#32165=DIRECTION('center_axis',(0.,0.,1.));
#32166=DIRECTION('ref_axis',(1.,0.,0.));
#32167=DIRECTION('',(0.,0.,-1.));
#32168=DIRECTION('center_axis',(0.,0.,1.));
#32169=DIRECTION('ref_axis',(1.,0.,0.));
#32170=DIRECTION('',(0.,0.,-1.));
#32171=DIRECTION('center_axis',(0.,0.,1.));
#32172=DIRECTION('ref_axis',(1.,0.,0.));
#32173=DIRECTION('',(0.,0.,-1.));
#32174=DIRECTION('center_axis',(0.,0.,1.));
#32175=DIRECTION('ref_axis',(1.,0.,0.));
#32176=DIRECTION('',(0.,0.,-1.));
#32177=DIRECTION('center_axis',(0.,0.,1.));
#32178=DIRECTION('ref_axis',(1.,0.,0.));
#32179=DIRECTION('',(0.,0.,-1.));
#32180=DIRECTION('center_axis',(0.,0.,1.));
#32181=DIRECTION('ref_axis',(1.,0.,0.));
#32182=DIRECTION('',(0.,0.,-1.));
#32183=DIRECTION('center_axis',(0.,0.,1.));
#32184=DIRECTION('ref_axis',(1.,0.,0.));
#32185=DIRECTION('',(0.,0.,-1.));
#32186=DIRECTION('center_axis',(0.,0.,1.));
#32187=DIRECTION('ref_axis',(1.,0.,0.));
#32188=DIRECTION('',(0.,0.,-1.));
#32189=DIRECTION('center_axis',(0.,0.,1.));
#32190=DIRECTION('ref_axis',(1.,0.,0.));
#32191=DIRECTION('',(0.,0.,-1.));
#32192=DIRECTION('center_axis',(0.,0.,1.));
#32193=DIRECTION('ref_axis',(1.,0.,0.));
#32194=DIRECTION('',(0.,0.,-1.));
#32195=DIRECTION('center_axis',(0.,0.,1.));
#32196=DIRECTION('ref_axis',(1.,0.,0.));
#32197=DIRECTION('',(0.,0.,-1.));
#32198=DIRECTION('center_axis',(0.,0.,1.));
#32199=DIRECTION('ref_axis',(1.,0.,0.));
#32200=DIRECTION('',(0.,0.,-1.));
#32201=DIRECTION('center_axis',(0.,0.,1.));
#32202=DIRECTION('ref_axis',(0.812982922164426,-0.582287530580031,0.));
#32203=DIRECTION('',(0.,0.,1.));
#32204=DIRECTION('center_axis',(0.,0.,1.));
#32205=DIRECTION('ref_axis',(1.,9.56839379238543E-14,0.));
#32206=DIRECTION('center_axis',(0.,0.,1.));
#32207=DIRECTION('ref_axis',(1.,9.56839379238543E-14,0.));
#32208=DIRECTION('',(0.,0.,1.));
#32209=DIRECTION('center_axis',(0.,0.,1.));
#32210=DIRECTION('ref_axis',(1.,9.56839379238543E-14,0.));
#32211=DIRECTION('',(0.,0.,1.));
#32212=DIRECTION('center_axis',(0.,0.,1.));
#32213=DIRECTION('ref_axis',(1.,9.56839379238543E-14,0.));
#32214=DIRECTION('',(0.,0.,1.));
#32215=DIRECTION('center_axis',(0.,0.,1.));
#32216=DIRECTION('ref_axis',(1.,9.56839379238543E-14,0.));
#32217=DIRECTION('',(0.,0.,1.));
#32218=DIRECTION('center_axis',(0.,0.,1.));
#32219=DIRECTION('ref_axis',(1.,9.56839379238543E-14,0.));
#32220=DIRECTION('',(0.,0.,1.));
#32221=DIRECTION('center_axis',(0.,0.,1.));
#32222=DIRECTION('ref_axis',(1.,9.56839379238543E-14,0.));
#32223=DIRECTION('',(0.,0.,1.));
#32224=DIRECTION('center_axis',(0.,0.,1.));
#32225=DIRECTION('ref_axis',(1.,9.56839379238543E-14,0.));
#32226=DIRECTION('',(0.,0.,1.));
#32227=DIRECTION('center_axis',(0.,0.,1.));
#32228=DIRECTION('ref_axis',(1.,9.56839379238543E-14,0.));
#32229=DIRECTION('',(0.,0.,1.));
#32230=DIRECTION('center_axis',(0.,0.,1.));
#32231=DIRECTION('ref_axis',(1.,9.56839379238543E-14,0.));
#32232=DIRECTION('',(0.,0.,1.));
#32233=DIRECTION('center_axis',(0.,0.,1.));
#32234=DIRECTION('ref_axis',(1.,9.56839379238543E-14,0.));
#32235=DIRECTION('',(0.,0.,1.));
#32236=DIRECTION('center_axis',(0.,0.,1.));
#32237=DIRECTION('ref_axis',(1.,9.56839379238543E-14,0.));
#32238=DIRECTION('',(0.,0.,1.));
#32239=DIRECTION('center_axis',(0.,0.,1.));
#32240=DIRECTION('ref_axis',(1.,9.56839379238543E-14,0.));
#32241=DIRECTION('',(0.,0.,1.));
#32242=DIRECTION('center_axis',(0.,0.,1.));
#32243=DIRECTION('ref_axis',(1.,9.56839379238543E-14,0.));
#32244=DIRECTION('',(0.,0.,1.));
#32245=DIRECTION('center_axis',(0.,0.,1.));
#32246=DIRECTION('ref_axis',(1.,9.56839379238543E-14,0.));
#32247=DIRECTION('',(0.,0.,1.));
#32248=DIRECTION('center_axis',(0.,0.,1.));
#32249=DIRECTION('ref_axis',(1.,0.,0.));
#32250=DIRECTION('center_axis',(0.,0.,1.));
#32251=DIRECTION('ref_axis',(1.,0.,0.));
#32252=DIRECTION('center_axis',(0.,0.,1.));
#32253=DIRECTION('ref_axis',(1.,0.,0.));
#32254=DIRECTION('center_axis',(0.,0.,1.));
#32255=DIRECTION('ref_axis',(1.,0.,0.));
#32256=DIRECTION('center_axis',(0.,0.,1.));
#32257=DIRECTION('ref_axis',(1.,0.,0.));
#32258=DIRECTION('center_axis',(0.,0.,1.));
#32259=DIRECTION('ref_axis',(1.,0.,0.));
#32260=DIRECTION('center_axis',(0.,0.,-1.));
#32261=DIRECTION('ref_axis',(1.,9.56839379238543E-14,0.));
#32262=DIRECTION('center_axis',(0.,0.,1.));
#32263=DIRECTION('ref_axis',(1.,9.56839379238543E-14,0.));
#32264=DIRECTION('center_axis',(0.,0.,1.));
#32265=DIRECTION('ref_axis',(1.,0.,0.));
#32266=DIRECTION('center_axis',(1.22464679914735E-16,-1.,0.));
#32267=DIRECTION('ref_axis',(-1.,-1.22464679914735E-16,0.));
#32268=DIRECTION('center_axis',(0.,0.,-1.));
#32269=DIRECTION('ref_axis',(1.,0.,0.));
#32270=DIRECTION('center_axis',(0.,0.,1.));
#32271=DIRECTION('ref_axis',(1.,0.,0.));
#32272=DIRECTION('center_axis',(0.,0.,1.));
#32273=DIRECTION('ref_axis',(-0.645026930002996,-0.764159839019894,0.));
#32274=DIRECTION('center_axis',(0.,0.,-1.));
#32275=DIRECTION('ref_axis',(-1.,0.,0.));
#32276=DIRECTION('center_axis',(0.,0.,1.));
#32277=DIRECTION('ref_axis',(1.,0.,0.));
#32278=DIRECTION('center_axis',(0.,0.,1.));
#32279=DIRECTION('ref_axis',(1.,0.,0.));
#32280=DIRECTION('',(0.5,-0.866025403784439,0.));
#32281=DIRECTION('center_axis',(0.,0.,1.));
#32282=DIRECTION('ref_axis',(1.,0.,0.));
#32283=DIRECTION('center_axis',(0.,0.,1.));
#32284=DIRECTION('ref_axis',(1.,0.,0.));
#32285=DIRECTION('',(-0.5,-0.866025403784439,0.));
#32286=DIRECTION('center_axis',(0.,0.,1.));
#32287=DIRECTION('ref_axis',(1.,0.,0.));
#32288=DIRECTION('center_axis',(0.,0.,1.));
#32289=DIRECTION('ref_axis',(1.,0.,0.));
#32290=DIRECTION('',(-1.,1.60246890531964E-16,0.));
#32291=DIRECTION('center_axis',(0.,0.,1.));
#32292=DIRECTION('ref_axis',(1.,0.,0.));
#32293=DIRECTION('center_axis',(0.,0.,1.));
#32294=DIRECTION('ref_axis',(1.,0.,0.));
#32295=DIRECTION('',(-0.5,0.866025403784439,0.));
#32296=DIRECTION('center_axis',(0.,0.,1.));
#32297=DIRECTION('ref_axis',(1.,0.,0.));
#32298=DIRECTION('center_axis',(0.,0.,1.));
#32299=DIRECTION('ref_axis',(1.,0.,0.));
#32300=DIRECTION('',(0.5,0.866025403784439,0.));
#32301=DIRECTION('center_axis',(0.,0.,1.));
#32302=DIRECTION('ref_axis',(1.,0.,0.));
#32303=DIRECTION('center_axis',(0.,0.,1.));
#32304=DIRECTION('ref_axis',(1.,0.,0.));
#32305=DIRECTION('',(1.,-1.60246890531964E-16,0.));
#32306=DIRECTION('center_axis',(0.,0.,1.));
#32307=DIRECTION('ref_axis',(1.,0.,0.));
#32308=DIRECTION('center_axis',(0.,0.,1.));
#32309=DIRECTION('ref_axis',(1.,0.,0.));
#32310=DIRECTION('',(-0.857492925712544,-1.05012596676537E-16,0.514495755427527));
#32311=DIRECTION('center_axis',(0.866025403784439,0.5,0.));
#32312=DIRECTION('ref_axis',(0.5,-0.866025403784439,0.));
#32313=DIRECTION('',(0.5,-0.866025403784439,0.));
#32314=DIRECTION('',(0.,0.,-1.));
#32315=DIRECTION('',(0.,0.,-1.));
#32316=DIRECTION('center_axis',(1.60246890531964E-16,1.,0.));
#32317=DIRECTION('ref_axis',(1.,-1.60246890531964E-16,0.));
#32318=DIRECTION('',(1.,-1.60246890531964E-16,0.));
#32319=DIRECTION('',(0.,0.,-1.));
#32320=DIRECTION('center_axis',(-0.866025403784439,0.5,0.));
#32321=DIRECTION('ref_axis',(0.5,0.866025403784439,0.));
#32322=DIRECTION('',(0.5,0.866025403784439,0.));
#32323=DIRECTION('',(0.,0.,-1.));
#32324=DIRECTION('center_axis',(-0.866025403784439,-0.5,0.));
#32325=DIRECTION('ref_axis',(-0.5,0.866025403784439,0.));
#32326=DIRECTION('',(-0.5,0.866025403784439,0.));
#32327=DIRECTION('',(0.,0.,-1.));
#32328=DIRECTION('center_axis',(-1.60246890531964E-16,-1.,0.));
#32329=DIRECTION('ref_axis',(-1.,1.60246890531964E-16,0.));
#32330=DIRECTION('',(-1.,1.60246890531964E-16,0.));
#32331=DIRECTION('',(0.,0.,-1.));
#32332=DIRECTION('center_axis',(0.866025403784439,-0.5,0.));
#32333=DIRECTION('ref_axis',(-0.5,-0.866025403784439,0.));
#32334=DIRECTION('',(-0.5,-0.866025403784439,0.));
#32335=DIRECTION('center_axis',(-0.782019212317096,-0.623254323343969,0.));
#32336=DIRECTION('ref_axis',(-0.623254323343969,0.782019212317096,0.));
#32337=DIRECTION('',(0.,0.,1.));
#32338=DIRECTION('',(-0.623254323343969,0.782019212317096,0.));
#32339=DIRECTION('',(0.,0.,-1.));
#32340=DIRECTION('',(-0.623254323343969,0.782019212317096,0.));
#32341=DIRECTION('center_axis',(0.,0.,1.));
#32342=DIRECTION('ref_axis',(1.,0.,0.));
#32343=DIRECTION('center_axis',(0.,0.,1.));
#32344=DIRECTION('ref_axis',(1.,0.,0.));
#32345=DIRECTION('',(0.980112771261784,0.198441315278714,0.));
#32346=DIRECTION('center_axis',(-0.198441315278714,0.980112771261784,0.));
#32347=DIRECTION('ref_axis',(0.980112771261784,0.198441315278714,0.));
#32348=DIRECTION('',(0.,0.,-1.));
#32349=DIRECTION('',(0.980112771261784,0.198441315278714,0.));
#32350=DIRECTION('center_axis',(0.,0.,-1.));
#32351=DIRECTION('ref_axis',(-1.,0.,0.));
#32352=DIRECTION('center_axis',(0.,0.,-1.));
#32353=DIRECTION('ref_axis',(1.,0.,0.));
#32354=DIRECTION('center_axis',(-0.948023216125629,-0.318201165439129,0.));
#32355=DIRECTION('ref_axis',(-0.318201165439129,0.948023216125629,0.));
#32356=DIRECTION('',(0.,0.,1.));
#32357=DIRECTION('',(-0.318201165439129,0.948023216125629,0.));
#32358=DIRECTION('',(0.,0.,-1.));
#32359=DIRECTION('',(-0.318201165439129,0.948023216125629,0.));
#32360=DIRECTION('center_axis',(0.,0.,1.));
#32361=DIRECTION('ref_axis',(1.,0.,0.));
#32362=DIRECTION('center_axis',(0.,0.,1.));
#32363=DIRECTION('ref_axis',(1.,0.,0.));
#32364=DIRECTION('',(0.988875665786086,-0.148744470875809,0.));
#32365=DIRECTION('center_axis',(0.148744470875809,0.988875665786086,0.));
#32366=DIRECTION('ref_axis',(0.988875665786086,-0.148744470875809,0.));
#32367=DIRECTION('',(0.,0.,-1.));
#32368=DIRECTION('',(0.988875665786086,-0.148744470875809,0.));
#32369=DIRECTION('center_axis',(0.,0.,-1.));
#32370=DIRECTION('ref_axis',(-1.,0.,0.));
#32371=DIRECTION('center_axis',(0.,0.,-1.));
#32372=DIRECTION('ref_axis',(1.,0.,0.));
#32373=DIRECTION('center_axis',(-0.999681628736863,0.0252317491667324,0.));
#32374=DIRECTION('ref_axis',(0.0252317491667324,0.999681628736863,0.));
#32375=DIRECTION('',(0.,0.,1.));
#32376=DIRECTION('',(0.0252317491667324,0.999681628736863,0.));
#32377=DIRECTION('',(0.,0.,-1.));
#32378=DIRECTION('',(0.0252317491667324,0.999681628736863,0.));
#32379=DIRECTION('center_axis',(0.,0.,1.));
#32380=DIRECTION('ref_axis',(1.,0.,0.));
#32381=DIRECTION('center_axis',(0.,0.,1.));
#32382=DIRECTION('ref_axis',(1.,0.,0.));
#32383=DIRECTION('',(0.87836556076609,-0.477989478608131,0.));
#32384=DIRECTION('center_axis',(0.477989478608131,0.87836556076609,0.));
#32385=DIRECTION('ref_axis',(0.87836556076609,-0.477989478608131,0.));
#32386=DIRECTION('',(0.,0.,-1.));
#32387=DIRECTION('',(0.87836556076609,-0.477989478608131,0.));
#32388=DIRECTION('center_axis',(0.,0.,-1.));
#32389=DIRECTION('ref_axis',(-1.,0.,0.));
#32390=DIRECTION('center_axis',(0.,0.,-1.));
#32391=DIRECTION('ref_axis',(1.,0.,0.));
#32392=DIRECTION('center_axis',(-0.930763683192908,0.365621342442113,0.));
#32393=DIRECTION('ref_axis',(0.365621342442113,0.930763683192908,0.));
#32394=DIRECTION('',(0.,0.,1.));
#32395=DIRECTION('',(0.365621342442113,0.930763683192908,0.));
#32396=DIRECTION('',(0.,0.,-1.));
#32397=DIRECTION('',(0.365621342442113,0.930763683192908,0.));
#32398=DIRECTION('center_axis',(0.,0.,1.));
#32399=DIRECTION('ref_axis',(1.,0.,0.));
#32400=DIRECTION('center_axis',(0.,0.,1.));
#32401=DIRECTION('ref_axis',(1.,0.,0.));
#32402=DIRECTION('',(0.661911605822662,-0.749581900846909,0.));
#32403=DIRECTION('center_axis',(0.749581900846909,0.661911605822662,0.));
#32404=DIRECTION('ref_axis',(0.661911605822662,-0.749581900846909,0.));
#32405=DIRECTION('',(0.,0.,-1.));
#32406=DIRECTION('',(0.661911605822662,-0.749581900846909,0.));
#32407=DIRECTION('center_axis',(0.,0.,-1.));
#32408=DIRECTION('ref_axis',(-1.,0.,0.));
#32409=DIRECTION('center_axis',(0.,0.,-1.));
#32410=DIRECTION('ref_axis',(1.,0.,0.));
#32411=DIRECTION('center_axis',(-0.749581900846909,0.661911605822661,0.));
#32412=DIRECTION('ref_axis',(0.661911605822661,0.749581900846909,0.));
#32413=DIRECTION('',(0.,0.,1.));
#32414=DIRECTION('',(0.661911605822661,0.749581900846909,0.));
#32415=DIRECTION('',(0.,0.,-1.));
#32416=DIRECTION('',(0.661911605822661,0.749581900846909,0.));
#32417=DIRECTION('center_axis',(0.,0.,1.));
#32418=DIRECTION('ref_axis',(1.,0.,0.));
#32419=DIRECTION('center_axis',(0.,0.,1.));
#32420=DIRECTION('ref_axis',(1.,0.,0.));
#32421=DIRECTION('',(0.365621342442119,-0.930763683192905,0.));
#32422=DIRECTION('center_axis',(0.930763683192905,0.365621342442119,0.));
#32423=DIRECTION('ref_axis',(0.365621342442119,-0.930763683192905,0.));
#32424=DIRECTION('',(0.,0.,-1.));
#32425=DIRECTION('',(0.365621342442119,-0.930763683192905,0.));
#32426=DIRECTION('center_axis',(0.,0.,-1.));
#32427=DIRECTION('ref_axis',(-1.,0.,0.));
#32428=DIRECTION('center_axis',(0.,0.,-1.));
#32429=DIRECTION('ref_axis',(1.,0.,0.));
#32430=DIRECTION('center_axis',(-0.477989478608131,0.87836556076609,0.));
#32431=DIRECTION('ref_axis',(0.87836556076609,0.477989478608131,0.));
#32432=DIRECTION('',(0.,0.,1.));
#32433=DIRECTION('',(0.87836556076609,0.477989478608131,0.));
#32434=DIRECTION('',(0.,0.,-1.));
#32435=DIRECTION('',(0.87836556076609,0.477989478608131,0.));
#32436=DIRECTION('center_axis',(0.,0.,1.));
#32437=DIRECTION('ref_axis',(1.,0.,0.));
#32438=DIRECTION('center_axis',(0.,0.,1.));
#32439=DIRECTION('ref_axis',(1.,0.,0.));
#32440=DIRECTION('',(0.0252317491667324,-0.999681628736863,0.));
#32441=DIRECTION('center_axis',(0.999681628736863,0.0252317491667324,0.));
#32442=DIRECTION('ref_axis',(0.0252317491667324,-0.999681628736863,0.));
#32443=DIRECTION('',(0.,0.,-1.));
#32444=DIRECTION('',(0.0252317491667324,-0.999681628736863,0.));
#32445=DIRECTION('center_axis',(0.,0.,-1.));
#32446=DIRECTION('ref_axis',(-1.,0.,0.));
#32447=DIRECTION('center_axis',(0.,0.,-1.));
#32448=DIRECTION('ref_axis',(1.,0.,0.));
#32449=DIRECTION('center_axis',(-0.148744470875812,0.988875665786086,0.));
#32450=DIRECTION('ref_axis',(0.988875665786086,0.148744470875812,0.));
#32451=DIRECTION('',(0.,0.,1.));
#32452=DIRECTION('',(0.988875665786086,0.148744470875812,0.));
#32453=DIRECTION('',(0.,0.,-1.));
#32454=DIRECTION('',(0.988875665786086,0.148744470875812,0.));
#32455=DIRECTION('center_axis',(0.,0.,1.));
#32456=DIRECTION('ref_axis',(1.,0.,0.));
#32457=DIRECTION('center_axis',(0.,0.,1.));
#32458=DIRECTION('ref_axis',(1.,0.,0.));
#32459=DIRECTION('',(-0.318201165439124,-0.94802321612563,0.));
#32460=DIRECTION('center_axis',(0.94802321612563,-0.318201165439124,0.));
#32461=DIRECTION('ref_axis',(-0.318201165439124,-0.94802321612563,0.));
#32462=DIRECTION('',(0.,0.,-1.));
#32463=DIRECTION('',(-0.318201165439124,-0.94802321612563,0.));
#32464=DIRECTION('center_axis',(0.,0.,-1.));
#32465=DIRECTION('ref_axis',(-1.,0.,0.));
#32466=DIRECTION('center_axis',(0.,0.,-1.));
#32467=DIRECTION('ref_axis',(1.,0.,0.));
#32468=DIRECTION('center_axis',(0.198441315278718,0.980112771261783,0.));
#32469=DIRECTION('ref_axis',(0.980112771261783,-0.198441315278718,0.));
#32470=DIRECTION('',(0.,0.,1.));
#32471=DIRECTION('',(0.980112771261783,-0.198441315278718,0.));
#32472=DIRECTION('',(0.,0.,-1.));
#32473=DIRECTION('',(0.980112771261783,-0.198441315278718,0.));
#32474=DIRECTION('center_axis',(0.,0.,1.));
#32475=DIRECTION('ref_axis',(1.,0.,0.));
#32476=DIRECTION('center_axis',(0.,0.,1.));
#32477=DIRECTION('ref_axis',(1.,0.,0.));
#32478=DIRECTION('',(-0.623254323343971,-0.782019212317094,0.));
#32479=DIRECTION('center_axis',(0.782019212317094,-0.623254323343971,0.));
#32480=DIRECTION('ref_axis',(-0.623254323343971,-0.782019212317094,0.));
#32481=DIRECTION('',(0.,0.,-1.));
#32482=DIRECTION('',(-0.623254323343971,-0.782019212317094,0.));
#32483=DIRECTION('center_axis',(0.,0.,-1.));
#32484=DIRECTION('ref_axis',(-1.,0.,0.));
#32485=DIRECTION('center_axis',(0.,0.,-1.));
#32486=DIRECTION('ref_axis',(1.,0.,0.));
#32487=DIRECTION('center_axis',(0.521692150128735,0.853133811599363,0.));
#32488=DIRECTION('ref_axis',(0.853133811599363,-0.521692150128735,0.));
#32489=DIRECTION('',(0.,0.,1.));
#32490=DIRECTION('',(0.853133811599363,-0.521692150128735,0.));
#32491=DIRECTION('',(0.,0.,-1.));
#32492=DIRECTION('',(0.853133811599363,-0.521692150128735,0.));
#32493=DIRECTION('center_axis',(0.,0.,1.));
#32494=DIRECTION('ref_axis',(1.,0.,0.));
#32495=DIRECTION('center_axis',(0.,0.,1.));
#32496=DIRECTION('ref_axis',(1.,0.,0.));
#32497=DIRECTION('',(-0.853133811599363,-0.521692150128735,0.));
#32498=DIRECTION('center_axis',(0.,0.,1.));
#32499=DIRECTION('ref_axis',(1.,0.,0.));
#32500=DIRECTION('center_axis',(0.521692150128735,-0.853133811599363,0.));
#32501=DIRECTION('ref_axis',(-0.853133811599363,-0.521692150128735,0.));
#32502=DIRECTION('',(0.,0.,-1.));
#32503=DIRECTION('',(-0.853133811599363,-0.521692150128735,0.));
#32504=DIRECTION('center_axis',(0.,0.,-1.));
#32505=DIRECTION('ref_axis',(-1.,0.,0.));
#32506=DIRECTION('center_axis',(0.,0.,-1.));
#32507=DIRECTION('ref_axis',(1.,0.,0.));
#32508=DIRECTION('center_axis',(0.,0.,-1.));
#32509=DIRECTION('ref_axis',(1.,0.,0.));
#32510=DIRECTION('center_axis',(0.661911605822661,0.749581900846909,0.));
#32511=DIRECTION('ref_axis',(0.749581900846909,-0.661911605822661,0.));
#32512=DIRECTION('',(0.,0.,1.));
#32513=DIRECTION('',(0.749581900846909,-0.661911605822661,0.));
#32514=DIRECTION('',(0.,0.,-1.));
#32515=DIRECTION('',(0.749581900846909,-0.661911605822661,0.));
#32516=DIRECTION('center_axis',(0.,0.,1.));
#32517=DIRECTION('ref_axis',(1.,0.,0.));
#32518=DIRECTION('center_axis',(0.,0.,1.));
#32519=DIRECTION('ref_axis',(1.,0.,0.));
#32520=DIRECTION('',(-0.930763683192906,-0.365621342442116,0.));
#32521=DIRECTION('center_axis',(0.365621342442116,-0.930763683192906,0.));
#32522=DIRECTION('ref_axis',(-0.930763683192906,-0.365621342442116,0.));
#32523=DIRECTION('',(0.,0.,-1.));
#32524=DIRECTION('',(-0.930763683192906,-0.365621342442116,0.));
#32525=DIRECTION('center_axis',(0.,0.,-1.));
#32526=DIRECTION('ref_axis',(-1.,0.,0.));
#32527=DIRECTION('center_axis',(0.,0.,-1.));
#32528=DIRECTION('ref_axis',(1.,0.,0.));
#32529=DIRECTION('center_axis',(0.878365560766093,0.477989478608124,0.));
#32530=DIRECTION('ref_axis',(0.477989478608124,-0.878365560766093,0.));
#32531=DIRECTION('',(0.,0.,1.));
#32532=DIRECTION('',(0.477989478608124,-0.878365560766093,0.));
#32533=DIRECTION('',(0.,0.,-1.));
#32534=DIRECTION('',(0.477989478608124,-0.878365560766093,0.));
#32535=DIRECTION('center_axis',(0.,0.,1.));
#32536=DIRECTION('ref_axis',(1.,0.,0.));
#32537=DIRECTION('center_axis',(0.,0.,1.));
#32538=DIRECTION('ref_axis',(1.,0.,0.));
#32539=DIRECTION('',(-0.999681628736863,-0.0252317491667277,0.));
#32540=DIRECTION('center_axis',(0.0252317491667277,-0.999681628736863,0.));
#32541=DIRECTION('ref_axis',(-0.999681628736863,-0.0252317491667277,0.));
#32542=DIRECTION('',(0.,0.,-1.));
#32543=DIRECTION('',(-0.999681628736863,-0.0252317491667277,0.));
#32544=DIRECTION('center_axis',(0.,0.,-1.));
#32545=DIRECTION('ref_axis',(-1.,0.,0.));
#32546=DIRECTION('center_axis',(0.,0.,-1.));
#32547=DIRECTION('ref_axis',(1.,0.,0.));
#32548=DIRECTION('center_axis',(0.988875665786086,0.148744470875811,0.));
#32549=DIRECTION('ref_axis',(0.148744470875811,-0.988875665786086,0.));
#32550=DIRECTION('',(0.,0.,1.));
#32551=DIRECTION('',(0.148744470875811,-0.988875665786086,0.));
#32552=DIRECTION('',(0.,0.,-1.));
#32553=DIRECTION('',(0.148744470875811,-0.988875665786086,0.));
#32554=DIRECTION('center_axis',(0.,0.,1.));
#32555=DIRECTION('ref_axis',(1.,0.,0.));
#32556=DIRECTION('center_axis',(0.,0.,1.));
#32557=DIRECTION('ref_axis',(1.,0.,0.));
#32558=DIRECTION('',(-0.94802321612563,0.318201165439124,0.));
#32559=DIRECTION('center_axis',(-0.318201165439124,-0.94802321612563,0.));
#32560=DIRECTION('ref_axis',(-0.94802321612563,0.318201165439124,0.));
#32561=DIRECTION('',(0.,0.,-1.));
#32562=DIRECTION('',(-0.94802321612563,0.318201165439124,0.));
#32563=DIRECTION('center_axis',(0.,0.,-1.));
#32564=DIRECTION('ref_axis',(-1.,0.,0.));
#32565=DIRECTION('center_axis',(0.,0.,-1.));
#32566=DIRECTION('ref_axis',(1.,0.,0.));
#32567=DIRECTION('center_axis',(0.980112771261783,-0.19844131527872,0.));
#32568=DIRECTION('ref_axis',(-0.19844131527872,-0.980112771261783,0.));
#32569=DIRECTION('',(0.,0.,1.));
#32570=DIRECTION('',(-0.19844131527872,-0.980112771261783,0.));
#32571=DIRECTION('',(0.,0.,-1.));
#32572=DIRECTION('',(-0.19844131527872,-0.980112771261783,0.));
#32573=DIRECTION('center_axis',(0.,0.,1.));
#32574=DIRECTION('ref_axis',(1.,0.,0.));
#32575=DIRECTION('center_axis',(0.,0.,1.));
#32576=DIRECTION('ref_axis',(1.,0.,0.));
#32577=DIRECTION('',(-0.782019212317096,0.623254323343969,0.));
#32578=DIRECTION('center_axis',(-0.623254323343969,-0.782019212317096,0.));
#32579=DIRECTION('ref_axis',(-0.782019212317096,0.623254323343969,0.));
#32580=DIRECTION('',(0.,0.,-1.));
#32581=DIRECTION('',(-0.782019212317096,0.623254323343969,0.));
#32582=DIRECTION('center_axis',(0.,0.,-1.));
#32583=DIRECTION('ref_axis',(-1.,0.,0.));
#32584=DIRECTION('center_axis',(0.,0.,-1.));
#32585=DIRECTION('ref_axis',(1.,0.,0.));
#32586=DIRECTION('center_axis',(0.853133811599362,-0.521692150128737,0.));
#32587=DIRECTION('ref_axis',(-0.521692150128737,-0.853133811599362,0.));
#32588=DIRECTION('',(0.,0.,1.));
#32589=DIRECTION('',(-0.521692150128737,-0.853133811599362,0.));
#32590=DIRECTION('',(0.,0.,-1.));
#32591=DIRECTION('',(-0.521692150128737,-0.853133811599362,0.));
#32592=DIRECTION('center_axis',(0.,0.,1.));
#32593=DIRECTION('ref_axis',(1.,0.,0.));
#32594=DIRECTION('center_axis',(0.,0.,1.));
#32595=DIRECTION('ref_axis',(1.,0.,0.));
#32596=DIRECTION('',(-0.521692150128737,0.853133811599362,0.));
#32597=DIRECTION('center_axis',(-0.853133811599362,-0.521692150128737,0.));
#32598=DIRECTION('ref_axis',(-0.521692150128737,0.853133811599362,0.));
#32599=DIRECTION('',(0.,0.,-1.));
#32600=DIRECTION('',(-0.521692150128737,0.853133811599362,0.));
#32601=DIRECTION('center_axis',(0.,0.,-1.));
#32602=DIRECTION('ref_axis',(-1.,0.,0.));
#32603=DIRECTION('center_axis',(0.,0.,-1.));
#32604=DIRECTION('ref_axis',(1.,0.,0.));
#32605=DIRECTION('center_axis',(0.62325432334397,-0.782019212317095,0.));
#32606=DIRECTION('ref_axis',(-0.782019212317095,-0.62325432334397,0.));
#32607=DIRECTION('',(0.,0.,1.));
#32608=DIRECTION('',(-0.782019212317095,-0.62325432334397,0.));
#32609=DIRECTION('',(0.,0.,-1.));
#32610=DIRECTION('',(-0.782019212317095,-0.62325432334397,0.));
#32611=DIRECTION('center_axis',(0.,0.,1.));
#32612=DIRECTION('ref_axis',(1.,0.,0.));
#32613=DIRECTION('center_axis',(0.,0.,1.));
#32614=DIRECTION('ref_axis',(1.,0.,0.));
#32615=DIRECTION('',(-0.19844131527872,0.980112771261783,0.));
#32616=DIRECTION('center_axis',(-0.980112771261783,-0.19844131527872,0.));
#32617=DIRECTION('ref_axis',(-0.19844131527872,0.980112771261783,0.));
#32618=DIRECTION('',(0.,0.,-1.));
#32619=DIRECTION('',(-0.19844131527872,0.980112771261783,0.));
#32620=DIRECTION('center_axis',(0.,0.,-1.));
#32621=DIRECTION('ref_axis',(-1.,0.,0.));
#32622=DIRECTION('center_axis',(0.,0.,-1.));
#32623=DIRECTION('ref_axis',(1.,0.,0.));
#32624=DIRECTION('center_axis',(0.318201165439123,-0.948023216125631,0.));
#32625=DIRECTION('ref_axis',(-0.948023216125631,-0.318201165439123,0.));
#32626=DIRECTION('',(0.,0.,1.));
#32627=DIRECTION('',(-0.948023216125631,-0.318201165439123,0.));
#32628=DIRECTION('',(0.,0.,-1.));
#32629=DIRECTION('',(-0.948023216125631,-0.318201165439123,0.));
#32630=DIRECTION('center_axis',(0.,0.,1.));
#32631=DIRECTION('ref_axis',(1.,0.,0.));
#32632=DIRECTION('center_axis',(0.,0.,1.));
#32633=DIRECTION('ref_axis',(1.,0.,0.));
#32634=DIRECTION('',(0.148744470875811,0.988875665786086,0.));
#32635=DIRECTION('center_axis',(-0.988875665786086,0.148744470875811,0.));
#32636=DIRECTION('ref_axis',(0.148744470875811,0.988875665786086,0.));
#32637=DIRECTION('',(0.,0.,-1.));
#32638=DIRECTION('',(0.148744470875811,0.988875665786086,0.));
#32639=DIRECTION('center_axis',(0.,0.,-1.));
#32640=DIRECTION('ref_axis',(-1.,0.,0.));
#32641=DIRECTION('center_axis',(0.,0.,-1.));
#32642=DIRECTION('ref_axis',(1.,0.,0.));
#32643=DIRECTION('center_axis',(-0.0252317491667293,-0.999681628736863,
0.));
#32644=DIRECTION('ref_axis',(-0.999681628736863,0.0252317491667293,0.));
#32645=DIRECTION('',(0.,0.,1.));
#32646=DIRECTION('',(-0.999681628736863,0.0252317491667293,0.));
#32647=DIRECTION('',(0.,0.,-1.));
#32648=DIRECTION('',(-0.999681628736863,0.0252317491667293,0.));
#32649=DIRECTION('center_axis',(0.,0.,1.));
#32650=DIRECTION('ref_axis',(1.,0.,0.));
#32651=DIRECTION('center_axis',(0.,0.,1.));
#32652=DIRECTION('ref_axis',(1.,0.,0.));
#32653=DIRECTION('',(0.477989478608125,0.878365560766093,0.));
#32654=DIRECTION('center_axis',(-0.878365560766093,0.477989478608125,0.));
#32655=DIRECTION('ref_axis',(0.477989478608125,0.878365560766093,0.));
#32656=DIRECTION('',(0.,0.,-1.));
#32657=DIRECTION('',(0.477989478608125,0.878365560766093,0.));
#32658=DIRECTION('center_axis',(0.,0.,-1.));
#32659=DIRECTION('ref_axis',(-1.,0.,0.));
#32660=DIRECTION('center_axis',(0.,0.,-1.));
#32661=DIRECTION('ref_axis',(1.,0.,0.));
#32662=DIRECTION('center_axis',(-0.365621342442117,-0.930763683192906,0.));
#32663=DIRECTION('ref_axis',(-0.930763683192906,0.365621342442117,0.));
#32664=DIRECTION('',(0.,0.,1.));
#32665=DIRECTION('',(-0.930763683192906,0.365621342442117,0.));
#32666=DIRECTION('',(0.,0.,-1.));
#32667=DIRECTION('',(-0.930763683192906,0.365621342442117,0.));
#32668=DIRECTION('center_axis',(0.,0.,1.));
#32669=DIRECTION('ref_axis',(1.,0.,0.));
#32670=DIRECTION('center_axis',(0.,0.,1.));
#32671=DIRECTION('ref_axis',(1.,0.,0.));
#32672=DIRECTION('',(0.749581900846911,0.661911605822659,0.));
#32673=DIRECTION('center_axis',(-0.661911605822659,0.749581900846911,0.));
#32674=DIRECTION('ref_axis',(0.749581900846911,0.661911605822659,0.));
#32675=DIRECTION('',(0.,0.,-1.));
#32676=DIRECTION('',(0.749581900846911,0.661911605822659,0.));
#32677=DIRECTION('center_axis',(0.,0.,-1.));
#32678=DIRECTION('ref_axis',(-1.,0.,0.));
#32679=DIRECTION('center_axis',(0.,0.,-1.));
#32680=DIRECTION('ref_axis',(1.,0.,0.));
#32681=DIRECTION('center_axis',(-0.198441315278718,-0.980112771261783,0.));
#32682=DIRECTION('ref_axis',(-0.980112771261783,0.198441315278718,0.));
#32683=DIRECTION('',(0.,0.,1.));
#32684=DIRECTION('',(-0.980112771261783,0.198441315278718,0.));
#32685=DIRECTION('',(0.,0.,-1.));
#32686=DIRECTION('',(-0.980112771261783,0.198441315278718,0.));
#32687=DIRECTION('center_axis',(0.,0.,1.));
#32688=DIRECTION('ref_axis',(1.,0.,0.));
#32689=DIRECTION('center_axis',(0.,0.,1.));
#32690=DIRECTION('ref_axis',(1.,0.,0.));
#32691=DIRECTION('',(0.623254323343969,0.782019212317096,0.));
#32692=DIRECTION('center_axis',(-0.782019212317096,0.623254323343969,0.));
#32693=DIRECTION('ref_axis',(0.623254323343969,0.782019212317096,0.));
#32694=DIRECTION('',(0.,0.,-1.));
#32695=DIRECTION('',(0.623254323343969,0.782019212317096,0.));
#32696=DIRECTION('center_axis',(0.,0.,-1.));
#32697=DIRECTION('ref_axis',(-1.,0.,0.));
#32698=DIRECTION('center_axis',(0.,0.,-1.));
#32699=DIRECTION('ref_axis',(1.,0.,0.));
#32700=DIRECTION('center_axis',(0.148744470875811,-0.988875665786086,0.));
#32701=DIRECTION('ref_axis',(-0.988875665786086,-0.148744470875811,0.));
#32702=DIRECTION('',(0.,0.,1.));
#32703=DIRECTION('',(-0.988875665786086,-0.148744470875811,0.));
#32704=DIRECTION('',(0.,0.,-1.));
#32705=DIRECTION('',(-0.988875665786086,-0.148744470875811,0.));
#32706=DIRECTION('center_axis',(0.,0.,1.));
#32707=DIRECTION('ref_axis',(1.,0.,0.));
#32708=DIRECTION('center_axis',(0.,0.,1.));
#32709=DIRECTION('ref_axis',(1.,0.,0.));
#32710=DIRECTION('',(0.318201165439122,0.948023216125631,0.));
#32711=DIRECTION('center_axis',(-0.948023216125631,0.318201165439122,0.));
#32712=DIRECTION('ref_axis',(0.318201165439122,0.948023216125631,0.));
#32713=DIRECTION('',(0.,0.,-1.));
#32714=DIRECTION('',(0.318201165439122,0.948023216125631,0.));
#32715=DIRECTION('center_axis',(0.,0.,-1.));
#32716=DIRECTION('ref_axis',(-1.,0.,0.));
#32717=DIRECTION('center_axis',(0.,0.,-1.));
#32718=DIRECTION('ref_axis',(1.,0.,0.));
#32719=DIRECTION('center_axis',(0.477989478608127,-0.878365560766092,0.));
#32720=DIRECTION('ref_axis',(-0.878365560766092,-0.477989478608127,0.));
#32721=DIRECTION('',(0.,0.,1.));
#32722=DIRECTION('',(-0.878365560766092,-0.477989478608127,0.));
#32723=DIRECTION('',(0.,0.,-1.));
#32724=DIRECTION('',(-0.878365560766092,-0.477989478608127,0.));
#32725=DIRECTION('center_axis',(0.,0.,1.));
#32726=DIRECTION('ref_axis',(1.,0.,0.));
#32727=DIRECTION('center_axis',(0.,0.,1.));
#32728=DIRECTION('ref_axis',(1.,0.,0.));
#32729=DIRECTION('',(-0.0252317491667292,0.999681628736863,0.));
#32730=DIRECTION('center_axis',(-0.999681628736863,-0.0252317491667292,
0.));
#32731=DIRECTION('ref_axis',(-0.0252317491667292,0.999681628736863,0.));
#32732=DIRECTION('',(0.,0.,-1.));
#32733=DIRECTION('',(-0.0252317491667292,0.999681628736863,0.));
#32734=DIRECTION('center_axis',(0.,0.,-1.));
#32735=DIRECTION('ref_axis',(-1.,0.,0.));
#32736=DIRECTION('center_axis',(0.,0.,-1.));
#32737=DIRECTION('ref_axis',(1.,0.,0.));
#32738=DIRECTION('center_axis',(0.749581900846912,-0.661911605822658,0.));
#32739=DIRECTION('ref_axis',(-0.661911605822658,-0.749581900846912,0.));
#32740=DIRECTION('',(0.,0.,1.));
#32741=DIRECTION('',(-0.661911605822658,-0.749581900846912,0.));
#32742=DIRECTION('',(0.,0.,-1.));
#32743=DIRECTION('',(-0.661911605822658,-0.749581900846912,0.));
#32744=DIRECTION('center_axis',(0.,0.,1.));
#32745=DIRECTION('ref_axis',(1.,0.,0.));
#32746=DIRECTION('center_axis',(0.,0.,1.));
#32747=DIRECTION('ref_axis',(1.,0.,0.));
#32748=DIRECTION('',(-0.365621342442117,0.930763683192906,0.));
#32749=DIRECTION('center_axis',(-0.930763683192906,-0.365621342442117,0.));
#32750=DIRECTION('ref_axis',(-0.365621342442117,0.930763683192906,0.));
#32751=DIRECTION('',(0.,0.,-1.));
#32752=DIRECTION('',(-0.365621342442117,0.930763683192906,0.));
#32753=DIRECTION('center_axis',(0.,0.,-1.));
#32754=DIRECTION('ref_axis',(-1.,0.,0.));
#32755=DIRECTION('center_axis',(0.,0.,-1.));
#32756=DIRECTION('ref_axis',(1.,0.,0.));
#32757=DIRECTION('center_axis',(0.930763683192906,-0.365621342442117,0.));
#32758=DIRECTION('ref_axis',(-0.365621342442117,-0.930763683192906,0.));
#32759=DIRECTION('',(0.,0.,1.));
#32760=DIRECTION('',(-0.365621342442117,-0.930763683192906,0.));
#32761=DIRECTION('',(0.,0.,-1.));
#32762=DIRECTION('',(-0.365621342442117,-0.930763683192906,0.));
#32763=DIRECTION('center_axis',(0.,0.,1.));
#32764=DIRECTION('ref_axis',(1.,0.,0.));
#32765=DIRECTION('center_axis',(0.,0.,1.));
#32766=DIRECTION('ref_axis',(1.,0.,0.));
#32767=DIRECTION('',(-0.66191160582266,0.749581900846911,0.));
#32768=DIRECTION('center_axis',(-0.749581900846911,-0.66191160582266,0.));
#32769=DIRECTION('ref_axis',(-0.66191160582266,0.749581900846911,0.));
#32770=DIRECTION('',(0.,0.,-1.));
#32771=DIRECTION('',(-0.66191160582266,0.749581900846911,0.));
#32772=DIRECTION('center_axis',(0.,0.,-1.));
#32773=DIRECTION('ref_axis',(-1.,0.,0.));
#32774=DIRECTION('center_axis',(0.,0.,-1.));
#32775=DIRECTION('ref_axis',(1.,0.,0.));
#32776=DIRECTION('center_axis',(0.999681628736863,-0.0252317491667285,0.));
#32777=DIRECTION('ref_axis',(-0.0252317491667285,-0.999681628736863,0.));
#32778=DIRECTION('',(0.,0.,1.));
#32779=DIRECTION('',(-0.0252317491667285,-0.999681628736863,0.));
#32780=DIRECTION('',(0.,0.,-1.));
#32781=DIRECTION('',(-0.0252317491667285,-0.999681628736863,0.));
#32782=DIRECTION('center_axis',(0.,0.,1.));
#32783=DIRECTION('ref_axis',(1.,0.,0.));
#32784=DIRECTION('center_axis',(0.,0.,1.));
#32785=DIRECTION('ref_axis',(1.,0.,0.));
#32786=DIRECTION('',(-0.878365560766093,0.477989478608125,0.));
#32787=DIRECTION('center_axis',(-0.477989478608125,-0.878365560766093,0.));
#32788=DIRECTION('ref_axis',(-0.878365560766093,0.477989478608125,0.));
#32789=DIRECTION('',(0.,0.,-1.));
#32790=DIRECTION('',(-0.878365560766093,0.477989478608125,0.));
#32791=DIRECTION('center_axis',(0.,0.,-1.));
#32792=DIRECTION('ref_axis',(-1.,0.,0.));
#32793=DIRECTION('center_axis',(0.,0.,-1.));
#32794=DIRECTION('ref_axis',(1.,0.,0.));
#32795=DIRECTION('center_axis',(0.94802321612563,0.318201165439124,0.));
#32796=DIRECTION('ref_axis',(0.318201165439124,-0.94802321612563,0.));
#32797=DIRECTION('',(0.,0.,1.));
#32798=DIRECTION('',(0.318201165439124,-0.94802321612563,0.));
#32799=DIRECTION('',(0.,0.,-1.));
#32800=DIRECTION('',(0.318201165439124,-0.94802321612563,0.));
#32801=DIRECTION('center_axis',(0.,0.,1.));
#32802=DIRECTION('ref_axis',(1.,0.,0.));
#32803=DIRECTION('center_axis',(0.,0.,1.));
#32804=DIRECTION('ref_axis',(1.,0.,0.));
#32805=DIRECTION('',(-0.988875665786087,0.148744470875807,0.));
#32806=DIRECTION('center_axis',(-0.148744470875807,-0.988875665786087,0.));
#32807=DIRECTION('ref_axis',(-0.988875665786087,0.148744470875807,0.));
#32808=DIRECTION('',(0.,0.,-1.));
#32809=DIRECTION('',(-0.988875665786087,0.148744470875807,0.));
#32810=DIRECTION('center_axis',(0.,0.,-1.));
#32811=DIRECTION('ref_axis',(-1.,0.,0.));
#32812=DIRECTION('center_axis',(0.,0.,-1.));
#32813=DIRECTION('ref_axis',(1.,0.,0.));
#32814=DIRECTION('center_axis',(0.782019212317095,0.62325432334397,0.));
#32815=DIRECTION('ref_axis',(0.62325432334397,-0.782019212317095,0.));
#32816=DIRECTION('',(0.,0.,1.));
#32817=DIRECTION('',(0.62325432334397,-0.782019212317095,0.));
#32818=DIRECTION('',(0.,0.,-1.));
#32819=DIRECTION('',(0.62325432334397,-0.782019212317095,0.));
#32820=DIRECTION('center_axis',(0.,0.,1.));
#32821=DIRECTION('ref_axis',(1.,0.,0.));
#32822=DIRECTION('center_axis',(0.,0.,1.));
#32823=DIRECTION('ref_axis',(1.,0.,0.));
#32824=DIRECTION('',(-0.980112771261782,-0.198441315278722,0.));
#32825=DIRECTION('center_axis',(0.198441315278722,-0.980112771261782,0.));
#32826=DIRECTION('ref_axis',(-0.980112771261782,-0.198441315278722,0.));
#32827=DIRECTION('',(0.,0.,-1.));
#32828=DIRECTION('',(-0.980112771261782,-0.198441315278722,0.));
#32829=DIRECTION('center_axis',(0.,0.,-1.));
#32830=DIRECTION('ref_axis',(-1.,0.,0.));
#32831=DIRECTION('center_axis',(0.,0.,-1.));
#32832=DIRECTION('ref_axis',(1.,0.,0.));
#32833=DIRECTION('center_axis',(0.,0.,1.));
#32834=DIRECTION('ref_axis',(1.,0.,0.));
#32835=DIRECTION('center_axis',(0.,0.,1.));
#32836=DIRECTION('ref_axis',(1.,0.,0.));
#32837=DIRECTION('',(-0.853133811599362,0.521692150128736,0.));
#32838=DIRECTION('',(0.853133811599362,0.521692150128736,0.));
#32839=DIRECTION('center_axis',(-0.521692150128736,-0.853133811599362,0.));
#32840=DIRECTION('ref_axis',(-0.853133811599362,0.521692150128736,0.));
#32841=DIRECTION('',(0.,0.,1.));
#32842=DIRECTION('',(-0.853133811599362,0.521692150128736,0.));
#32843=DIRECTION('',(0.,0.,-1.));
#32844=DIRECTION('center_axis',(-0.521692150128736,0.853133811599362,0.));
#32845=DIRECTION('ref_axis',(0.853133811599362,0.521692150128736,0.));
#32846=DIRECTION('',(0.,0.,-1.));
#32847=DIRECTION('',(0.853133811599362,0.521692150128736,0.));
#32848=DIRECTION('center_axis',(0.,0.,-1.));
#32849=DIRECTION('ref_axis',(-1.,0.,0.));
#32850=DIRECTION('center_axis',(0.,0.,-1.));
#32851=DIRECTION('ref_axis',(1.,0.,0.));
#32852=DIRECTION('center_axis',(0.365621342442119,0.930763683192905,0.));
#32853=DIRECTION('ref_axis',(0.930763683192905,-0.365621342442119,0.));
#32854=DIRECTION('',(0.,0.,1.));
#32855=DIRECTION('',(0.930763683192905,-0.365621342442119,0.));
#32856=DIRECTION('',(0.,0.,-1.));
#32857=DIRECTION('',(0.930763683192905,-0.365621342442119,0.));
#32858=DIRECTION('center_axis',(0.,0.,1.));
#32859=DIRECTION('ref_axis',(1.,0.,0.));
#32860=DIRECTION('center_axis',(0.,0.,1.));
#32861=DIRECTION('ref_axis',(1.,0.,0.));
#32862=DIRECTION('',(-0.749581900846912,-0.661911605822659,0.));
#32863=DIRECTION('center_axis',(0.661911605822659,-0.749581900846912,0.));
#32864=DIRECTION('ref_axis',(-0.749581900846912,-0.661911605822659,0.));
#32865=DIRECTION('',(0.,0.,-1.));
#32866=DIRECTION('',(-0.749581900846912,-0.661911605822659,0.));
#32867=DIRECTION('center_axis',(0.,0.,-1.));
#32868=DIRECTION('ref_axis',(-1.,0.,0.));
#32869=DIRECTION('center_axis',(0.,0.,-1.));
#32870=DIRECTION('ref_axis',(1.,0.,0.));
#32871=DIRECTION('center_axis',(0.0252317491667325,0.999681628736863,0.));
#32872=DIRECTION('ref_axis',(0.999681628736863,-0.0252317491667325,0.));
#32873=DIRECTION('',(0.,0.,1.));
#32874=DIRECTION('',(0.999681628736863,-0.0252317491667325,0.));
#32875=DIRECTION('',(0.,0.,-1.));
#32876=DIRECTION('',(0.999681628736863,-0.0252317491667325,0.));
#32877=DIRECTION('center_axis',(0.,0.,1.));
#32878=DIRECTION('ref_axis',(1.,0.,0.));
#32879=DIRECTION('center_axis',(0.,0.,1.));
#32880=DIRECTION('ref_axis',(1.,0.,0.));
#32881=DIRECTION('',(-0.477989478608127,-0.878365560766092,0.));
#32882=DIRECTION('center_axis',(0.878365560766092,-0.477989478608127,0.));
#32883=DIRECTION('ref_axis',(-0.477989478608127,-0.878365560766092,0.));
#32884=DIRECTION('',(0.,0.,-1.));
#32885=DIRECTION('',(-0.477989478608127,-0.878365560766092,0.));
#32886=DIRECTION('center_axis',(0.,0.,-1.));
#32887=DIRECTION('ref_axis',(-1.,0.,0.));
#32888=DIRECTION('center_axis',(0.,0.,-1.));
#32889=DIRECTION('ref_axis',(1.,0.,0.));
#32890=DIRECTION('center_axis',(-0.318201165439124,0.94802321612563,0.));
#32891=DIRECTION('ref_axis',(0.94802321612563,0.318201165439124,0.));
#32892=DIRECTION('',(0.,0.,1.));
#32893=DIRECTION('',(0.94802321612563,0.318201165439124,0.));
#32894=DIRECTION('',(0.,0.,-1.));
#32895=DIRECTION('',(0.94802321612563,0.318201165439124,0.));
#32896=DIRECTION('center_axis',(0.,0.,1.));
#32897=DIRECTION('ref_axis',(1.,0.,0.));
#32898=DIRECTION('center_axis',(0.,0.,1.));
#32899=DIRECTION('ref_axis',(1.,0.,0.));
#32900=DIRECTION('',(-0.148744470875809,-0.988875665786086,0.));
#32901=DIRECTION('center_axis',(0.988875665786086,-0.148744470875809,0.));
#32902=DIRECTION('ref_axis',(-0.148744470875809,-0.988875665786086,0.));
#32903=DIRECTION('',(0.,0.,-1.));
#32904=DIRECTION('',(-0.148744470875809,-0.988875665786086,0.));
#32905=DIRECTION('center_axis',(0.,0.,-1.));
#32906=DIRECTION('ref_axis',(-1.,0.,0.));
#32907=DIRECTION('center_axis',(0.,0.,-1.));
#32908=DIRECTION('ref_axis',(1.,0.,0.));
#32909=DIRECTION('center_axis',(-0.623254323343969,0.782019212317096,0.));
#32910=DIRECTION('ref_axis',(0.782019212317096,0.623254323343969,0.));
#32911=DIRECTION('',(0.,0.,1.));
#32912=DIRECTION('',(0.782019212317096,0.623254323343969,0.));
#32913=DIRECTION('',(0.,0.,-1.));
#32914=DIRECTION('',(0.782019212317096,0.623254323343969,0.));
#32915=DIRECTION('center_axis',(0.,0.,1.));
#32916=DIRECTION('ref_axis',(1.,0.,0.));
#32917=DIRECTION('center_axis',(0.,0.,1.));
#32918=DIRECTION('ref_axis',(1.,0.,0.));
#32919=DIRECTION('',(0.198441315278714,-0.980112771261784,0.));
#32920=DIRECTION('center_axis',(0.980112771261784,0.198441315278714,0.));
#32921=DIRECTION('ref_axis',(0.198441315278714,-0.980112771261784,0.));
#32922=DIRECTION('',(0.,0.,-1.));
#32923=DIRECTION('',(0.198441315278714,-0.980112771261784,0.));
#32924=DIRECTION('center_axis',(0.,0.,-1.));
#32925=DIRECTION('ref_axis',(-1.,0.,0.));
#32926=DIRECTION('center_axis',(0.,0.,-1.));
#32927=DIRECTION('ref_axis',(1.,0.,0.));
#32928=DIRECTION('center_axis',(-0.853133811599361,0.521692150128738,0.));
#32929=DIRECTION('ref_axis',(0.521692150128738,0.853133811599361,0.));
#32930=DIRECTION('',(0.,0.,1.));
#32931=DIRECTION('',(0.521692150128738,0.853133811599361,0.));
#32932=DIRECTION('',(0.,0.,-1.));
#32933=DIRECTION('',(0.521692150128738,0.853133811599361,0.));
#32934=DIRECTION('center_axis',(0.,0.,1.));
#32935=DIRECTION('ref_axis',(1.,0.,0.));
#32936=DIRECTION('center_axis',(0.,0.,1.));
#32937=DIRECTION('ref_axis',(1.,0.,0.));
#32938=DIRECTION('',(0.521692150128738,-0.853133811599361,0.));
#32939=DIRECTION('center_axis',(0.853133811599361,0.521692150128738,0.));
#32940=DIRECTION('ref_axis',(0.521692150128738,-0.853133811599361,0.));
#32941=DIRECTION('',(0.,0.,-1.));
#32942=DIRECTION('',(0.521692150128738,-0.853133811599361,0.));
#32943=DIRECTION('center_axis',(0.,0.,-1.));
#32944=DIRECTION('ref_axis',(-1.,0.,0.));
#32945=DIRECTION('center_axis',(0.,0.,-1.));
#32946=DIRECTION('ref_axis',(1.,0.,0.));
#32947=DIRECTION('center_axis',(-0.980112771261782,0.198441315278721,0.));
#32948=DIRECTION('ref_axis',(0.198441315278721,0.980112771261782,0.));
#32949=DIRECTION('',(0.,0.,1.));
#32950=DIRECTION('',(0.198441315278721,0.980112771261782,0.));
#32951=DIRECTION('',(0.,0.,-1.));
#32952=DIRECTION('',(0.198441315278721,0.980112771261782,0.));
#32953=DIRECTION('center_axis',(0.,0.,1.));
#32954=DIRECTION('ref_axis',(1.,0.,0.));
#32955=DIRECTION('center_axis',(0.,0.,1.));
#32956=DIRECTION('ref_axis',(1.,0.,0.));
#32957=DIRECTION('',(0.782019212317093,-0.623254323343973,0.));
#32958=DIRECTION('center_axis',(0.623254323343973,0.782019212317093,0.));
#32959=DIRECTION('ref_axis',(0.782019212317093,-0.623254323343973,0.));
#32960=DIRECTION('',(0.,0.,-1.));
#32961=DIRECTION('',(0.782019212317093,-0.623254323343973,0.));
#32962=DIRECTION('center_axis',(0.,0.,-1.));
#32963=DIRECTION('ref_axis',(-1.,0.,0.));
#32964=DIRECTION('center_axis',(0.,0.,-1.));
#32965=DIRECTION('ref_axis',(1.,0.,0.));
#32966=DIRECTION('center_axis',(-0.988875665786087,-0.148744470875808,0.));
#32967=DIRECTION('ref_axis',(-0.148744470875808,0.988875665786087,0.));
#32968=DIRECTION('',(0.,0.,1.));
#32969=DIRECTION('',(-0.148744470875808,0.988875665786087,0.));
#32970=DIRECTION('',(0.,0.,-1.));
#32971=DIRECTION('',(-0.148744470875808,0.988875665786087,0.));
#32972=DIRECTION('center_axis',(0.,0.,1.));
#32973=DIRECTION('ref_axis',(1.,0.,0.));
#32974=DIRECTION('center_axis',(0.,0.,1.));
#32975=DIRECTION('ref_axis',(1.,0.,0.));
#32976=DIRECTION('',(0.948023216125631,-0.318201165439121,0.));
#32977=DIRECTION('center_axis',(0.318201165439121,0.948023216125631,0.));
#32978=DIRECTION('ref_axis',(0.948023216125631,-0.318201165439121,0.));
#32979=DIRECTION('',(0.,0.,-1.));
#32980=DIRECTION('',(0.948023216125631,-0.318201165439121,0.));
#32981=DIRECTION('center_axis',(0.,0.,-1.));
#32982=DIRECTION('ref_axis',(-1.,0.,0.));
#32983=DIRECTION('center_axis',(0.,0.,-1.));
#32984=DIRECTION('ref_axis',(1.,0.,0.));
#32985=DIRECTION('center_axis',(-0.87836556076609,-0.477989478608131,0.));
#32986=DIRECTION('ref_axis',(-0.477989478608131,0.87836556076609,0.));
#32987=DIRECTION('',(0.,0.,1.));
#32988=DIRECTION('',(-0.477989478608131,0.87836556076609,0.));
#32989=DIRECTION('',(0.,0.,-1.));
#32990=DIRECTION('',(-0.477989478608131,0.87836556076609,0.));
#32991=DIRECTION('center_axis',(0.,0.,1.));
#32992=DIRECTION('ref_axis',(1.,0.,0.));
#32993=DIRECTION('center_axis',(0.,0.,1.));
#32994=DIRECTION('ref_axis',(1.,0.,0.));
#32995=DIRECTION('',(0.999681628736863,0.0252317491667324,0.));
#32996=DIRECTION('center_axis',(-0.0252317491667324,0.999681628736863,0.));
#32997=DIRECTION('ref_axis',(0.999681628736863,0.0252317491667324,0.));
#32998=DIRECTION('',(0.,0.,-1.));
#32999=DIRECTION('',(0.999681628736863,0.0252317491667324,0.));
#33000=DIRECTION('center_axis',(0.,0.,-1.));
#33001=DIRECTION('ref_axis',(-1.,0.,0.));
#33002=DIRECTION('center_axis',(0.,0.,-1.));
#33003=DIRECTION('ref_axis',(1.,0.,0.));
#33004=DIRECTION('center_axis',(-0.661911605822662,-0.749581900846909,0.));
#33005=DIRECTION('ref_axis',(-0.749581900846909,0.661911605822662,0.));
#33006=DIRECTION('',(0.,0.,1.));
#33007=DIRECTION('',(-0.749581900846909,0.661911605822662,0.));
#33008=DIRECTION('',(0.,0.,-1.));
#33009=DIRECTION('',(-0.749581900846909,0.661911605822662,0.));
#33010=DIRECTION('center_axis',(0.,0.,1.));
#33011=DIRECTION('ref_axis',(1.,0.,0.));
#33012=DIRECTION('center_axis',(0.,0.,1.));
#33013=DIRECTION('ref_axis',(1.,0.,0.));
#33014=DIRECTION('',(0.930763683192905,0.365621342442119,0.));
#33015=DIRECTION('center_axis',(-0.365621342442119,0.930763683192905,0.));
#33016=DIRECTION('ref_axis',(0.930763683192905,0.365621342442119,0.));
#33017=DIRECTION('',(0.,0.,-1.));
#33018=DIRECTION('',(0.930763683192905,0.365621342442119,0.));
#33019=DIRECTION('center_axis',(0.,0.,-1.));
#33020=DIRECTION('ref_axis',(-1.,0.,0.));
#33021=DIRECTION('center_axis',(0.,0.,-1.));
#33022=DIRECTION('ref_axis',(1.,0.,0.));
#33023=DIRECTION('center_axis',(0.,0.,-1.));
#33024=DIRECTION('ref_axis',(-1.,0.,0.));
#33025=DIRECTION('center_axis',(0.,0.,1.));
#33026=DIRECTION('ref_axis',(1.,0.,0.));
#33027=DIRECTION('center_axis',(0.,0.,1.));
#33028=DIRECTION('ref_axis',(1.,0.,0.));
#33029=DIRECTION('',(0.707106781186548,8.65956056235493E-17,-0.707106781186547));
#33030=DIRECTION('center_axis',(0.,0.,1.));
#33031=DIRECTION('ref_axis',(1.,0.,0.));
#33032=DIRECTION('center_axis',(0.,0.,1.));
#33033=DIRECTION('ref_axis',(1.,0.,0.));
#33034=DIRECTION('',(0.707106781186548,8.65956056235494E-17,-0.707106781186547));
#33035=DIRECTION('center_axis',(0.,0.,1.));
#33036=DIRECTION('ref_axis',(1.,0.,0.));
#33037=DIRECTION('center_axis',(0.,0.,1.));
#33038=DIRECTION('ref_axis',(1.,0.,0.));
#33039=DIRECTION('center_axis',(0.,0.,1.));
#33040=DIRECTION('ref_axis',(1.,0.,0.));
#33041=DIRECTION('center_axis',(0.,0.,1.));
#33042=DIRECTION('ref_axis',(1.,0.,0.));
#33043=DIRECTION('center_axis',(0.,0.,1.));
#33044=DIRECTION('ref_axis',(1.,0.,0.));
#33045=DIRECTION('center_axis',(0.,0.,1.));
#33046=DIRECTION('ref_axis',(1.,0.,0.));
#33047=DIRECTION('center_axis',(0.,0.,1.));
#33048=DIRECTION('ref_axis',(1.,0.,0.));
#33049=DIRECTION('center_axis',(0.,0.,1.));
#33050=DIRECTION('ref_axis',(1.,0.,0.));
#33051=DIRECTION('center_axis',(0.,0.,1.));
#33052=DIRECTION('ref_axis',(1.,0.,0.));
#33053=DIRECTION('center_axis',(0.,0.,1.));
#33054=DIRECTION('ref_axis',(1.,0.,0.));
#33055=DIRECTION('center_axis',(0.,0.,1.));
#33056=DIRECTION('ref_axis',(1.,0.,0.));
#33057=DIRECTION('center_axis',(0.,0.,1.));
#33058=DIRECTION('ref_axis',(1.,0.,0.));
#33059=DIRECTION('center_axis',(0.,0.,1.));
#33060=DIRECTION('ref_axis',(1.,0.,0.));
#33061=DIRECTION('center_axis',(0.,0.,1.));
#33062=DIRECTION('ref_axis',(1.,0.,0.));
#33063=DIRECTION('center_axis',(0.,0.,1.));
#33064=DIRECTION('ref_axis',(1.,0.,0.));
#33065=DIRECTION('center_axis',(0.,0.,1.));
#33066=DIRECTION('ref_axis',(1.,0.,0.));
#33067=DIRECTION('center_axis',(0.,0.,1.));
#33068=DIRECTION('ref_axis',(1.,0.,0.));
#33069=DIRECTION('',(0.,0.,-1.));
#33070=DIRECTION('center_axis',(0.,0.,1.));
#33071=DIRECTION('ref_axis',(1.,0.,0.));
#33072=DIRECTION('center_axis',(0.,0.,1.));
#33073=DIRECTION('ref_axis',(1.,0.,0.));
#33074=DIRECTION('center_axis',(0.,0.,1.));
#33075=DIRECTION('ref_axis',(1.,0.,0.));
#33076=DIRECTION('center_axis',(0.,0.,1.));
#33077=DIRECTION('ref_axis',(1.,0.,0.));
#33078=DIRECTION('center_axis',(0.,0.,1.));
#33079=DIRECTION('ref_axis',(1.,0.,0.));
#33080=DIRECTION('center_axis',(0.,0.,1.));
#33081=DIRECTION('ref_axis',(1.,0.,0.));
#33082=DIRECTION('center_axis',(0.,0.,1.));
#33083=DIRECTION('ref_axis',(1.,0.,0.));
#33084=DIRECTION('center_axis',(0.,0.,1.));
#33085=DIRECTION('ref_axis',(1.,0.,0.));
#33086=DIRECTION('center_axis',(0.,0.,1.));
#33087=DIRECTION('ref_axis',(1.,0.,0.));
#33088=DIRECTION('center_axis',(0.,0.,1.));
#33089=DIRECTION('ref_axis',(1.,0.,0.));
#33090=DIRECTION('center_axis',(0.,0.,1.));
#33091=DIRECTION('ref_axis',(1.,0.,0.));
#33092=DIRECTION('center_axis',(0.,0.,1.));
#33093=DIRECTION('ref_axis',(1.,0.,0.));
#33094=DIRECTION('center_axis',(0.,0.,1.));
#33095=DIRECTION('ref_axis',(1.,0.,0.));
#33096=DIRECTION('center_axis',(0.,0.,1.));
#33097=DIRECTION('ref_axis',(1.,0.,0.));
#33098=DIRECTION('center_axis',(0.,0.,1.));
#33099=DIRECTION('ref_axis',(1.,0.,0.));
#33100=DIRECTION('center_axis',(0.,0.,1.));
#33101=DIRECTION('ref_axis',(1.,0.,0.));
#33102=DIRECTION('center_axis',(0.,0.,1.));
#33103=DIRECTION('ref_axis',(1.,0.,0.));
#33104=DIRECTION('center_axis',(0.,0.,1.));
#33105=DIRECTION('ref_axis',(1.,0.,0.));
#33106=DIRECTION('center_axis',(0.,0.,1.));
#33107=DIRECTION('ref_axis',(1.,0.,0.));
#33108=DIRECTION('center_axis',(0.,0.,1.));
#33109=DIRECTION('ref_axis',(1.,0.,0.));
#33110=DIRECTION('center_axis',(0.,0.,-1.));
#33111=DIRECTION('ref_axis',(1.,0.,0.));
#33112=DIRECTION('center_axis',(0.,0.,1.));
#33113=DIRECTION('ref_axis',(1.,0.,0.));
#33114=DIRECTION('',(-0.707106781186548,-8.65956056235493E-17,-0.707106781186547));
#33115=DIRECTION('center_axis',(0.,0.,1.));
#33116=DIRECTION('ref_axis',(1.,0.,0.));
#50311=CARTESIAN_POINT('',(0.,0.,0.));
#50312=CARTESIAN_POINT('Origin',(0.,0.,-0.975));
#50313=CARTESIAN_POINT('',(-0.393684988231328,0.000287216083460287,-1.9162836477965));
#50314=CARTESIAN_POINT('',(-0.393656552223556,0.000403437008091592,-1.9346163522035));
#50315=CARTESIAN_POINT('',(-0.3933,-4.81653586104654E-17,-0.975));
#50316=CARTESIAN_POINT('',(0.175074362083496,0.352527701706987,-1.9567));
#50317=CARTESIAN_POINT('Ctrl Pts',(-0.393684988231328,0.000287216083460287,
-1.9162836477965));
#50318=CARTESIAN_POINT('Ctrl Pts',(-0.393812206257712,0.016808807481143,
-1.91712178211581));
#50319=CARTESIAN_POINT('Ctrl Pts',(-0.392861270962247,0.0333148644649716,
-1.91795991643512));
#50320=CARTESIAN_POINT('Ctrl Pts',(-0.390782425694577,0.0496765903311048,
-1.91879805075443));
#50321=CARTESIAN_POINT('Ctrl Pts',(-0.37447258502525,0.178044557924503,
-1.92537373843066));
#50322=CARTESIAN_POINT('Ctrl Pts',(-0.288735561555079,0.297528391908798,
-1.93194942610689));
#50323=CARTESIAN_POINT('Ctrl Pts',(-0.172352287678191,0.354187200525085,
-1.93852511378312));
#50324=CARTESIAN_POINT('Ctrl Pts',(-0.0651263535802379,0.406387946185369,
-1.94458340918875));
#50325=CARTESIAN_POINT('Ctrl Pts',(0.0681129064719315,0.405261193659393,
-1.95064170459437));
#50326=CARTESIAN_POINT('Ctrl Pts',(0.175279276633879,0.352769203968886,
-1.9567));
#50327=CARTESIAN_POINT('',(-0.17486944753311,0.352286199445089,-1.9567));
#50328=CARTESIAN_POINT('Origin',(0.,0.,-1.9567));
#50329=CARTESIAN_POINT('Ctrl Pts',(-0.17486944753311,0.352286199445089,
-1.9567));
#50330=CARTESIAN_POINT('Ctrl Pts',(-0.291310645032561,0.294486581098141,
-1.95012431232377));
#50331=CARTESIAN_POINT('Ctrl Pts',(-0.375888601233118,0.174960586654857,
-1.94354862464754));
#50332=CARTESIAN_POINT('Ctrl Pts',(-0.391123834940899,0.0466546186985258,
-1.93697293697131));
#50333=CARTESIAN_POINT('Ctrl Pts',(-0.392943828096371,0.0313272539881675,
-1.93618740871537));
#50334=CARTESIAN_POINT('Ctrl Pts',(-0.393774261195228,0.0158745940662237,
-1.93540188045944));
#50335=CARTESIAN_POINT('Ctrl Pts',(-0.393656552223556,0.000403437008091592,
-1.9346163522035));
#50336=CARTESIAN_POINT('Origin',(0.,0.,-0.975));
#50337=CARTESIAN_POINT('',(-0.392686056089118,7.50994904183955E-5,-1.7912836477965));
#50338=CARTESIAN_POINT('',(-0.392691811994703,9.34764795687181E-5,-1.8096163522035));
#50339=CARTESIAN_POINT('',(-0.3933,-4.81653586104654E-17,-0.975));
#50340=CARTESIAN_POINT('Ctrl Pts',(-0.392686056089118,7.50994904183955E-5,
-1.7912836477965));
#50341=CARTESIAN_POINT('Ctrl Pts',(-0.392790040690049,0.0606067827725276,
-1.79433432272509));
#50342=CARTESIAN_POINT('Ctrl Pts',(-0.379632353738202,0.121095544704464,
-1.79738499765368));
#50343=CARTESIAN_POINT('Ctrl Pts',(-0.352975241504574,0.174895223853803,
-1.80043567258227));
#50344=CARTESIAN_POINT('Ctrl Pts',(-0.295516204241772,0.290859689242099,
-1.8070113602585));
#50345=CARTESIAN_POINT('Ctrl Pts',(-0.17533720758107,0.375745868571807,
-1.81358704793474));
#50346=CARTESIAN_POINT('Ctrl Pts',(-0.0468355728346856,0.391133692962758,
-1.82016273561097));
#50347=CARTESIAN_POINT('Ctrl Pts',(0.0816660619116985,0.406521517353708,
-1.8267384232872));
#50348=CARTESIAN_POINT('Ctrl Pts',(0.218490334743764,0.3524109868059,-1.83331411096343));
#50349=CARTESIAN_POINT('Ctrl Pts',(0.301704002577892,0.253289260265722,
-1.83988979863966));
#50350=CARTESIAN_POINT('Ctrl Pts',(0.384917670412021,0.154167533725544,
-1.84646548631589));
#50351=CARTESIAN_POINT('Ctrl Pts',(0.414520733248213,0.0100346111929961,
-1.85304117399212));
#50352=CARTESIAN_POINT('Ctrl Pts',(0.377115660733795,-0.11385867192349,
-1.85961686166835));
#50353=CARTESIAN_POINT('Ctrl Pts',(0.339710588219377,-0.237751955039975,
-1.86619254934458));
#50354=CARTESIAN_POINT('Ctrl Pts',(0.235297380354349,-0.341405598740398,
-1.87276823702081));
#50355=CARTESIAN_POINT('Ctrl Pts',(0.111133817323469,-0.377921810128355,
-1.87934392469704));
#50356=CARTESIAN_POINT('Ctrl Pts',(-0.0130297457074104,-0.414438021516312,
-1.88591961237327));
#50357=CARTESIAN_POINT('Ctrl Pts',(-0.156943663904142,-0.383816800591803,
-1.8924953000495));
#50358=CARTESIAN_POINT('Ctrl Pts',(-0.255459294068266,-0.299880139528298,
-1.89907098772573));
#50359=CARTESIAN_POINT('Ctrl Pts',(-0.341418164438697,-0.226642009135542,
-1.90480854108266));
#50360=CARTESIAN_POINT('Ctrl Pts',(-0.392814101313171,-0.112813405143687,
-1.91054609443958));
#50361=CARTESIAN_POINT('Ctrl Pts',(-0.393684988231328,0.000287216083460287,
-1.9162836477965));
#50362=CARTESIAN_POINT('Ctrl Pts',(-0.393656552223556,0.000403437008091592,
-1.9346163522035));
#50363=CARTESIAN_POINT('Ctrl Pts',(-0.392788914801179,-0.11363506524309,
-1.9288261927832));
#50364=CARTESIAN_POINT('Ctrl Pts',(-0.340406617480196,-0.228678557895452,
-1.92303603336291));
#50365=CARTESIAN_POINT('Ctrl Pts',(-0.253096937644416,-0.301956026031023,
-1.91724587394262));
#50366=CARTESIAN_POINT('Ctrl Pts',(-0.153942295425146,-0.385174761334857,
-1.91067018626639));
#50367=CARTESIAN_POINT('Ctrl Pts',(-0.00974049977160341,-0.414526290473145,
-1.90409449859016));
#50368=CARTESIAN_POINT('Ctrl Pts',(0.114141367823281,-0.37699543192958,
-1.89751881091392));
#50369=CARTESIAN_POINT('Ctrl Pts',(0.238023235418165,-0.339464573386015,
-1.89094312323769));
#50370=CARTESIAN_POINT('Ctrl Pts',(0.341585174954392,-0.235051327160598,
-1.88436743556146));
#50371=CARTESIAN_POINT('Ctrl Pts',(0.378000101690373,-0.110880914803365,
-1.87779174788523));
#50372=CARTESIAN_POINT('Ctrl Pts',(0.414415028426353,0.0132894975538674,
-1.871216060209));
#50373=CARTESIAN_POINT('Ctrl Pts',(0.383682942362089,0.157217076042915,
-1.86464037253277));
#50374=CARTESIAN_POINT('Ctrl Pts',(0.2996888006567,0.255683706134081,-1.85806468485654));
#50375=CARTESIAN_POINT('Ctrl Pts',(0.21569465895131,0.354150336225248,-1.85148899718031));
#50376=CARTESIAN_POINT('Ctrl Pts',(0.0784384616047951,0.407156017918534,
-1.84491330950408));
#50377=CARTESIAN_POINT('Ctrl Pts',(-0.0499387246305632,0.390745066784524,
-1.83833762182785));
#50378=CARTESIAN_POINT('Ctrl Pts',(-0.178315910865922,0.374334115650513,
-1.83176193415162));
#50379=CARTESIAN_POINT('Ctrl Pts',(-0.297814085990123,0.288506531689206,
-1.82518624647539));
#50380=CARTESIAN_POINT('Ctrl Pts',(-0.354350523610512,0.172092132577462,
-1.81861055879916));
#50381=CARTESIAN_POINT('Ctrl Pts',(-0.380127315594231,0.119015039712826,
-1.81561248993394));
#50382=CARTESIAN_POINT('Ctrl Pts',(-0.392815978841773,0.0595797332697563,
-1.81261442106872));
#50383=CARTESIAN_POINT('Ctrl Pts',(-0.392691811994703,9.34764795687181E-5,
-1.8096163522035));
#50384=CARTESIAN_POINT('Origin',(0.,0.,-0.975));
#50385=CARTESIAN_POINT('',(-0.393429058327419,-0.000336684366980755,-1.6662836477965));
#50386=CARTESIAN_POINT('',(-0.393398187730971,-0.000340795866165029,-1.6846163522035));
#50387=CARTESIAN_POINT('',(-0.3933,-4.81653586104654E-17,-0.975));
#50388=CARTESIAN_POINT('Ctrl Pts',(-0.393429058327419,-0.000336684366980755,
-1.6662836477965));
#50389=CARTESIAN_POINT('Ctrl Pts',(-0.392492058309276,0.103596594079765,
-1.67154686333438));
#50390=CARTESIAN_POINT('Ctrl Pts',(-0.350086285532408,0.208206253664161,
-1.67681007887225));
#50391=CARTESIAN_POINT('Ctrl Pts',(-0.276234805241032,0.280845339194954,
-1.68207329441012));
#50392=CARTESIAN_POINT('Ctrl Pts',(-0.183967204697426,0.371598213763818,
-1.68864898208635));
#50393=CARTESIAN_POINT('Ctrl Pts',(-0.0426154383454463,0.412447648980525,
-1.69522466976258));
#50394=CARTESIAN_POINT('Ctrl Pts',(0.0838389849720331,0.384903597594179,
-1.70180035743881));
#50395=CARTESIAN_POINT('Ctrl Pts',(0.210293408289513,0.357359546207833,
-1.70837604511505));
#50396=CARTESIAN_POINT('Ctrl Pts',(0.321850488572492,0.261422008218435,
-1.71495173279128));
#50397=CARTESIAN_POINT('Ctrl Pts',(0.368014963339217,0.140516079073615,
-1.72152742046751));
#50398=CARTESIAN_POINT('Ctrl Pts',(0.414179438105941,0.0196101499287949,
-1.72810310814374));
#50399=CARTESIAN_POINT('Ctrl Pts',(0.394951307356412,-0.126264170371447,
-1.73467879581997));
#50400=CARTESIAN_POINT('Ctrl Pts',(0.319034040445492,-0.231078060471686,
-1.7412544834962));
#50401=CARTESIAN_POINT('Ctrl Pts',(0.243116773534572,-0.335891950571925,
-1.74783017117243));
#50402=CARTESIAN_POINT('Ctrl Pts',(0.110510370462263,-0.399645410472161,
-1.75440585884866));
#50403=CARTESIAN_POINT('Ctrl Pts',(-0.0187622313884131,-0.393481452764923,
-1.76098154652489));
#50404=CARTESIAN_POINT('Ctrl Pts',(-0.148034833239089,-0.387317495057686,
-1.76755723420112));
#50405=CARTESIAN_POINT('Ctrl Pts',(-0.273973633868132,-0.311236119742974,
-1.77413292187735));
#50406=CARTESIAN_POINT('Ctrl Pts',(-0.339573495250203,-0.199674056362176,
-1.78070860955358));
#50407=CARTESIAN_POINT('Ctrl Pts',(-0.374739451877235,-0.139869254958381,
-1.78423362230122));
#50408=CARTESIAN_POINT('Ctrl Pts',(-0.392565903318857,-0.0698684245494068,
-1.78775863504886));
#50409=CARTESIAN_POINT('Ctrl Pts',(-0.392686056089118,7.50994904183955E-5,
-1.7912836477965));
#50410=CARTESIAN_POINT('Ctrl Pts',(-0.392691811994703,9.34764795687181E-5,
-1.8096163522035));
#50411=CARTESIAN_POINT('Ctrl Pts',(-0.392543642733838,-0.0708919347490211,
-1.80603873339249));
#50412=CARTESIAN_POINT('Ctrl Pts',(-0.374150216296977,-0.141949898425392,
-1.80246111458148));
#50413=CARTESIAN_POINT('Ctrl Pts',(-0.3379793340135,-0.202362794921726,
-1.79888349577047));
#50414=CARTESIAN_POINT('Ctrl Pts',(-0.271497006679522,-0.31340210904699,
-1.79230780809423));
#50415=CARTESIAN_POINT('Ctrl Pts',(-0.144957651894991,-0.388479523035339,
-1.785732120418));
#50416=CARTESIAN_POINT('Ctrl Pts',(-0.0156399934846813,-0.393617199251612,
-1.77915643274177));
#50417=CARTESIAN_POINT('Ctrl Pts',(0.113677664925628,-0.398754875467886,
-1.77258074506554));
#50418=CARTESIAN_POINT('Ctrl Pts',(0.245773626961716,-0.333952813912084,
-1.76600505738931));
#50419=CARTESIAN_POINT('Ctrl Pts',(0.320856915188691,-0.228540314522024,
-1.75942936971308));
#50420=CARTESIAN_POINT('Ctrl Pts',(0.395940203415666,-0.123127815131962,
-1.75285368203685));
#50421=CARTESIAN_POINT('Ctrl Pts',(0.414010817833527,0.0228951220923579,
-1.74627799436062));
#50422=CARTESIAN_POINT('Ctrl Pts',(0.366888750868655,0.143431191298164,
-1.73970230668439));
#50423=CARTESIAN_POINT('Ctrl Pts',(0.319766683903784,0.263967260503969,
-1.73312661900816));
#50424=CARTESIAN_POINT('Ctrl Pts',(0.207451935556179,0.35901646169126,-1.72655093133193));
#50425=CARTESIAN_POINT('Ctrl Pts',(0.0807829683652689,0.385556430393323,
-1.7199752436557));
#50426=CARTESIAN_POINT('Ctrl Pts',(-0.0458859988256416,0.412096399095387,
-1.71339955597947));
#50427=CARTESIAN_POINT('Ctrl Pts',(-0.186909184859858,0.370127135312224,
-1.70682386830324));
#50428=CARTESIAN_POINT('Ctrl Pts',(-0.278453939513988,0.278645235121949,
-1.700248180627));
#50429=CARTESIAN_POINT('Ctrl Pts',(-0.350994484233901,0.20615449660954,
-1.6950375711525));
#50430=CARTESIAN_POINT('Ctrl Pts',(-0.392467220602993,0.102574472201558,
-1.689826961678));
#50431=CARTESIAN_POINT('Ctrl Pts',(-0.393398187730971,-0.000340795866165029,
-1.6846163522035));
#50432=CARTESIAN_POINT('Origin',(0.,0.,-0.975));
#50433=CARTESIAN_POINT('',(-0.393658757357236,0.000274916615761227,-1.5412836477965));
#50434=CARTESIAN_POINT('',(-0.393685317967325,0.000263450781192951,-1.5596163522035));
#50435=CARTESIAN_POINT('',(-0.3933,-4.81653586104654E-17,-0.975));
#50436=CARTESIAN_POINT('Ctrl Pts',(-0.393658757357236,0.000274916615761227,
-1.5412836477965));
#50437=CARTESIAN_POINT('Ctrl Pts',(-0.393800352394406,0.0180217662467705,
-1.54218371626743));
#50438=CARTESIAN_POINT('Ctrl Pts',(-0.392702743301847,0.0357510060110471,
-1.54308378473835));
#50439=CARTESIAN_POINT('Ctrl Pts',(-0.390305752494891,0.0533027934246246,
-1.54398385320928));
#50440=CARTESIAN_POINT('Ctrl Pts',(-0.372793903765057,0.181532007000592,
-1.55055954088551));
#50441=CARTESIAN_POINT('Ctrl Pts',(-0.285928614910863,0.300289845966023,
-1.55713522856174));
#50442=CARTESIAN_POINT('Ctrl Pts',(-0.169028625036337,0.355821714128369,
-1.56371091623797));
#50443=CARTESIAN_POINT('Ctrl Pts',(-0.0521286351618115,0.411353582290715,
-1.5702866039142));
#50444=CARTESIAN_POINT('Ctrl Pts',(0.0948060557330462,0.403659479649976,
-1.57686229159043));
#50445=CARTESIAN_POINT('Ctrl Pts',(0.205266870788755,0.336222069051615,
-1.58343797926666));
#50446=CARTESIAN_POINT('Ctrl Pts',(0.315727685844463,0.268784658453253,
-1.59001366694289));
#50447=CARTESIAN_POINT('Ctrl Pts',(0.389714625061023,0.141603939897268,
-1.59658935461912));
#50448=CARTESIAN_POINT('Ctrl Pts',(0.393738210339229,0.0122470423297462,
-1.60316504229535));
#50449=CARTESIAN_POINT('Ctrl Pts',(0.397761795617435,-0.117109855237775,
-1.60974072997159));
#50450=CARTESIAN_POINT('Ctrl Pts',(0.331822026957288,-0.248642931816833,
-1.61631641764782));
#50451=CARTESIAN_POINT('Ctrl Pts',(0.225765908359775,-0.322814998917635,
-1.62289210532405));
#50452=CARTESIAN_POINT('Ctrl Pts',(0.119709789762263,-0.396987066018437,
-1.62946779300028));
#50453=CARTESIAN_POINT('Ctrl Pts',(-0.0264626787726145,-0.413798123640983,
-1.63604348067651));
#50454=CARTESIAN_POINT('Ctrl Pts',(-0.146587934364655,-0.365638816110993,
-1.64261916835274));
#50455=CARTESIAN_POINT('Ctrl Pts',(-0.266713189956696,-0.317479508581004,
-1.64919485602897));
#50456=CARTESIAN_POINT('Ctrl Pts',(-0.3607912326059,-0.204349835898478,
-1.6557705437052));
#50457=CARTESIAN_POINT('Ctrl Pts',(-0.386238536562886,-0.0774568425967047,
-1.66234623138143));
#50458=CARTESIAN_POINT('Ctrl Pts',(-0.391317682514508,-0.0521296788898022,
-1.66365870351979));
#50459=CARTESIAN_POINT('Ctrl Pts',(-0.39366271518768,-0.0262542116329496,
-1.66497117565815));
#50460=CARTESIAN_POINT('Ctrl Pts',(-0.393429058327419,-0.000336684366980755,
-1.6662836477965));
#50461=CARTESIAN_POINT('Ctrl Pts',(-0.393398187730971,-0.000340795866165029,
-1.6846163522035));
#50462=CARTESIAN_POINT('Ctrl Pts',(-0.393642082987207,-0.0273025917466196,
-1.68325127400177));
#50463=CARTESIAN_POINT('Ctrl Pts',(-0.391103442761171,-0.0542187628766391,
-1.68188619580004));
#50464=CARTESIAN_POINT('Ctrl Pts',(-0.385611918437396,-0.0805183487896309,
-1.68052111759831));
#50465=CARTESIAN_POINT('Ctrl Pts',(-0.35915881943263,-0.20720549591355,
-1.67394542992208));
#50466=CARTESIAN_POINT('Ctrl Pts',(-0.264186298149056,-0.319585253564002,
-1.66736974224585));
#50467=CARTESIAN_POINT('Ctrl Pts',(-0.143682792882962,-0.366790109162457,
-1.66079405456962));
#50468=CARTESIAN_POINT('Ctrl Pts',(-0.0231792876168675,-0.413994964760912,
-1.65421836689339));
#50469=CARTESIAN_POINT('Ctrl Pts',(0.122855201631747,-0.39602491830737,
-1.64764267921716));
#50470=CARTESIAN_POINT('Ctrl Pts',(0.228319585447469,-0.321013883609743,
-1.64106699154093));
#50471=CARTESIAN_POINT('Ctrl Pts',(0.333783969263191,-0.246002848912117,
-1.6344913038647));
#50472=CARTESIAN_POINT('Ctrl Pts',(0.39867824764602,-0.113950825970406,
-1.62791561618847));
#50473=CARTESIAN_POINT('Ctrl Pts',(0.393628638093698,0.0153700760896384,
-1.62133992851224));
#50474=CARTESIAN_POINT('Ctrl Pts',(0.388579028541375,0.144690978149683,
-1.61476424083601));
#50475=CARTESIAN_POINT('Ctrl Pts',(0.313585531053901,0.271280759328061,
-1.60818855315978));
#50476=CARTESIAN_POINT('Ctrl Pts',(0.202593237697407,0.337839785620704,
-1.60161286548355));
#50477=CARTESIAN_POINT('Ctrl Pts',(0.0916009443409129,0.404398811913346,
-1.59503717780731));
#50478=CARTESIAN_POINT('Ctrl Pts',(-0.0553901448846022,0.410927083320253,
-1.58846149013108));
#50479=CARTESIAN_POINT('Ctrl Pts',(-0.171845927581847,0.354469632623865,
-1.58188580245485));
#50480=CARTESIAN_POINT('Ctrl Pts',(-0.288301710279093,0.298012181927477,
-1.57531011477862));
#50481=CARTESIAN_POINT('Ctrl Pts',(-0.374222186448069,0.178569009127795,
-1.56873442710239));
#50482=CARTESIAN_POINT('Ctrl Pts',(-0.390716276005324,0.0502049236873175,
-1.56215873942616));
#50483=CARTESIAN_POINT('Ctrl Pts',(-0.392842003615096,0.0336615989056209,
-1.56131127701861));
#50484=CARTESIAN_POINT('Ctrl Pts',(-0.393814588422652,0.0169701015529035,
-1.56046381461105));
#50485=CARTESIAN_POINT('Ctrl Pts',(-0.393685317967325,0.000263450781192951,
-1.5596163522035));
#50486=CARTESIAN_POINT('Origin',(0.,0.,-0.975));
#50487=CARTESIAN_POINT('',(-0.392680002949509,5.54103040254772E-5,-1.4162836477965));
#50488=CARTESIAN_POINT('',(-0.39268505468958,7.18397355967851E-5,-1.4346163522035));
#50489=CARTESIAN_POINT('',(-0.3933,-4.81653586104654E-17,-0.975));
#50490=CARTESIAN_POINT('Ctrl Pts',(-0.392680002949509,5.54103040254772E-5,
-1.4162836477965));
#50491=CARTESIAN_POINT('Ctrl Pts',(-0.392758615348053,0.0618182368767579,
-1.41939625687671));
#50492=CARTESIAN_POINT('Ctrl Pts',(-0.379036335622443,0.123548029294639,
-1.42250886595692));
#50493=CARTESIAN_POINT('Ctrl Pts',(-0.351326532985881,0.178183712592334,
-1.42562147503713));
#50494=CARTESIAN_POINT('Ctrl Pts',(-0.292786895333777,0.293606876916932,
-1.43219716271336));
#50495=CARTESIAN_POINT('Ctrl Pts',(-0.171820036208097,0.37736857237224,
-1.43877285038959));
#50496=CARTESIAN_POINT('Ctrl Pts',(-0.043180442965895,0.391554871712072,
-1.44534853806582));
#50497=CARTESIAN_POINT('Ctrl Pts',(0.0854591502763071,0.405741171051904,
-1.45192422574205));
#50498=CARTESIAN_POINT('Ctrl Pts',(0.221771477635032,0.35035207427626,-1.45849991341828));
#50499=CARTESIAN_POINT('Ctrl Pts',(0.304056072899483,0.250458924261499,
-1.46507560109451));
#50500=CARTESIAN_POINT('Ctrl Pts',(0.386340668163933,0.150565774246737,
-1.47165128877074));
#50501=CARTESIAN_POINT('Ctrl Pts',(0.414597531334111,0.00616857099285846,
-1.47822697644697));
#50502=CARTESIAN_POINT('Ctrl Pts',(0.376036464587567,-0.117372677880283,
-1.4848026641232));
#50503=CARTESIAN_POINT('Ctrl Pts',(0.337475397841023,-0.240913926753425,
-1.49137835179943));
#50504=CARTESIAN_POINT('Ctrl Pts',(0.232096401177758,-0.34359922124583,
-1.49795403947566));
#50505=CARTESIAN_POINT('Ctrl Pts',(0.107598265687765,-0.378949048623052,
-1.50452972715189));
#50506=CARTESIAN_POINT('Ctrl Pts',(-0.0168998698022284,-0.414298876000273,
-1.51110541482813));
#50507=CARTESIAN_POINT('Ctrl Pts',(-0.16051714411895,-0.382313236262312,
-1.51768110250436));
#50508=CARTESIAN_POINT('Ctrl Pts',(-0.258246576974574,-0.297470122300079,
-1.52425679018059));
#50509=CARTESIAN_POINT('Ctrl Pts',(-0.342598978327816,-0.22424018335657,
-1.52993240938589));
#50510=CARTESIAN_POINT('Ctrl Pts',(-0.392765892493847,-0.11163252582122,
-1.5356080285912));
#50511=CARTESIAN_POINT('Ctrl Pts',(-0.393658757357236,0.000274916615761227,
-1.5412836477965));
#50512=CARTESIAN_POINT('Ctrl Pts',(-0.393685317967325,0.000263450781192951,
-1.5596163522035));
#50513=CARTESIAN_POINT('Ctrl Pts',(-0.392811544355544,-0.112661273964597,
-1.55388812693482));
#50514=CARTESIAN_POINT('Ctrl Pts',(-0.341596538395714,-0.22627832356657,
-1.54815990166615));
#50515=CARTESIAN_POINT('Ctrl Pts',(-0.255878681665093,-0.299509336414108,
-1.54243167639747));
#50516=CARTESIAN_POINT('Ctrl Pts',(-0.157479294822075,-0.383574512993783,
-1.53585598872124));
#50517=CARTESIAN_POINT('Ctrl Pts',(-0.0136128181905055,-0.41441986807186,
-1.52928030104501));
#50518=CARTESIAN_POINT('Ctrl Pts',(0.110600969279798,-0.37808354670996,
-1.52270461336878));
#50519=CARTESIAN_POINT('Ctrl Pts',(0.234814756750101,-0.34174722534806,
-1.51612892569255));
#50520=CARTESIAN_POINT('Ctrl Pts',(0.339375855059138,-0.238229227546182,
-1.50955323801632));
#50521=CARTESIAN_POINT('Ctrl Pts',(0.376955686759376,-0.114385981693005,
-1.50297755034009));
#50522=CARTESIAN_POINT('Ctrl Pts',(0.414535518459615,0.0094572641601714,
-1.49640186266386));
#50523=CARTESIAN_POINT('Ctrl Pts',(0.385134083551055,0.153625758064647,
-1.48982617498762));
#50524=CARTESIAN_POINT('Ctrl Pts',(0.302059659365895,0.252863015750642,
-1.48325048731139));
#50525=CARTESIAN_POINT('Ctrl Pts',(0.218985235180735,0.352100273436638,
-1.47667479963516));
#50526=CARTESIAN_POINT('Ctrl Pts',(0.0822378217189762,0.406406294904155,
-1.47009911195893));
#50527=CARTESIAN_POINT('Ctrl Pts',(-0.0462851773144539,0.391199980781066,
-1.4635234242827));
#50528=CARTESIAN_POINT('Ctrl Pts',(-0.174808176347883,0.375993666657979,
-1.45694773660647));
#50529=CARTESIAN_POINT('Ctrl Pts',(-0.295106760952984,0.291275016944286,
-1.45037204893024));
#50530=CARTESIAN_POINT('Ctrl Pts',(-0.352728931790508,0.175391115113851,
-1.44379636125401));
#50531=CARTESIAN_POINT('Ctrl Pts',(-0.379543468198143,0.121464422323106,
-1.44073635823717));
#50532=CARTESIAN_POINT('Ctrl Pts',(-0.392785328249549,0.0607888449821143,
-1.43767635522034));
#50533=CARTESIAN_POINT('Ctrl Pts',(-0.39268505468958,7.18397355967851E-5,
-1.4346163522035));
#50534=CARTESIAN_POINT('Origin',(0.,0.,-0.975));
#50535=CARTESIAN_POINT('',(-0.393465141926397,-0.00033072980931359,-1.2912836477965));
#50536=CARTESIAN_POINT('',(-0.393434478492496,-0.000335863925950309,-1.3096163522035));
#50537=CARTESIAN_POINT('',(-0.3933,-4.81653586104654E-17,-0.975));
#50538=CARTESIAN_POINT('Ctrl Pts',(-0.393465141926397,-0.00033072980931359,
-1.2912836477965));
#50539=CARTESIAN_POINT('Ctrl Pts',(-0.392524065374241,0.104800679194081,
-1.29660879748599));
#50540=CARTESIAN_POINT('Ctrl Pts',(-0.349003498856052,0.210620107401743,
-1.30193394717549));
#50541=CARTESIAN_POINT('Ctrl Pts',(-0.273599856866439,0.283412925845174,
-1.30725909686498));
#50542=CARTESIAN_POINT('Ctrl Pts',(-0.180488709145554,0.373300134105479,
-1.31383478454121));
#50543=CARTESIAN_POINT('Ctrl Pts',(-0.0387615952056478,0.412827691645586,
-1.32041047221744));
#50544=CARTESIAN_POINT('Ctrl Pts',(0.0874300675804848,0.384103829057202,
-1.32698615989367));
#50545=CARTESIAN_POINT('Ctrl Pts',(0.213621730366617,0.355379966468818,
-1.3335618475699));
#50546=CARTESIAN_POINT('Ctrl Pts',(0.324277941998977,0.258404683751943,
-1.34013753524613));
#50547=CARTESIAN_POINT('Ctrl Pts',(0.369311230716079,0.137072911548536,
-1.34671322292236));
#50548=CARTESIAN_POINT('Ctrl Pts',(0.414344519433181,0.0157411393451306,
-1.35328891059859));
#50549=CARTESIAN_POINT('Ctrl Pts',(0.393754885235027,-0.129947122344807,
-1.35986459827482));
#50550=CARTESIAN_POINT('Ctrl Pts',(0.316862028355783,-0.234047480652203,
-1.36644028595105));
#50551=CARTESIAN_POINT('Ctrl Pts',(0.239969171476537,-0.338147838959601,
-1.37301597362728));
#50552=CARTESIAN_POINT('Ctrl Pts',(0.106773091916198,-0.400660293884456,
-1.37959166130351));
#50553=CARTESIAN_POINT('Ctrl Pts',(-0.0224362837557882,-0.393289182898671,
-1.38616734897974));
#50554=CARTESIAN_POINT('Ctrl Pts',(-0.151645659427774,-0.385918071912887,
-1.39274303665597));
#50555=CARTESIAN_POINT('Ctrl Pts',(-0.276868331211408,-0.308663395016463,
-1.3993187243322));
#50556=CARTESIAN_POINT('Ctrl Pts',(-0.341423459013961,-0.196493739971308,
-1.40589441200844));
#50557=CARTESIAN_POINT('Ctrl Pts',(-0.375421345222065,-0.137419715985304,
-1.40935749060446));
#50558=CARTESIAN_POINT('Ctrl Pts',(-0.392592539054185,-0.0686617068225455,
-1.41282056920048));
#50559=CARTESIAN_POINT('Ctrl Pts',(-0.392680002949509,5.54103040254772E-5,
-1.4162836477965));
#50560=CARTESIAN_POINT('Ctrl Pts',(-0.39268505468958,7.18397355967851E-5,
-1.4346163522035));
#50561=CARTESIAN_POINT('Ctrl Pts',(-0.392569848850048,-0.0696868640091281,
-1.43110066754411));
#50562=CARTESIAN_POINT('Ctrl Pts',(-0.374842937939681,-0.139500252864576,
-1.42758498288471));
#50563=CARTESIAN_POINT('Ctrl Pts',(-0.339853957551454,-0.199195959086854,
-1.42406929822532));
#50564=CARTESIAN_POINT('Ctrl Pts',(-0.274411055404927,-0.310849977509947,
-1.41749361054909));
#50565=CARTESIAN_POINT('Ctrl Pts',(-0.148579494041927,-0.387108860408956,
-1.41091792287286));
#50566=CARTESIAN_POINT('Ctrl Pts',(-0.0193157215696609,-0.39345475659486,
-1.40434223519663));
#50567=CARTESIAN_POINT('Ctrl Pts',(0.109948050902604,-0.399800652780763,
-1.3977665475204));
#50568=CARTESIAN_POINT('Ctrl Pts',(0.242644034484135,-0.33623356225356,
-1.39119085984416));
#50569=CARTESIAN_POINT('Ctrl Pts',(0.318708666244829,-0.231526518231,-1.38461517216793));
#50570=CARTESIAN_POINT('Ctrl Pts',(0.394773298005524,-0.126819474208439,
-1.3780394844917));
#50571=CARTESIAN_POINT('Ctrl Pts',(0.414206577945384,0.0190275233094804,
-1.37146379681547));
#50572=CARTESIAN_POINT('Ctrl Pts',(0.368212218484911,0.139998231210439,
-1.36488810913924));
#50573=CARTESIAN_POINT('Ctrl Pts',(0.322217859024438,0.260968939111397,
-1.35831242146301));
#50574=CARTESIAN_POINT('Ctrl Pts',(0.210795860163633,0.357063357395395,
-1.35173673378678));
#50575=CARTESIAN_POINT('Ctrl Pts',(0.0843803198993765,0.384785270245916,
-1.34516104611055));
#50576=CARTESIAN_POINT('Ctrl Pts',(-0.0420352203648793,0.412507183096438,
-1.33858535843432));
#50577=CARTESIAN_POINT('Ctrl Pts',(-0.183444302032587,0.371856590513483,
-1.33200967075809));
#50578=CARTESIAN_POINT('Ctrl Pts',(-0.275839461984906,0.281233592936417,
-1.32543398308186));
#50579=CARTESIAN_POINT('Ctrl Pts',(-0.349924110720866,0.208569906371435,
-1.32016143945574));
#50580=CARTESIAN_POINT('Ctrl Pts',(-0.392496651065346,0.103777881823186,
-1.31488889582962));
#50581=CARTESIAN_POINT('Ctrl Pts',(-0.393434478492496,-0.000335863925950309,
-1.3096163522035));
#50582=CARTESIAN_POINT('Origin',(0.,0.,-0.975));
#50583=CARTESIAN_POINT('',(-0.393626427439675,0.000287423903241796,-1.1662836477965));
#50584=CARTESIAN_POINT('',(-0.393653923221138,0.000276869757435893,-1.1846163522035));
#50585=CARTESIAN_POINT('',(-0.3933,-4.81653586104654E-17,-0.975));
#50586=CARTESIAN_POINT('Ctrl Pts',(-0.393626427439675,0.000287423903241796,
-1.1662836477965));
#50587=CARTESIAN_POINT('Ctrl Pts',(-0.393782557155591,0.0192595098298366,
-1.16724565041905));
#50588=CARTESIAN_POINT('Ctrl Pts',(-0.392527937158206,0.0382108672674389,
-1.16820765304159));
#50589=CARTESIAN_POINT('Ctrl Pts',(-0.389790918787831,0.0569456569372362,
-1.16916965566413));
#50590=CARTESIAN_POINT('Ctrl Pts',(-0.371082260884058,0.185005729396081,
-1.17574534334036));
#50591=CARTESIAN_POINT('Ctrl Pts',(-0.283111643718684,0.302947126481015,
-1.18232103101659));
#50592=CARTESIAN_POINT('Ctrl Pts',(-0.165698122527018,0.357384807181973,
-1.18889671869282));
#50593=CARTESIAN_POINT('Ctrl Pts',(-0.0482846013353533,0.41182248788293,
-1.19547240636906));
#50594=CARTESIAN_POINT('Ctrl Pts',(0.0985718238826033,0.402756452199911,
-1.20204809404529));
#50595=CARTESIAN_POINT('Ctrl Pts',(0.208398002251702,0.334290354139894,
-1.20862378172152));
#50596=CARTESIAN_POINT('Ctrl Pts',(0.318224180620801,0.265824256079877,
-1.21519946939775));
#50597=CARTESIAN_POINT('Ctrl Pts',(0.391020112141041,0.137958095642862,
-1.22177515707398));
#50598=CARTESIAN_POINT('Ctrl Pts',(0.393835417339004,0.00856926268048242,
-1.22835084475021));
#50599=CARTESIAN_POINT('Ctrl Pts',(0.396650722536966,-0.120819570281897,
-1.23492653242644));
#50600=CARTESIAN_POINT('Ctrl Pts',(0.329485401412651,-0.25173107576964,
-1.24150222010267));
#50601=CARTESIAN_POINT('Ctrl Pts',(0.222741191704447,-0.324909417732935,
-1.2480779077789));
#50602=CARTESIAN_POINT('Ctrl Pts',(0.115996981996244,-0.398087759696229,
-1.25465359545513));
#50603=CARTESIAN_POINT('Ctrl Pts',(-0.0303261162958466,-0.413532938135074,
-1.26122928313136));
#50604=CARTESIAN_POINT('Ctrl Pts',(-0.149996357609078,-0.364253841321533,
-1.26780497080759));
#50605=CARTESIAN_POINT('Ctrl Pts',(-0.269666598922309,-0.314974744507992,
-1.27438065848382));
#50606=CARTESIAN_POINT('Ctrl Pts',(-0.362683983256681,-0.200971372442066,
-1.28095634616005));
#50607=CARTESIAN_POINT('Ctrl Pts',(-0.386945084672934,-0.0738462569188511,
-1.28753203383628));
#50608=CARTESIAN_POINT('Ctrl Pts',(-0.391558963922528,-0.0496701108094308,
-1.28878257182302));
#50609=CARTESIAN_POINT('Ctrl Pts',(-0.393686140780048,-0.0250193917670572,
-1.29003310980976));
#50610=CARTESIAN_POINT('Ctrl Pts',(-0.393465141926397,-0.00033072980931359,
-1.2912836477965));
#50611=CARTESIAN_POINT('Ctrl Pts',(-0.393434478492496,-0.000335863925950309,
-1.3096163522035));
#50612=CARTESIAN_POINT('Ctrl Pts',(-0.39366626874752,-0.0260682651972441,
-1.30831320815339));
#50613=CARTESIAN_POINT('Ctrl Pts',(-0.391354744535682,-0.0517592328627442,
-1.30701006410328));
#50614=CARTESIAN_POINT('Ctrl Pts',(-0.386347075720562,-0.0769134556904893,
-1.30570692005317));
#50615=CARTESIAN_POINT('Ctrl Pts',(-0.361078291266969,-0.203842104169159,
-1.29913123237694));
#50616=CARTESIAN_POINT('Ctrl Pts',(-0.267159484122848,-0.31710399855532,
-1.29255554470071));
#50617=CARTESIAN_POINT('Ctrl Pts',(-0.147102100607386,-0.365432229806147,
-1.28597985702447));
#50618=CARTESIAN_POINT('Ctrl Pts',(-0.0270447170919244,-0.413760461056975,
-1.27940416934824));
#50619=CARTESIAN_POINT('Ctrl Pts',(0.119151242794877,-0.39715502917247,
-1.27282848167201));
#50620=CARTESIAN_POINT('Ctrl Pts',(0.225311581468663,-0.32313222346311,
-1.26625279399578));
#50621=CARTESIAN_POINT('Ctrl Pts',(0.331471920142449,-0.24910941775375,
-1.25967710631955));
#50622=CARTESIAN_POINT('Ctrl Pts',(0.39759663760322,-0.117669238219534,
-1.25310141864332));
#50623=CARTESIAN_POINT('Ctrl Pts',(0.393755015369873,0.0116931798586055,
-1.24652573096709));
#50624=CARTESIAN_POINT('Ctrl Pts',(0.389913393136526,0.141055597936746,
-1.23995004329086));
#50625=CARTESIAN_POINT('Ctrl Pts',(0.31610543120906,0.26834025455881,-1.23337435561463));
#50626=CARTESIAN_POINT('Ctrl Pts',(0.205739594907986,0.335932971991804,
-1.2267986679384));
#50627=CARTESIAN_POINT('Ctrl Pts',(0.0953737586069128,0.403525689424797,
-1.22022298026217));
#50628=CARTESIAN_POINT('Ctrl Pts',(-0.0515499520677672,0.411426467668722,
-1.21364729258594));
#50629=CARTESIAN_POINT('Ctrl Pts',(-0.168527930124931,0.356059095308551,
-1.20707160490971));
#50630=CARTESIAN_POINT('Ctrl Pts',(-0.285505908182095,0.30069172294838,
-1.20049591723348));
#50631=CARTESIAN_POINT('Ctrl Pts',(-0.372538153621742,0.182056199984112,
-1.19392022955725));
#50632=CARTESIAN_POINT('Ctrl Pts',(-0.390230356160714,0.0538517568406279,
-1.18734454188102));
#50633=CARTESIAN_POINT('Ctrl Pts',(-0.392677131145371,0.0361214926909641,
-1.18643514532184));
#50634=CARTESIAN_POINT('Ctrl Pts',(-0.393797708142816,0.0182082133288689,
-1.18552574876267));
#50635=CARTESIAN_POINT('Ctrl Pts',(-0.393653923221138,0.000276869757435893,
-1.1846163522035));
#50636=CARTESIAN_POINT('Origin',(0.,0.,-0.975));
#50637=CARTESIAN_POINT('',(-0.392675709594332,3.59123229115022E-5,-1.0412836477965));
#50638=CARTESIAN_POINT('',(-0.392679206567132,5.24831113405046E-5,-1.0596163522035));
#50639=CARTESIAN_POINT('',(-0.3933,-4.81653586104654E-17,-0.975));
#50640=CARTESIAN_POINT('Ctrl Pts',(-0.392675709594332,3.59123229115022E-5,
-1.0412836477965));
#50641=CARTESIAN_POINT('Ctrl Pts',(-0.392727640745588,0.0630294066245346,
-1.04445819102833));
#50642=CARTESIAN_POINT('Ctrl Pts',(-0.378427444911321,0.126000646034939,
-1.04763273426015));
#50643=CARTESIAN_POINT('Ctrl Pts',(-0.349647097122614,0.181457090484786,
-1.05080727749198));
#50644=CARTESIAN_POINT('Ctrl Pts',(-0.290032039316968,0.29632850085984,
-1.05738296516821));
#50645=CARTESIAN_POINT('Ctrl Pts',(-0.16828817904421,0.37895679575142,-1.06395865284444));
#50646=CARTESIAN_POINT('Ctrl Pts',(-0.0395217057681203,0.391941070808678,
-1.07053434052067));
#50647=CARTESIAN_POINT('Ctrl Pts',(0.0892447675079717,0.404925345865936,
-1.0771100281969));
#50648=CARTESIAN_POINT('Ctrl Pts',(0.225033853787397,0.348265601088871,
-1.08368571587313));
#50649=CARTESIAN_POINT('Ctrl Pts',(0.306381926905658,0.247608325948566,
-1.09026140354936));
#50650=CARTESIAN_POINT('Ctrl Pts',(0.387730000023918,0.146951050808262,
-1.0968370912256));
#50651=CARTESIAN_POINT('Ctrl Pts',(0.414637059981015,0.00229624530471971,
-1.10341277890183));
#50652=CARTESIAN_POINT('Ctrl Pts',(0.374923884427774,-0.120879481712424,
-1.10998846657806));
#50653=CARTESIAN_POINT('Ctrl Pts',(0.335210708874532,-0.244055208729568,
-1.11656415425429));
#50654=CARTESIAN_POINT('Ctrl Pts',(0.228877297810951,-0.345751857260314,
-1.12313984193052));
#50655=CARTESIAN_POINT('Ctrl Pts',(0.104054448825274,-0.379937415758363,
-1.12971552960675));
#50656=CARTESIAN_POINT('Ctrl Pts',(-0.020768400160404,-0.414122974256413,
-1.13629121728298));
#50657=CARTESIAN_POINT('Ctrl Pts',(-0.164080687068179,-0.380797442721763,
-1.14286690495921));
#50658=CARTESIAN_POINT('Ctrl Pts',(-0.261013481200979,-0.295045303038061,
-1.14944259263544));
#50659=CARTESIAN_POINT('Ctrl Pts',(-0.343765309515822,-0.221838434256229,
-1.15505627768913));
#50660=CARTESIAN_POINT('Ctrl Pts',(-0.392715345669069,-0.110422581150446,
-1.16066996274281));
#50661=CARTESIAN_POINT('Ctrl Pts',(-0.393626427439675,0.000287423903241796,
-1.1662836477965));
#50662=CARTESIAN_POINT('Ctrl Pts',(-0.393653923221138,0.000276869757435893,
-1.1846163522035));
#50663=CARTESIAN_POINT('Ctrl Pts',(-0.392758024488892,-0.11145019999114,
-1.17895006108644));
#50664=CARTESIAN_POINT('Ctrl Pts',(-0.34277556993753,-0.22387857986823,
-1.17328376996938));
#50665=CARTESIAN_POINT('Ctrl Pts',(-0.258664734133429,-0.297106543010793,
-1.16761747885232));
#50666=CARTESIAN_POINT('Ctrl Pts',(-0.161054749928876,-0.38208703639603,
-1.16104179117609));
#50667=CARTESIAN_POINT('Ctrl Pts',(-0.0174826218814731,-0.414274659843806,
-1.15446610349986));
#50668=CARTESIAN_POINT('Ctrl Pts',(0.107065104714644,-0.379099994640705,
-1.14789041582363));
#50669=CARTESIAN_POINT('Ctrl Pts',(0.231612831310762,-0.343925329437603,
-1.1413147281474));
#50670=CARTESIAN_POINT('Ctrl Pts',(0.337136156455594,-0.241388375583624,
-1.13473904047117));
#50671=CARTESIAN_POINT('Ctrl Pts',(0.375870960174213,-0.117901500761677,
-1.12816335279494));
#50672=CARTESIAN_POINT('Ctrl Pts',(0.414605763892832,0.00558537406027194,
-1.12158766511871));
#50673=CARTESIAN_POINT('Ctrl Pts',(0.386552046185236,0.15002216985019,-1.11501197744248));
#50674=CARTESIAN_POINT('Ctrl Pts',(0.304408053022061,0.250030957762152,
-1.10843628976625));
#50675=CARTESIAN_POINT('Ctrl Pts',(0.222264059858886,0.350039745674113,
-1.10186060209002));
#50676=CARTESIAN_POINT('Ctrl Pts',(0.0860297912401334,0.405620525708119,
-1.09528491441379));
#50677=CARTESIAN_POINT('Ctrl Pts',(-0.0426296191580955,0.391615191424664,
-1.08870922673755));
#50678=CARTESIAN_POINT('Ctrl Pts',(-0.171289029556324,0.377609857141209,
-1.08213353906132));
#50679=CARTESIAN_POINT('Ctrl Pts',(-0.292373581734029,0.294018408540293,
-1.07555785138509));
#50680=CARTESIAN_POINT('Ctrl Pts',(-0.351075515706501,0.17867771225185,
-1.06898216370886));
#50681=CARTESIAN_POINT('Ctrl Pts',(-0.378945414423148,0.123917446176563,
-1.06586022654041));
#50682=CARTESIAN_POINT('Ctrl Pts',(-0.392753880852442,0.0620007011111865,
-1.06273828937195));
#50683=CARTESIAN_POINT('Ctrl Pts',(-0.392679206567132,5.24831113405046E-5,
-1.0596163522035));
#50684=CARTESIAN_POINT('Origin',(0.,0.,-0.975));
#50685=CARTESIAN_POINT('',(-0.393500865148788,-0.000323575883594496,-0.916283647796503));
#50686=CARTESIAN_POINT('',(-0.393470515958058,-0.000329728814630641,-0.934616352203498));
#50687=CARTESIAN_POINT('',(-0.3933,-4.81653586104654E-17,-0.975));
#50688=CARTESIAN_POINT('Ctrl Pts',(-0.393500865148788,-0.000323575883594496,
-0.916283647796503));
#50689=CARTESIAN_POINT('Ctrl Pts',(-0.392559185254019,0.106005602838139,
-0.921670731637612));
#50690=CARTESIAN_POINT('Ctrl Pts',(-0.347906081227037,0.213031985603417,
-0.92705781547872));
#50691=CARTESIAN_POINT('Ctrl Pts',(-0.27094104215407,0.28595580058803,-0.932444899319829));
#50692=CARTESIAN_POINT('Ctrl Pts',(-0.176994470342677,0.374969494386296,
-0.93902058699606));
#50693=CARTESIAN_POINT('Ctrl Pts',(-0.0349043771728895,0.413171693980084,
-0.94559627467229));
#50694=CARTESIAN_POINT('Ctrl Pts',(0.0910135209191817,0.383270540510706,
-0.952171962348521));
#50695=CARTESIAN_POINT('Ctrl Pts',(0.216931419011254,0.353369387041328,
-0.958747650024752));
#50696=CARTESIAN_POINT('Ctrl Pts',(0.32667712202561,0.255364880508782,-0.965323337700983));
#50697=CARTESIAN_POINT('Ctrl Pts',(0.370575291184627,0.133617819832924,
-0.971899025377213));
#50698=CARTESIAN_POINT('Ctrl Pts',(0.414473460343644,0.0118707591570669,
-0.978474713053443));
#50699=CARTESIAN_POINT('Ctrl Pts',(0.392524095647324,-0.133618855662101,
-0.985050400729674));
#50700=CARTESIAN_POINT('Ctrl Pts',(0.31466236628494,-0.23699654735341,-0.991626088405904));
#50701=CARTESIAN_POINT('Ctrl Pts',(0.236800636922554,-0.340374239044721,
-0.998201776082135));
#50702=CARTESIAN_POINT('Ctrl Pts',(0.1030265428941,-0.401640007608169,-1.00477746375837));
#50703=CARTESIAN_POINT('Ctrl Pts',(-0.026108356531957,-0.393062491129178,
-1.0113531514346));
#50704=CARTESIAN_POINT('Ctrl Pts',(-0.155243255958012,-0.384484974650187,
-1.01792883911083));
#50705=CARTESIAN_POINT('Ctrl Pts',(-0.279738960781671,-0.306064173128758,
-1.02450452678706));
#50706=CARTESIAN_POINT('Ctrl Pts',(-0.343243685524234,-0.193296509438779,
-1.03108021446329));
#50707=CARTESIAN_POINT('Ctrl Pts',(-0.376090248862751,-0.134969664893826,
-1.03448135890769));
#50708=CARTESIAN_POINT('Ctrl Pts',(-0.392620071559601,-0.0674541035728149,
-1.0378825033521));
#50709=CARTESIAN_POINT('Ctrl Pts',(-0.392675709594332,3.59123229115022E-5,
-1.0412836477965));
#50710=CARTESIAN_POINT('Ctrl Pts',(-0.392679206567132,5.24831113405046E-5,
-1.0596163522035));
#50711=CARTESIAN_POINT('Ctrl Pts',(-0.39259659556733,-0.0684798664614236,
-1.05616260169572));
#50712=CARTESIAN_POINT('Ctrl Pts',(-0.375522890959624,-0.137050734665287,
-1.05270885118795));
#50713=CARTESIAN_POINT('Ctrl Pts',(-0.34169948938714,-0.196013268777163,
-1.04925510068017));
#50714=CARTESIAN_POINT('Ctrl Pts',(-0.27730221332807,-0.30827360954176,
-1.04267941300394));
#50715=CARTESIAN_POINT('Ctrl Pts',(-0.152188345442694,-0.385704347094983,
-1.03610372532771));
#50716=CARTESIAN_POINT('Ctrl Pts',(-0.0229894767844834,-0.393257201512339,
-1.02952803765148));
#50717=CARTESIAN_POINT('Ctrl Pts',(0.106209391873727,-0.400810055929695,
-1.02295234997525));
#50718=CARTESIAN_POINT('Ctrl Pts',(0.239493261304774,-0.338485027211183,
-1.01637666229902));
#50719=CARTESIAN_POINT('Ctrl Pts',(0.316532467697458,-0.234492941210388,
-1.00980097462279));
#50720=CARTESIAN_POINT('Ctrl Pts',(0.393571674090142,-0.130500855209592,
-1.00322528694656));
#50721=CARTESIAN_POINT('Ctrl Pts',(0.414366217444464,0.0151582880734869,
-0.996649599270326));
#50722=CARTESIAN_POINT('Ctrl Pts',(0.369503647363922,0.136553275936165,
-0.990073911594096));
#50723=CARTESIAN_POINT('Ctrl Pts',(0.32464107728338,0.257948263798845,-0.983498223917865));
#50724=CARTESIAN_POINT('Ctrl Pts',(0.214121393767973,0.355079096241123,
-0.976922536241634));
#50725=CARTESIAN_POINT('Ctrl Pts',(0.0879702704379724,0.383980434531775,
-0.970346848565403));
#50726=CARTESIAN_POINT('Ctrl Pts',(-0.0381808528920271,0.412881772822426,
-0.963771160889173));
#50727=CARTESIAN_POINT('Ctrl Pts',(-0.179963416036617,0.373553616961452,
-0.957195473212943));
#50728=CARTESIAN_POINT('Ctrl Pts',(-0.273200903072934,0.283797479101337,
-0.950619785536712));
#50729=CARTESIAN_POINT('Ctrl Pts',(-0.348839121786578,0.210983479044568,
-0.945285307758974));
#50730=CARTESIAN_POINT('Ctrl Pts',(-0.392529121558599,0.104982092359763,
-0.939950829981236));
#50731=CARTESIAN_POINT('Ctrl Pts',(-0.393470515958058,-0.000329728814630641,
-0.934616352203498));
#50732=CARTESIAN_POINT('Origin',(0.,0.,-0.975));
#50733=CARTESIAN_POINT('',(-0.393593124134507,0.000298827634702806,-0.791283647796503));
#50734=CARTESIAN_POINT('',(-0.39362143792178,0.00028921277307428,-0.809616352203499));
#50735=CARTESIAN_POINT('',(-0.3933,-4.81653586104654E-17,-0.975));
#50736=CARTESIAN_POINT('Ctrl Pts',(-0.393593124134507,0.000298827634702806,
-0.791283647796503));
#50737=CARTESIAN_POINT('Ctrl Pts',(-0.393763705766818,0.0204967956566175,
-0.792307584570663));
#50738=CARTESIAN_POINT('Ctrl Pts',(-0.392341422207924,0.0406706868593803,
-0.793331521344824));
#50739=CARTESIAN_POINT('Ctrl Pts',(-0.389242085705192,0.0605835532908611,
-0.794355458118985));
#50740=CARTESIAN_POINT('Ctrl Pts',(-0.369338250468678,0.188463314713854,
-0.800931145795216));
#50741=CARTESIAN_POINT('Ctrl Pts',(-0.28026997813637,0.305577982858121,
-0.807506833471447));
#50742=CARTESIAN_POINT('Ctrl Pts',(-0.162353167016069,0.358916727630976,
-0.814082521147678));
#50743=CARTESIAN_POINT('Ctrl Pts',(-0.0444363558957643,0.412255472403833,
-0.820658208823909));
#50744=CARTESIAN_POINT('Ctrl Pts',(0.102328994012537,0.401818293805276,
-0.827233896500139));
#50745=CARTESIAN_POINT('Ctrl Pts',(0.211510956198164,0.332329480518375,
-0.83380958417637));
#50746=CARTESIAN_POINT('Ctrl Pts',(0.320692918383789,0.262840667231475,
-0.8403852718526));
#50747=CARTESIAN_POINT('Ctrl Pts',(0.392291492846743,0.134300219256238,
-0.846960959528831));
#50748=CARTESIAN_POINT('Ctrl Pts',(0.393898272289506,0.00489073622447934,
-0.853536647205062));
#50749=CARTESIAN_POINT('Ctrl Pts',(0.395505051732269,-0.124518746807278,
-0.860112334881293));
#50750=CARTESIAN_POINT('Ctrl Pts',(0.32712003615484,-0.254797264895555,
-0.866688022557523));
#50751=CARTESIAN_POINT('Ctrl Pts',(0.219697046279269,-0.326975497659441,
-0.873263710233753));
#50752=CARTESIAN_POINT('Ctrl Pts',(0.112274056403699,-0.399153730423328,
-0.879839397909984));
#50753=CARTESIAN_POINT('Ctrl Pts',(-0.0341869077700128,-0.413231677862823,
-0.886415085586215));
#50754=CARTESIAN_POINT('Ctrl Pts',(-0.15339169701149,-0.362837092234807,
-0.892990773262446));
#50755=CARTESIAN_POINT('Ctrl Pts',(-0.27259648625297,-0.312442506606791,
-0.899566460938676));
#50756=CARTESIAN_POINT('Ctrl Pts',(-0.364545100562215,-0.19757538791126,
-0.906142148614907));
#50757=CARTESIAN_POINT('Ctrl Pts',(-0.387617882490338,-0.0702292345621217,
-0.912717836291137));
#50758=CARTESIAN_POINT('Ctrl Pts',(-0.391788457255595,-0.0472104821955896,
-0.913906440126259));
#50759=CARTESIAN_POINT('Ctrl Pts',(-0.393708636991104,-0.0237839996196404,
-0.915095043961381));
#50760=CARTESIAN_POINT('Ctrl Pts',(-0.393500865148788,-0.000323575883594496,
-0.916283647796503));
#50761=CARTESIAN_POINT('Ctrl Pts',(-0.393470515958058,-0.000329728814630641,
-0.934616352203498));
#50762=CARTESIAN_POINT('Ctrl Pts',(-0.393689556714375,-0.0248333597821209,
-0.933375142305005));
#50763=CARTESIAN_POINT('Ctrl Pts',(-0.391594249852963,-0.0492996586709999,
-0.932133932406512));
#50764=CARTESIAN_POINT('Ctrl Pts',(-0.38704854515182,-0.0733018845596751,
-0.930892722508019));
#50765=CARTESIAN_POINT('Ctrl Pts',(-0.362966289266348,-0.200460990501319,
-0.924317034831789));
#50766=CARTESIAN_POINT('Ctrl Pts',(-0.27010936656736,-0.31459508252535,
-0.917741347155559));
#50767=CARTESIAN_POINT('Ctrl Pts',(-0.150508571575497,-0.364042459702771,
-0.911165659479328));
#50768=CARTESIAN_POINT('Ctrl Pts',(-0.0309077765836359,-0.413489836880192,
-0.904589971803098));
#50769=CARTESIAN_POINT('Ctrl Pts',(0.115436890701099,-0.398250499211004,
-0.898014284126867));
#50770=CARTESIAN_POINT('Ctrl Pts',(0.222283921718536,-0.325222386575045,
-0.891438596450636));
#50771=CARTESIAN_POINT('Ctrl Pts',(0.329130952735972,-0.252194273939086,
-0.884862908774405));
#50772=CARTESIAN_POINT('Ctrl Pts',(0.396480347486111,-0.121377386336356,
-0.878287221098174));
#50773=CARTESIAN_POINT('Ctrl Pts',(0.393847049071157,0.00801526806051965,
-0.871711533421944));
#50774=CARTESIAN_POINT('Ctrl Pts',(0.391213750656204,0.137407922457395,
-0.865135845745713));
#50775=CARTESIAN_POINT('Ctrl Pts',(0.318597759076159,0.265376343648415,
-0.858560158069483));
#50776=CARTESIAN_POINT('Ctrl Pts',(0.208868005718157,0.333996854433482,
-0.851984470393252));
#50777=CARTESIAN_POINT('Ctrl Pts',(0.0991382523601543,0.402617365218549,
-0.845408782717021));
#50778=CARTESIAN_POINT('Ctrl Pts',(-0.0477052627758059,0.411889965597663,
-0.83883309504079));
#50779=CARTESIAN_POINT('Ctrl Pts',(-0.165195232439238,0.357617502037424,
-0.83225740736456));
#50780=CARTESIAN_POINT('Ctrl Pts',(-0.282685202102669,0.303345038477185,
-0.825681719688329));
#50781=CARTESIAN_POINT('Ctrl Pts',(-0.370821626293572,0.185527510977596,
-0.819106032012099));
#50782=CARTESIAN_POINT('Ctrl Pts',(-0.389710398818481,0.0574938921702172,
-0.812530344335868));
#50783=CARTESIAN_POINT('Ctrl Pts',(-0.392500562485909,0.0385813476449172,
-0.811559013625078));
#50784=CARTESIAN_POINT('Ctrl Pts',(-0.393779752347368,0.0194458894757019,
-0.810587682914289));
#50785=CARTESIAN_POINT('Ctrl Pts',(-0.39362143792178,0.00028921277307428,
-0.809616352203499));
#50786=CARTESIAN_POINT('Origin',(0.,0.,-0.975));
#50787=CARTESIAN_POINT('',(-0.392673255853308,1.63036301740749E-5,-0.666283647796503));
#50788=CARTESIAN_POINT('',(-0.392675189741302,3.29645964630328E-5,-0.684616352203499));
#50789=CARTESIAN_POINT('',(-0.3933,-4.81653586104654E-17,-0.975));
#50790=CARTESIAN_POINT('Ctrl Pts',(-0.392673255853308,1.63036301740749E-5,
-0.666283647796503));
#50791=CARTESIAN_POINT('Ctrl Pts',(-0.392697283129928,0.0642397806098739,
-0.669520125179946));
#50792=CARTESIAN_POINT('Ctrl Pts',(-0.377805755035603,0.128452760339452,
-0.67275660256339));
#50793=CARTESIAN_POINT('Ctrl Pts',(-0.347937163399018,0.184714640836245,
-0.675993079946833));
#50794=CARTESIAN_POINT('Ctrl Pts',(-0.287251885344617,0.299024277639788,
-0.682568767623064));
#50795=CARTESIAN_POINT('Ctrl Pts',(-0.164741642994295,0.380511964747164,
-0.689144455299295));
#50796=CARTESIAN_POINT('Ctrl Pts',(-0.0358595213010159,0.392293082969346,
-0.695720142975526));
#50797=CARTESIAN_POINT('Ctrl Pts',(0.0930226003922591,0.404074201191528,
-0.702295830651757));
#50798=CARTESIAN_POINT('Ctrl Pts',(0.228276601428489,0.34614875052852,-0.708871518327987));
#50799=CARTESIAN_POINT('Ctrl Pts',(0.30868105684103,0.244736130068616,-0.715447206004218));
#50800=CARTESIAN_POINT('Ctrl Pts',(0.38908551225357,0.143323509608713,-0.722022893680448));
#50801=CARTESIAN_POINT('Ctrl Pts',(0.414640422042422,-0.00157628064808814,
-0.728598581356679));
#50802=CARTESIAN_POINT('Ctrl Pts',(0.37377860164979,-0.124375741855866,
-0.73517426903291));
#50803=CARTESIAN_POINT('Ctrl Pts',(0.332916781257156,-0.247175203063647,
-0.741749956709141));
#50804=CARTESIAN_POINT('Ctrl Pts',(0.225638230683036,-0.347874335222406,
-0.748325644385371));
#50805=CARTESIAN_POINT('Ctrl Pts',(0.100501555840629,-0.380892642994185,
-0.754901332061602));
#50806=CARTESIAN_POINT('Ctrl Pts',(-0.0246351190017731,-0.413910950765964,
-0.761477019737833));
#50807=CARTESIAN_POINT('Ctrl Pts',(-0.167629918112459,-0.379248434150768,
-0.768052707414064));
#50808=CARTESIAN_POINT('Ctrl Pts',(-0.263757618597442,-0.29259474849231,
-0.774628395090294));
#50809=CARTESIAN_POINT('Ctrl Pts',(-0.344916742047071,-0.219434388510343,
-0.780180145992364));
#50810=CARTESIAN_POINT('Ctrl Pts',(-0.392668236236193,-0.109213878633263,
-0.785731896894433));
#50811=CARTESIAN_POINT('Ctrl Pts',(-0.393593124134507,0.000298827634702806,
-0.791283647796503));
#50812=CARTESIAN_POINT('Ctrl Pts',(-0.39362143792178,0.00028921277307428,
-0.809616352203499));
#50813=CARTESIAN_POINT('Ctrl Pts',(-0.392707999744733,-0.110240448567251,
-0.804011995238058));
#50814=CARTESIAN_POINT('Ctrl Pts',(-0.343939653374366,-0.221476480648583,
-0.798407638272616));
#50815=CARTESIAN_POINT('Ctrl Pts',(-0.261428224532134,-0.294677834256525,
-0.792803281307176));
#50816=CARTESIAN_POINT('Ctrl Pts',(-0.164616156861964,-0.380566231760713,
-0.786227593630945));
#50817=CARTESIAN_POINT('Ctrl Pts',(-0.0213509006627109,-0.414093316653921,
-0.779651905954716));
#50818=CARTESIAN_POINT('Ctrl Pts',(0.103519901367221,-0.380083375859906,
-0.773076218278485));
#50819=CARTESIAN_POINT('Ctrl Pts',(0.228390703397158,-0.346073435065889,
-0.766500530602254));
#50820=CARTESIAN_POINT('Ctrl Pts',(0.334867051257771,-0.244526468584641,
-0.759924842926023));
#50821=CARTESIAN_POINT('Ctrl Pts',(0.374753448392003,-0.121406735819898,
-0.753349155249792));
#50822=CARTESIAN_POINT('Ctrl Pts',(0.414639845526233,0.00171299694484139,
-0.746773467573561));
#50823=CARTESIAN_POINT('Ctrl Pts',(0.387936291934087,0.146405495993077,
-0.740197779897331));
#50824=CARTESIAN_POINT('Ctrl Pts',(0.306729894762555,0.247177090854086,
-0.7336220922211));
#50825=CARTESIAN_POINT('Ctrl Pts',(0.225523497591022,0.347948685715098,
-0.72704640454487));
#50826=CARTESIAN_POINT('Ctrl Pts',(0.0898142568401032,0.404799376388883,
-0.720470716868639));
#50827=CARTESIAN_POINT('Ctrl Pts',(-0.0389703426375748,0.391996243577485,
-0.713895029192408));
#50828=CARTESIAN_POINT('Ctrl Pts',(-0.167754942115248,0.379193110766087,
-0.707319341516178));
#50829=CARTESIAN_POINT('Ctrl Pts',(-0.289614900319681,0.296736154469509,
-0.700743653839948));
#50830=CARTESIAN_POINT('Ctrl Pts',(-0.349391477172996,0.181948724268698,
-0.694167966163717));
#50831=CARTESIAN_POINT('Ctrl Pts',(-0.378334598870116,0.12636998864196,
-0.690984094843644));
#50832=CARTESIAN_POINT('Ctrl Pts',(-0.392722994987612,0.0632117500098348,
-0.687800223523571));
#50833=CARTESIAN_POINT('Ctrl Pts',(-0.392675189741302,3.29645964630328E-5,
-0.684616352203499));
#50834=CARTESIAN_POINT('Origin',(0.,0.,-0.975));
#50835=CARTESIAN_POINT('',(-0.393536100995357,-0.000315234482339499,-0.541283647796502));
#50836=CARTESIAN_POINT('',(-0.393506173951298,-0.000322395119289577,-0.559616352203498));
#50837=CARTESIAN_POINT('',(-0.3933,-4.81653586104654E-17,-0.975));
#50838=CARTESIAN_POINT('Ctrl Pts',(-0.393536100995357,-0.000315234482339499,
-0.541283647796502));
#50839=CARTESIAN_POINT('Ctrl Pts',(-0.392597489512059,0.107211443487718,
-0.546732665789229));
#50840=CARTESIAN_POINT('Ctrl Pts',(-0.346793977563156,0.215441809949464,
-0.552181683781956));
#50841=CARTESIAN_POINT('Ctrl Pts',(-0.26825859469211,0.288473732917049,
-0.557630701774682));
#50842=CARTESIAN_POINT('Ctrl Pts',(-0.173484793250727,0.376606148055041,
-0.564206389450913));
#50843=CARTESIAN_POINT('Ctrl Pts',(-0.0310441146165509,0.413479657540965,
-0.570782077127143));
#50844=CARTESIAN_POINT('Ctrl Pts',(0.0945890356312672,0.382403821312673,
-0.577357764803374));
#50845=CARTESIAN_POINT('Ctrl Pts',(0.220222185879085,0.351327985084382,
-0.583933452479604));
#50846=CARTESIAN_POINT('Ctrl Pts',(0.329047807740543,0.252302803141877,
-0.590509140155835));
#50847=CARTESIAN_POINT('Ctrl Pts',(0.371807028337272,0.130151073341996,
-0.597084827832066));
#50848=CARTESIAN_POINT('Ctrl Pts',(0.414566248934001,0.00799934354211448,
-0.603660515508297));
#50849=CARTESIAN_POINT('Ctrl Pts',(0.391259068265997,-0.137278934115147,
-0.610236203184528));
#50850=CARTESIAN_POINT('Ctrl Pts',(0.312435257885808,-0.239924942102313,
-0.616811890860758));
#50851=CARTESIAN_POINT('Ctrl Pts',(0.23361144750562,-0.342570950089479,
-0.623387578536989));
#50852=CARTESIAN_POINT('Ctrl Pts',(0.0992710074132505,-0.402584688406554,
-0.629963266213219));
#50853=CARTESIAN_POINT('Ctrl Pts',(-0.0297781520148116,-0.392801514605605,
-0.63653895388945));
#50854=CARTESIAN_POINT('Ctrl Pts',(-0.158827311442874,-0.383018340804656,
-0.643114641565681));
#50855=CARTESIAN_POINT('Ctrl Pts',(-0.282585190206626,-0.303438254885682,
-0.649690329241912));
#50856=CARTESIAN_POINT('Ctrl Pts',(-0.345033972709263,-0.190082418676341,
-0.656266016918142));
#50857=CARTESIAN_POINT('Ctrl Pts',(-0.376746187092345,-0.132519013348265,
-0.659605227210929));
#50858=CARTESIAN_POINT('Ctrl Pts',(-0.392648465898091,-0.0662457677398398,
-0.662944437503716));
#50859=CARTESIAN_POINT('Ctrl Pts',(-0.392673255853308,1.63036301740749E-5,
-0.666283647796503));
#50860=CARTESIAN_POINT('Ctrl Pts',(-0.392675189741302,3.29645964630328E-5,
-0.684616352203499));
#50861=CARTESIAN_POINT('Ctrl Pts',(-0.392624262238258,-0.0672721542933228,
-0.68122453584734));
#50862=CARTESIAN_POINT('Ctrl Pts',(-0.376189838802812,-0.134600591513086,
-0.677832719491182));
#50863=CARTESIAN_POINT('Ctrl Pts',(-0.343515216587402,-0.192813481263717,
-0.674440903135024));
#50864=CARTESIAN_POINT('Ctrl Pts',(-0.280169183646299,-0.305670352490252,
-0.667865215458793));
#50865=CARTESIAN_POINT('Ctrl Pts',(-0.155783922261904,-0.384266190838277,
-0.661289527782563));
#50866=CARTESIAN_POINT('Ctrl Pts',(-0.0266612267504973,-0.393025344694661,
-0.654713840106333));
#50867=CARTESIAN_POINT('Ctrl Pts',(0.102461468760913,-0.401784498551045,
-0.648138152430102));
#50868=CARTESIAN_POINT('Ctrl Pts',(0.236321598399336,-0.340706967915784,
-0.641562464753871));
#50869=CARTESIAN_POINT('Ctrl Pts',(0.314328659703452,-0.237438910613055,
-0.63498677707764));
#50870=CARTESIAN_POINT('Ctrl Pts',(0.392335721007567,-0.134170853310328,
-0.62841108940141));
#50871=CARTESIAN_POINT('Ctrl Pts',(0.414489713977377,0.0112877306598665,
-0.621835401725179));
#50872=CARTESIAN_POINT('Ctrl Pts',(0.370762846400388,0.133096409843133,
-0.615259714048949));
#50873=CARTESIAN_POINT('Ctrl Pts',(0.327035978823398,0.254905089026401,
-0.608684026372718));
#50874=CARTESIAN_POINT('Ctrl Pts',(0.217428250699609,0.353063863422739,
-0.602108338696487));
#50875=CARTESIAN_POINT('Ctrl Pts',(0.091552547796971,0.383142106243137,
-0.595532651020257));
#50876=CARTESIAN_POINT('Ctrl Pts',(-0.034323155105665,0.413220349063535,
-0.588956963344026));
#50877=CARTESIAN_POINT('Ctrl Pts',(-0.176466832787148,0.375218060307994,
-0.582381275667795));
#50878=CARTESIAN_POINT('Ctrl Pts',(-0.270538514296277,0.286336611117046,
-0.575805587991565));
#50879=CARTESIAN_POINT('Ctrl Pts',(-0.34773949604993,0.213395051796,-0.570409176062209));
#50880=CARTESIAN_POINT('Ctrl Pts',(-0.392564716544902,0.106187148606209,
-0.565012764132854));
#50881=CARTESIAN_POINT('Ctrl Pts',(-0.393506173951298,-0.000322395119289577,
-0.559616352203498));
#50882=CARTESIAN_POINT('Origin',(0.,0.,-0.975));
#50883=CARTESIAN_POINT('',(-0.393558983542489,0.000309099215769798,-0.416283647796503));
#50884=CARTESIAN_POINT('',(-0.393587999858846,0.00030044772715955,-0.434616352203498));
#50885=CARTESIAN_POINT('',(-0.3933,-4.81653586104654E-17,-0.975));
#50886=CARTESIAN_POINT('Ctrl Pts',(-0.393558983542489,0.000309099215769798,
-0.416283647796503));
#50887=CARTESIAN_POINT('Ctrl Pts',(-0.393743822683672,0.0217335979797476,
-0.417369518722281));
#50888=CARTESIAN_POINT('Ctrl Pts',(-0.392143183010408,0.0431304611559441,
-0.41845538964806));
#50889=CARTESIAN_POINT('Ctrl Pts',(-0.388659301138879,0.0642161659179647,
-0.419541260573839));
#50890=CARTESIAN_POINT('Ctrl Pts',(-0.367562024709244,0.191904462617531,
-0.426116948250069));
#50891=CARTESIAN_POINT('Ctrl Pts',(-0.277403866089175,0.308182185252994,
-0.4326926359263));
#50892=CARTESIAN_POINT('Ctrl Pts',(-0.158994050280294,0.360417341336711,
-0.43926832360253));
#50893=CARTESIAN_POINT('Ctrl Pts',(-0.040584234471411,0.412652497420429,
-0.445844011278761));
#50894=CARTESIAN_POINT('Ctrl Pts',(0.106077238526287,0.400845086952398,
-0.452419698954992));
#50895=CARTESIAN_POINT('Ctrl Pts',(0.214605461156142,0.330339619738361,
-0.458995386631223));
#50896=CARTESIAN_POINT('Ctrl Pts',(0.323133683785996,0.259834152524326,
-0.465571074307454));
#50897=CARTESIAN_POINT('Ctrl Pts',(0.393528656048009,0.130630628564292,
-0.472146761983684));
#50898=CARTESIAN_POINT('Ctrl Pts',(0.393926769589517,0.00121178308243824,
-0.478722449659915));
#50899=CARTESIAN_POINT('Ctrl Pts',(0.394324883131026,-0.128207062399414,
-0.485298137336145));
#50900=CARTESIAN_POINT('Ctrl Pts',(0.324726137952028,-0.257841229403082,
-0.491873825012376));
#50901=CARTESIAN_POINT('Ctrl Pts',(0.216633737843898,-0.329013057199999,
-0.498449512688606));
#50902=CARTESIAN_POINT('Ctrl Pts',(0.108541337735769,-0.400184884996917,
-0.505025200364837));
#50903=CARTESIAN_POINT('Ctrl Pts',(-0.0380447173014935,-0.412894373587085,
-0.511600888041068));
#50904=CARTESIAN_POINT('Ctrl Pts',(-0.156773656868775,-0.361388694819473,
-0.518176575717298));
#50905=CARTESIAN_POINT('Ctrl Pts',(-0.275502596436061,-0.309883016051859,
-0.524752263393529));
#50906=CARTESIAN_POINT('Ctrl Pts',(-0.366374420533366,-0.194162169926462,
-0.53132795106976));
#50907=CARTESIAN_POINT('Ctrl Pts',(-0.388256870457723,-0.066606086468731,
-0.53790363874599));
#50908=CARTESIAN_POINT('Ctrl Pts',(-0.392006180665944,-0.0447507947860351,
-0.539030308429494));
#50909=CARTESIAN_POINT('Ctrl Pts',(-0.393730173597839,-0.0225480566896565,
-0.540156978112998));
#50910=CARTESIAN_POINT('Ctrl Pts',(-0.393536100995357,-0.000315234482339499,
-0.541283647796502));
#50911=CARTESIAN_POINT('Ctrl Pts',(-0.393506173951298,-0.000322395119289577,
-0.559616352203498));
#50912=CARTESIAN_POINT('Ctrl Pts',(-0.393711910262872,-0.0235978832344477,
-0.558437076456623));
#50913=CARTESIAN_POINT('Ctrl Pts',(-0.391821969279263,-0.0468400210630716,
-0.557257800709748));
#50914=CARTESIAN_POINT('Ctrl Pts',(-0.387716254392333,-0.0696839196924745,
-0.556078524962873));
#50915=CARTESIAN_POINT('Ctrl Pts',(-0.364822627642485,-0.197062391684688,
-0.549502837286642));
#50916=CARTESIAN_POINT('Ctrl Pts',(-0.273035688806017,-0.312058726042759,
-0.542927149610411));
#50917=CARTESIAN_POINT('Ctrl Pts',(-0.153901914480065,-0.362620936111316,
-0.536351461934181));
#50918=CARTESIAN_POINT('Ctrl Pts',(-0.0347681401541137,-0.413183146179874,
-0.52977577425795));
#50919=CARTESIAN_POINT('Ctrl Pts',(0.111712469661326,-0.399311231958917,
-0.52320008658172));
#50920=CARTESIAN_POINT('Ctrl Pts',(0.219236873322318,-0.32728418225721,
-0.516624398905489));
#50921=CARTESIAN_POINT('Ctrl Pts',(0.326761276983311,-0.255257132555503,
-0.510048711229258));
#50922=CARTESIAN_POINT('Ctrl Pts',(0.395329474489862,-0.125074947373046,
-0.503473023553027));
#50923=CARTESIAN_POINT('Ctrl Pts',(0.393904729583154,0.00433665711985055,
-0.496897335876797));
#50924=CARTESIAN_POINT('Ctrl Pts',(0.392479984676447,0.133748261612745,
-0.490321648200566));
#50925=CARTESIAN_POINT('Ctrl Pts',(0.321062297356485,0.262389285416077,
-0.483745960524336));
#50926=CARTESIAN_POINT('Ctrl Pts',(0.211978198083273,0.332031604127538,
-0.477170272848105));
#50927=CARTESIAN_POINT('Ctrl Pts',(0.10289409881006,0.401673922838999,-0.470594585171874));
#50928=CARTESIAN_POINT('Ctrl Pts',(-0.0438564124164029,0.412317536458589,
-0.464018897495644));
#50929=CARTESIAN_POINT('Ctrl Pts',(-0.161848125655116,0.359144715640751,
-0.457443209819413));
#50930=CARTESIAN_POINT('Ctrl Pts',(-0.27983983889383,0.305971894822913,
-0.450867522143182));
#50931=CARTESIAN_POINT('Ctrl Pts',(-0.369072754144792,0.188982639567648,
-0.444291834466952));
#50932=CARTESIAN_POINT('Ctrl Pts',(-0.389156449096802,0.0611310127061034,
-0.437716146790721));
#50933=CARTESIAN_POINT('Ctrl Pts',(-0.392312282725616,0.0410411604895479,
-0.436682881928313));
#50934=CARTESIAN_POINT('Ctrl Pts',(-0.393760743963613,0.0206831040430797,
-0.435649617065905));
#50935=CARTESIAN_POINT('Ctrl Pts',(-0.393587999858846,0.000300447727159551,
-0.434616352203498));
#50936=CARTESIAN_POINT('Origin',(0.,0.,-0.975));
#50937=CARTESIAN_POINT('',(-0.392672644806505,-3.40218946998094E-6,-0.291283647796502));
#50938=CARTESIAN_POINT('',(-0.392673014342038,1.33379860697712E-5,-0.309616352203498));
#50939=CARTESIAN_POINT('',(-0.3933,-4.81653586104654E-17,-0.975));
#50940=CARTESIAN_POINT('Ctrl Pts',(-0.392672644806505,-3.40218946998094E-6,
-0.291283647796502));
#50941=CARTESIAN_POINT('Ctrl Pts',(-0.392667607343535,0.0654493539976286,
-0.294582059331564));
#50942=CARTESIAN_POINT('Ctrl Pts',(-0.377171222422322,0.130904364537333,
-0.297880470866626));
#50943=CARTESIAN_POINT('Ctrl Pts',(-0.346196882833469,0.187956111994733,
-0.301178882401688));
#50944=CARTESIAN_POINT('Ctrl Pts',(-0.284446679455652,0.301694033620098,
-0.307754570077918));
#50945=CARTESIAN_POINT('Ctrl Pts',(-0.16118073730096,0.382033941893919,
-0.314330257754149));
#50946=CARTESIAN_POINT('Ctrl Pts',(-0.0321942080223583,0.392610860537372,
-0.320905945430379));
#50947=CARTESIAN_POINT('Ctrl Pts',(0.0967923212562433,0.403187779180824,
-0.32748163310661));
#50948=CARTESIAN_POINT('Ctrl Pts',(0.231499437658754,0.344001708193907,
-0.33405732078284));
#50949=CARTESIAN_POINT('Ctrl Pts',(0.310953261656869,0.241842595997965,
-0.340633008459071));
#50950=CARTESIAN_POINT('Ctrl Pts',(0.390407085654983,0.139683483802024,
-0.347208696135302));
#50951=CARTESIAN_POINT('Ctrl Pts',(0.414607617248701,-0.00544866960294094,
-0.353784383811532));
#50952=CARTESIAN_POINT('Ctrl Pts',(0.372600716413692,-0.127861157977292,
-0.360360071487763));
#50953=CARTESIAN_POINT('Ctrl Pts',(0.330593815578682,-0.250273646351647,
-0.366935759163993));
#50954=CARTESIAN_POINT('Ctrl Pts',(0.222379482314941,-0.349966469695386,
-0.373511446840224));
#50955=CARTESIAN_POINT('Ctrl Pts',(0.0969398965000496,-0.381814644578891,
-0.380087134516455));
#50956=CARTESIAN_POINT('Ctrl Pts',(-0.0284996893148387,-0.413662819462395,
-0.386662822192686));
#50957=CARTESIAN_POINT('Ctrl Pts',(-0.171164527680877,-0.377666345885669,
-0.393238509868916));
#50958=CARTESIAN_POINT('Ctrl Pts',(-0.266478749744296,-0.290118673715471,
-0.399814197545147));
#50959=CARTESIAN_POINT('Ctrl Pts',(-0.3460533339709,-0.217028116376449,
-0.405304014295599));
#50960=CARTESIAN_POINT('Ctrl Pts',(-0.392624495852183,-0.108006327040057,
-0.410793831046051));
#50961=CARTESIAN_POINT('Ctrl Pts',(-0.393558983542489,0.000309099215769798,
-0.416283647796503));
#50962=CARTESIAN_POINT('Ctrl Pts',(-0.393587999858846,0.000300447727159551,
-0.434616352203498));
#50963=CARTESIAN_POINT('Ctrl Pts',(-0.392661402137344,-0.109031925299077,
-0.429073929389675));
#50964=CARTESIAN_POINT('Ctrl Pts',(-0.345088846953124,-0.219072095440072,
-0.423531506575852));
#50965=CARTESIAN_POINT('Ctrl Pts',(-0.264168911952582,-0.292223422497586,
-0.417989083762029));
#50966=CARTESIAN_POINT('Ctrl Pts',(-0.168163205203291,-0.379012232371915,
-0.411413396085799));
#50967=CARTESIAN_POINT('Ctrl Pts',(-0.02521731705165,-0.41387585365275,
-0.404837708409568));
#50968=CARTESIAN_POINT('Ctrl Pts',(0.0999656685633583,-0.381033604080488,
-0.398262020733337));
#50969=CARTESIAN_POINT('Ctrl Pts',(0.225148654178365,-0.348191354508227,
-0.391686333057106));
#50970=CARTESIAN_POINT('Ctrl Pts',(0.332568737256739,-0.24764323408287,
-0.385110645380876));
#50971=CARTESIAN_POINT('Ctrl Pts',(0.373603248787966,-0.124901381869836,
-0.378534957704645));
#50972=CARTESIAN_POINT('Ctrl Pts',(0.414637760319194,-0.00215952965679984,
-0.371959270028415));
#50973=CARTESIAN_POINT('Ctrl Pts',(0.389286700303273,0.142776054343914,
-0.365383582352184));
#50974=CARTESIAN_POINT('Ctrl Pts',(0.309024982211233,0.24430166525898,-0.358807894675953));
#50975=CARTESIAN_POINT('Ctrl Pts',(0.228763264119195,0.345827276174044,
-0.352232206999723));
#50976=CARTESIAN_POINT('Ctrl Pts',(0.0935908879510408,0.403942914003462,
-0.345656519323492));
#50977=CARTESIAN_POINT('Ctrl Pts',(-0.0353076671881922,0.392343101566332,
-0.339080831647261));
#50978=CARTESIAN_POINT('Ctrl Pts',(-0.164206222327427,0.380743289129201,
-0.332505143971031));
#50979=CARTESIAN_POINT('Ctrl Pts',(-0.286830956437741,0.29942802642552,
-0.3259294562948));
#50980=CARTESIAN_POINT('Ctrl Pts',(-0.347676962601307,0.185203870485553,
-0.319353768618569));
#50981=CARTESIAN_POINT('Ctrl Pts',(-0.377710977210929,0.128822027459561,
-0.316107963146879));
#50982=CARTESIAN_POINT('Ctrl Pts',(-0.39269273627193,0.0644220026535589,
-0.312862157675188));
#50983=CARTESIAN_POINT('Ctrl Pts',(-0.392673014342038,1.33379860697712E-5,
-0.309616352203498));
#50984=CARTESIAN_POINT('Origin',(0.,0.,-0.975));
#50985=CARTESIAN_POINT('',(-0.39357050162471,-0.000309514899277608,-0.166283647796502));
#50986=CARTESIAN_POINT('',(-0.393541380507519,-0.000314415350656495,-0.184616352203498));
#50987=CARTESIAN_POINT('',(-0.3933,-4.81653586104654E-17,-0.975));
#50988=CARTESIAN_POINT('Ctrl Pts',(-0.39357050162471,-0.000309514899277608,
-0.166283647796502));
#50989=CARTESIAN_POINT('Ctrl Pts',(-0.392638816960889,0.108414271758575,
-0.171794599940847));
#50990=CARTESIAN_POINT('Ctrl Pts',(-0.345667153138374,0.21784992059622,
-0.177305552085191));
#50991=CARTESIAN_POINT('Ctrl Pts',(-0.265552841170859,0.290968113516863,
-0.182816504229535));
#50992=CARTESIAN_POINT('Ctrl Pts',(-0.169960159525979,0.378213001061378,
-0.189392191905766));
#50993=CARTESIAN_POINT('Ctrl Pts',(-0.0271811390814353,0.413751465759291,
-0.195967879581997));
#50994=CARTESIAN_POINT('Ctrl Pts',(0.0981563482167165,0.381502906880402,
-0.202543567258227));
#50995=CARTESIAN_POINT('Ctrl Pts',(0.223493835514872,0.349254348001512,
-0.209119254934458));
#50996=CARTESIAN_POINT('Ctrl Pts',(0.331389789666634,0.249218765545815,
-0.215694942610689));
#50997=CARTESIAN_POINT('Ctrl Pts',(0.373006309497566,0.126673412826409,
-0.22227063028692));
#50998=CARTESIAN_POINT('Ctrl Pts',(0.414622829328497,0.00412806010700609,
-0.22884631796315));
#50999=CARTESIAN_POINT('Ctrl Pts',(0.389959914838601,-0.140927062876106,
-0.235422005639381));
#51000=CARTESIAN_POINT('Ctrl Pts',(0.310180910585397,-0.24283263818725,
-0.241997693315612));
#51001=CARTESIAN_POINT('Ctrl Pts',(0.230401906332192,-0.344738213498393,
-0.248573380991842));
#51002=CARTESIAN_POINT('Ctrl Pts',(0.0955068123156797,-0.403494241137569,
-0.255149068668073));
#51003=CARTESIAN_POINT('Ctrl Pts',(-0.0334453569779658,-0.392506156758443,
-0.261724756344303));
#51004=CARTESIAN_POINT('Ctrl Pts',(-0.162397526271611,-0.381518072379317,
-0.268300444020534));
#51005=CARTESIAN_POINT('Ctrl Pts',(-0.285406770842389,-0.300785875981889,
-0.274876131696764));
#51006=CARTESIAN_POINT('Ctrl Pts',(-0.346794160827309,-0.186851810294721,
-0.281451819372995));
#51007=CARTESIAN_POINT('Ctrl Pts',(-0.377389200992225,-0.130067879316267,
-0.284729095514164));
#51008=CARTESIAN_POINT('Ctrl Pts',(-0.392677649990676,-0.0650367535301259,
-0.288006371655333));
#51009=CARTESIAN_POINT('Ctrl Pts',(-0.392672644806505,-3.40218946998094E-6,
-0.291283647796502));
#51010=CARTESIAN_POINT('Ctrl Pts',(-0.392673014342038,1.33379860697712E-5,
-0.309616352203498));
#51011=CARTESIAN_POINT('Ctrl Pts',(-0.392652781551145,-0.0660637168975515,
-0.306286469998958));
#51012=CARTESIAN_POINT('Ctrl Pts',(-0.376843829560755,-0.132149865039833,
-0.302956587794418));
#51013=CARTESIAN_POINT('Ctrl Pts',(-0.345300981686382,-0.189596884509043,
-0.299626705589878));
#51014=CARTESIAN_POINT('Ctrl Pts',(-0.283011716391069,-0.303040434387422,
-0.293051017913647));
#51015=CARTESIAN_POINT('Ctrl Pts',(-0.159365907583621,-0.38279448496793,
-0.286475330237417));
#51016=CARTESIAN_POINT('Ctrl Pts',(-0.0303306494593879,-0.392759189393994,
-0.279899642561186));
#51017=CARTESIAN_POINT('Ctrl Pts',(0.098704608664847,-0.402723893820058,
-0.273323954884955));
#51018=CARTESIAN_POINT('Ctrl Pts',(0.23312931610587,-0.342899252091675,
-0.266748267208724));
#51019=CARTESIAN_POINT('Ctrl Pts',(0.312097431154972,-0.240364201991988,
-0.260172579532494));
#51020=CARTESIAN_POINT('Ctrl Pts',(0.391065546204075,-0.137829151892299,
-0.253596891856263));
#51021=CARTESIAN_POINT('Ctrl Pts',(0.414577068861256,0.00741630657869134,
-0.247021204180032));
#51022=CARTESIAN_POINT('Ctrl Pts',(0.37198971214902,0.12962799675346,-0.240445516503802));
#51023=CARTESIAN_POINT('Ctrl Pts',(0.329402355436786,0.251839686928225,
-0.233869828827571));
#51024=CARTESIAN_POINT('Ctrl Pts',(0.220716119355136,0.351017608806766,
-0.227294141151341));
#51025=CARTESIAN_POINT('Ctrl Pts',(0.0951268272738348,0.382270239135038,
-0.22071845347511));
#51026=CARTESIAN_POINT('Ctrl Pts',(-0.0304624648074687,0.413522869463311,
-0.214142765798879));
#51027=CARTESIAN_POINT('Ctrl Pts',(-0.172954812888427,0.376850208241315,
-0.207567078122649));
#51028=CARTESIAN_POINT('Ctrl Pts',(-0.26785250442914,0.288850996228523,
-0.200991390446418));
#51029=CARTESIAN_POINT('Ctrl Pts',(-0.346625169467209,0.215804620295093,
-0.195533044365445));
#51030=CARTESIAN_POINT('Ctrl Pts',(-0.392603563695526,0.107392576685488,
-0.190074698284471));
#51031=CARTESIAN_POINT('Ctrl Pts',(-0.393541380507519,-0.000314415350656495,
-0.184616352203498));
#51032=CARTESIAN_POINT('Origin',(0.,0.,-0.975));
#51033=CARTESIAN_POINT('',(-0.393507845663966,0.000361442601786236,-0.041283647796502));
#51034=CARTESIAN_POINT('',(-0.39355449651014,0.000302947205131077,-0.0596163522034978));
#51035=CARTESIAN_POINT('',(-0.3933,-4.81653586104654E-17,-0.975));
#51036=CARTESIAN_POINT('Ctrl Pts',(-0.393507845663966,0.000361442601786235,
-0.041283647796502));
#51037=CARTESIAN_POINT('Ctrl Pts',(-0.393708754658372,0.0229520255586643,
-0.0424314528738986));
#51038=CARTESIAN_POINT('Ctrl Pts',(-0.391919131196423,0.045518558677657,
-0.0435792579512952));
#51039=CARTESIAN_POINT('Ctrl Pts',(-0.388028994497127,0.0677340385174255,
-0.0447270630286917));
#51040=CARTESIAN_POINT('Ctrl Pts',(-0.365742698281716,0.195004826807769,
-0.0513027507049226));
#51041=CARTESIAN_POINT('Ctrl Pts',(-0.274516367855314,0.310753847632281,
-0.0578784383811535));
#51042=CARTESIAN_POINT('Ctrl Pts',(-0.155626506858587,0.361961149852793,
-0.0644541260573843));
#51043=CARTESIAN_POINT('Ctrl Pts',(-0.0367366458618627,0.413168452073304,
-0.0710298137336149));
#51044=CARTESIAN_POINT('Ctrl Pts',(0.109816745705184,0.399834035689818,
-0.0776055014098452));
#51045=CARTESIAN_POINT('Ctrl Pts',(0.217683740091212,0.328279870512349,
-0.0841811890860759));
#51046=CARTESIAN_POINT('Ctrl Pts',(0.32555073447724,0.256725705334881,-0.0907568767623065));
#51047=CARTESIAN_POINT('Ctrl Pts',(0.394731331682247,0.126951791363431,
-0.0973325644385373));
#51048=CARTESIAN_POINT('Ctrl Pts',(0.393919645176791,-0.00244560881035578,
-0.103908252114768));
#51049=CARTESIAN_POINT('Ctrl Pts',(0.393107958671335,-0.131843008984141,
-0.110483939790998));
#51050=CARTESIAN_POINT('Ctrl Pts',(0.322303988455414,-0.260863895360267,
-0.117059627467229));
#51051=CARTESIAN_POINT('Ctrl Pts',(0.213552187511225,-0.331033249415431,
-0.123635315143459));
#51052=CARTESIAN_POINT('Ctrl Pts',(0.10480038656703,-0.401202603470599,
-0.13021100281969));
#51053=CARTESIAN_POINT('Ctrl Pts',(-0.0418992451054321,-0.412520425204803,
-0.136786690495921));
#51054=CARTESIAN_POINT('Ctrl Pts',(-0.160142282896379,-0.359902860717048,
-0.143362378172152));
#51055=CARTESIAN_POINT('Ctrl Pts',(-0.278385320687322,-0.307285296229296,
-0.149938065848383));
#51056=CARTESIAN_POINT('Ctrl Pts',(-0.368171764596748,-0.190732345519584,
-0.156513753524613));
#51057=CARTESIAN_POINT('Ctrl Pts',(-0.38886181512885,-0.0629802149691723,
-0.163089441200844));
#51058=CARTESIAN_POINT('Ctrl Pts',(-0.392211948687912,-0.0422945864283189,
-0.16415417673273));
#51059=CARTESIAN_POINT('Ctrl Pts',(-0.393750506411561,-0.0213153367216679,
-0.165218912264616));
#51060=CARTESIAN_POINT('Ctrl Pts',(-0.39357050162471,-0.000309514899277608,
-0.166283647796502));
#51061=CARTESIAN_POINT('Ctrl Pts',(-0.393541380507519,-0.000314415350656495,
-0.184616352203498));
#51062=CARTESIAN_POINT('Ctrl Pts',(-0.393733354727773,-0.0223623948148967,
-0.18349901060824));
#51063=CARTESIAN_POINT('Ctrl Pts',(-0.392037973295506,-0.0443808301847042,
-0.182381669012983));
#51064=CARTESIAN_POINT('Ctrl Pts',(-0.38835019013725,-0.066060314914406,
-0.181264327417726));
#51065=CARTESIAN_POINT('Ctrl Pts',(-0.366647149304176,-0.193646651240961,
-0.174688639741495));
#51066=CARTESIAN_POINT('Ctrl Pts',(-0.275938032637555,-0.309493561090483,
-0.168112952065265));
#51067=CARTESIAN_POINT('Ctrl Pts',(-0.157281747236539,-0.361166943295072,
-0.161537264389034));
#51068=CARTESIAN_POINT('Ctrl Pts',(-0.0386254618355239,-0.412840325499661,
-0.154961576712803));
#51069=CARTESIAN_POINT('Ctrl Pts',(0.107977992299886,-0.400340180059318,
-0.148385889036573));
#51070=CARTESIAN_POINT('Ctrl Pts',(0.21617053708177,-0.329319039665975,
-0.141810201360342));
#51071=CARTESIAN_POINT('Ctrl Pts',(0.324363081863656,-0.258297899272631,
-0.135234513684112));
#51072=CARTESIAN_POINT('Ctrl Pts',(0.394144717292015,-0.128755763926285,
-0.128658826007881));
#51073=CARTESIAN_POINT('Ctrl Pts',(0.393928367963568,0.000660750832538935,
-0.12208313833165));
#51074=CARTESIAN_POINT('Ctrl Pts',(0.393712018635121,0.130077265591359,
-0.11550745065542));
#51075=CARTESIAN_POINT('Ctrl Pts',(0.323497684549871,0.259368159762656,
-0.108931762979189));
#51076=CARTESIAN_POINT('Ctrl Pts',(0.215069295256064,0.330031485880104,
-0.102356075302959));
#51077=CARTESIAN_POINT('Ctrl Pts',(0.106640905962253,0.400694811997555,
-0.095780387626728));
#51078=CARTESIAN_POINT('Ctrl Pts',(-0.0400015385401184,0.412730570061151,
-0.0892046999504971));
#51079=CARTESIAN_POINT('Ctrl Pts',(-0.158485743372544,0.360651915243996,
-0.0826290122742663));
#51080=CARTESIAN_POINT('Ctrl Pts',(-0.276969948204966,0.308573260426843,
-0.0760533245980357));
#51081=CARTESIAN_POINT('Ctrl Pts',(-0.367295913367443,0.192380192728942,
-0.0694776369218051));
#51082=CARTESIAN_POINT('Ctrl Pts',(-0.388570758753071,0.0647411738202655,
-0.0629019492455745));
#51083=CARTESIAN_POINT('Ctrl Pts',(-0.392114143238029,0.0434825413330083,
-0.061806750231549));
#51084=CARTESIAN_POINT('Ctrl Pts',(-0.393742061671785,0.0219064001501816,
-0.0607115512175234));
#51085=CARTESIAN_POINT('Ctrl Pts',(-0.39355449651014,0.000302947205131077,
-0.0596163522034978));
#51086=CARTESIAN_POINT('Origin',(0.,0.,-2.18777734492731));
#51087=CARTESIAN_POINT('',(-0.322496652456404,-0.000253620427588302,-0.125277344927309));
#51088=CARTESIAN_POINT('',(-0.322483537662866,0.00024823877578703,-0.100622655072689));
#51089=CARTESIAN_POINT('',(-0.322275,-3.08760083991297E-14,-2.18777734492731));
#51090=CARTESIAN_POINT('',(-0.104132061245188,0.305520369126831,-0.0250000000000002));
#51091=CARTESIAN_POINT('Ctrl Pts',(-0.322496652456404,-0.000253620427588306,
-0.125277344927308));
#51092=CARTESIAN_POINT('Ctrl Pts',(-0.322644150657985,-0.0174660568064599,
-0.124212609395423));
#51093=CARTESIAN_POINT('Ctrl Pts',(-0.313597410155885,-0.140824332617286,
-0.116572186187306));
#51094=CARTESIAN_POINT('Ctrl Pts',(-0.154540307687754,-0.347298426219855,
-0.102356075302959));
#51095=CARTESIAN_POINT('Ctrl Pts',(0.206082299461314,-0.319476526910996,
-0.0826290122742663));
#51096=CARTESIAN_POINT('Ctrl Pts',(0.380135308624816,-0.00231248299897462,
-0.0629019492455747));
#51097=CARTESIAN_POINT('Ctrl Pts',(0.214533253773463,0.308335699989221,
-0.0436922784874857));
#51098=CARTESIAN_POINT('Ctrl Pts',(-0.0114010986281019,0.336540681884783,
-0.0310582954056278));
#51099=CARTESIAN_POINT('Ctrl Pts',(-0.104132061245188,0.305520369126832,
-0.0250000000000003));
#51100=CARTESIAN_POINT('',(0.254670486854674,0.19749460435719,-0.0249999999999999));
#51101=CARTESIAN_POINT('Origin',(0.,0.,-0.0249999999999999));
#51102=CARTESIAN_POINT('Ctrl Pts',(-0.322483537662866,0.000248238775787049,
-0.100622655072689));
#51103=CARTESIAN_POINT('Ctrl Pts',(-0.321714440718607,-0.0883351074034859,
-0.0951421664104844));
#51104=CARTESIAN_POINT('Ctrl Pts',(-0.238074661536136,-0.284436749901765,
-0.0830859900720496));
#51105=CARTESIAN_POINT('Ctrl Pts',(0.0930026936990432,-0.368843116278878,
-0.0644541260573834));
#51106=CARTESIAN_POINT('Ctrl Pts',(0.359454556187757,-0.123370117592038,
-0.0447270630286919));
#51107=CARTESIAN_POINT('Ctrl Pts',(0.319948400855436,0.113318339423062,
-0.0315756876762305));
#51108=CARTESIAN_POINT('Ctrl Pts',(0.254670486854674,0.19749460435719,-0.0249999999999999));
#51109=CARTESIAN_POINT('Origin',(0.,0.,-2.18777734492731));
#51110=CARTESIAN_POINT('',(-0.321760937210822,-2.78779714989989E-6,-0.250277344927308));
#51111=CARTESIAN_POINT('',(-0.322472790244243,-0.000257635919520965,-0.225622655072689));
#51112=CARTESIAN_POINT('',(-0.322275,-3.08760083991297E-14,-2.18777734492731));
#51113=CARTESIAN_POINT('Ctrl Pts',(-0.321760937210822,-2.7877971498988E-6,
-0.250277344927308));
#51114=CARTESIAN_POINT('Ctrl Pts',(-0.321765038522105,-0.053291939343827,
-0.247000068786139));
#51115=CARTESIAN_POINT('Ctrl Pts',(-0.284101601363802,-0.213497576922093,
-0.23714710496874));
#51116=CARTESIAN_POINT('Ctrl Pts',(-0.032275256763624,-0.378773723290174,
-0.22071845347511));
#51117=CARTESIAN_POINT('Ctrl Pts',(0.299328987509231,-0.234337424225216,
-0.200991390446418));
#51118=CARTESIAN_POINT('Ctrl Pts',(0.359956300760417,0.122242589194944,
-0.181264327417726));
#51119=CARTESIAN_POINT('Ctrl Pts',(0.0947223676997066,0.368153857966175,
-0.161537264389034));
#51120=CARTESIAN_POINT('Ctrl Pts',(-0.237318620500534,0.285507073440862,
-0.142874936892228));
#51121=CARTESIAN_POINT('Ctrl Pts',(-0.321733218245798,0.0888360270302314,
-0.130788297071653));
#51122=CARTESIAN_POINT('Ctrl Pts',(-0.322496652456404,-0.000253620427588306,
-0.125277344927308));
#51123=CARTESIAN_POINT('Ctrl Pts',(-0.322472790244243,-0.000257635919520943,
-0.225622655072689));
#51124=CARTESIAN_POINT('Ctrl Pts',(-0.322630096351111,-0.0183240294660091,
-0.224505313477432));
#51125=CARTESIAN_POINT('Ctrl Pts',(-0.313065172617578,-0.142546609137769,
-0.216812284205945));
#51126=CARTESIAN_POINT('Ctrl Pts',(-0.151778919131785,-0.348529367587568,
-0.202543567258227));
#51127=CARTESIAN_POINT('Ctrl Pts',(0.208607260742278,-0.317801035232212,
-0.182816504229535));
#51128=CARTESIAN_POINT('Ctrl Pts',(0.380147127696309,0.000644362698709406,
-0.163089441200843));
#51129=CARTESIAN_POINT('Ctrl Pts',(0.207543584467282,0.318472150029413,
-0.143362378172152));
#51130=CARTESIAN_POINT('Ctrl Pts',(-0.152938443007933,0.348058907694893,
-0.12363531514346));
#51131=CARTESIAN_POINT('Ctrl Pts',(-0.313294198957135,0.141781264569365,
-0.109388740776972));
#51132=CARTESIAN_POINT('Ctrl Pts',(-0.322637230931287,0.0179503816638393,
-0.101717854086715));
#51133=CARTESIAN_POINT('Ctrl Pts',(-0.322483537662866,0.000248238775787049,
-0.100622655072689));
#51134=CARTESIAN_POINT('Origin',(0.,0.,-2.18777734492731));
#51135=CARTESIAN_POINT('',(-0.322487214393989,0.000253279811224501,-0.375277344927309));
#51136=CARTESIAN_POINT('',(-0.321761240012917,1.0929314634589E-5,-0.350622655072689));
#51137=CARTESIAN_POINT('',(-0.322275,-3.08760083991297E-14,-2.18777734492731));
#51138=CARTESIAN_POINT('Ctrl Pts',(-0.322487214393989,0.000253279811224492,
-0.375277344927309));
#51139=CARTESIAN_POINT('Ctrl Pts',(-0.321721483347979,-0.0885017519624719,
-0.369787528176857));
#51140=CARTESIAN_POINT('Ctrl Pts',(-0.237851341202248,-0.28483941242138,
-0.357722023750175));
#51141=CARTESIAN_POINT('Ctrl Pts',(0.093548368701956,-0.368456518342696,
-0.339080831647262));
#51142=CARTESIAN_POINT('Ctrl Pts',(0.359564953389757,-0.12338783304061,
-0.319353768618569));
#51143=CARTESIAN_POINT('Ctrl Pts',(0.300074287338146,0.233381539488646,
-0.299626705589878));
#51144=CARTESIAN_POINT('Ctrl Pts',(-0.0310678632234075,0.378874987446754,
-0.279899642561186));
#51145=CARTESIAN_POINT('Ctrl Pts',(-0.283744372563332,0.214190345213263,
-0.263449855673663));
#51146=CARTESIAN_POINT('Ctrl Pts',(-0.321756809449883,0.0536300293912535,
-0.25357575646237));
#51147=CARTESIAN_POINT('Ctrl Pts',(-0.321760937210822,-2.7877971498988E-6,
-0.250277344927308));
#51148=CARTESIAN_POINT('Ctrl Pts',(-0.321761240012917,1.09293146345925E-5,
-0.350622655072689));
#51149=CARTESIAN_POINT('Ctrl Pts',(-0.321744661007864,-0.0541334461306104,
-0.34729277286815));
#51150=CARTESIAN_POINT('Ctrl Pts',(-0.283209573736967,-0.215221637656999,
-0.33738720298738));
#51151=CARTESIAN_POINT('Ctrl Pts',(-0.029269501228293,-0.379018126859581,
-0.320905945430379));
#51152=CARTESIAN_POINT('Ctrl Pts',(0.301178420896456,-0.231954920047871,
-0.301178882401687));
#51153=CARTESIAN_POINT('Ctrl Pts',(0.358975339007382,0.125092983298727,
-0.281451819372995));
#51154=CARTESIAN_POINT('Ctrl Pts',(0.0917987048867537,0.368895918259873,
-0.261724756344303));
#51155=CARTESIAN_POINT('Ctrl Pts',(-0.238641519661772,0.283851896091718,
-0.243115034910868));
#51156=CARTESIAN_POINT('Ctrl Pts',(-0.321704331273786,0.0879988371505342,
-0.231081001153663));
#51157=CARTESIAN_POINT('Ctrl Pts',(-0.322472790244243,-0.000257635919520943,
-0.225622655072689));
#51158=CARTESIAN_POINT('Origin',(0.,0.,-2.18777734492731));
#51159=CARTESIAN_POINT('',(-0.322468464145128,-0.000258307126375694,-0.500277344927309));
#51160=CARTESIAN_POINT('',(-0.322510990731018,0.000246190671888573,-0.475622655072689));
#51161=CARTESIAN_POINT('',(-0.322275,-3.08760083991297E-14,-2.18777734492731));
#51162=CARTESIAN_POINT('Ctrl Pts',(-0.322468464145128,-0.000258307126375657,
-0.500277344927309));
#51163=CARTESIAN_POINT('Ctrl Pts',(-0.322627489692965,-0.0184761631570425,
-0.499150675243805));
#51164=CARTESIAN_POINT('Ctrl Pts',(-0.312969978781256,-0.142852070661369,
-0.49144831788407));
#51165=CARTESIAN_POINT('Ctrl Pts',(-0.151288792665831,-0.348745193702454,
-0.477170272848105));
#51166=CARTESIAN_POINT('Ctrl Pts',(0.209054616084237,-0.317502246064031,
-0.457443209819413));
#51167=CARTESIAN_POINT('Ctrl Pts',(0.380144895279971,0.00116938758285907,
-0.437716146790722));
#51168=CARTESIAN_POINT('Ctrl Pts',(0.207097300423056,0.318782398141369,
-0.41798908376203));
#51169=CARTESIAN_POINT('Ctrl Pts',(-0.15343150362219,0.34780782307336,-0.398262020733337));
#51170=CARTESIAN_POINT('Ctrl Pts',(-0.313384552995844,0.141515052741351,
-0.384024774455097));
#51171=CARTESIAN_POINT('Ctrl Pts',(-0.322638673926724,0.0178087853773642,
-0.376363215853088));
#51172=CARTESIAN_POINT('Ctrl Pts',(-0.322487214393989,0.000253279811224492,
-0.375277344927309));
#51173=CARTESIAN_POINT('Ctrl Pts',(-0.322510990731018,0.000246190671888582,
-0.475622655072689));
#51174=CARTESIAN_POINT('Ctrl Pts',(-0.321751724825343,-0.0893421401621455,
-0.470080232258867));
#51175=CARTESIAN_POINT('Ctrl Pts',(-0.236521348985171,-0.286488688677642,
-0.457962121768814));
#51176=CARTESIAN_POINT('Ctrl Pts',(0.096468281849101,-0.367702807740199,
-0.43926832360253));
#51177=CARTESIAN_POINT('Ctrl Pts',(0.360532410560641,-0.120531598662528,
-0.419541260573839));
#51178=CARTESIAN_POINT('Ctrl Pts',(0.298213471837286,0.235754559490252,
-0.399814197545147));
#51179=CARTESIAN_POINT('Ctrl Pts',(-0.0340723979536573,0.378616627998834,
-0.380087134516455));
#51180=CARTESIAN_POINT('Ctrl Pts',(-0.284630677265904,0.212465708670196,
-0.363689953692302));
#51181=CARTESIAN_POINT('Ctrl Pts',(-0.321777400411997,0.0527882046914952,
-0.35386846054438));
#51182=CARTESIAN_POINT('Ctrl Pts',(-0.321761240012917,1.09293146345925E-5,
-0.350622655072689));
#51183=CARTESIAN_POINT('Origin',(0.,0.,-2.18777734492731));
#51184=CARTESIAN_POINT('',(-0.32176143791031,1.33594009879692E-5,-0.625277344927309));
#51185=CARTESIAN_POINT('',(-0.322443941546287,-0.000264174642984033,-0.600622655072689));
#51186=CARTESIAN_POINT('',(-0.322275,-3.08760083991297E-14,-2.18777734492731));
#51187=CARTESIAN_POINT('Ctrl Pts',(-0.32176143791031,1.33594009879487E-5,
-0.625277344927309));
#51188=CARTESIAN_POINT('Ctrl Pts',(-0.32174112470711,-0.0542826208959099,
-0.621938134634522));
#51189=CARTESIAN_POINT('Ctrl Pts',(-0.283050431304305,-0.215527298967927,
-0.612023236665505));
#51190=CARTESIAN_POINT('Ctrl Pts',(-0.0287363371895775,-0.37905900832026,
-0.595532651020257));
#51191=CARTESIAN_POINT('Ctrl Pts',(0.30150443573772,-0.231530957091147,
-0.575805587991564));
#51192=CARTESIAN_POINT('Ctrl Pts',(0.358799032608658,0.125597623625804,
-0.556078524962874));
#51193=CARTESIAN_POINT('Ctrl Pts',(0.0912797550693568,0.36902508747417,
-0.53635146193418));
#51194=CARTESIAN_POINT('Ctrl Pts',(-0.238875075374452,0.283558159143536,
-0.517751068588993));
#51195=CARTESIAN_POINT('Ctrl Pts',(-0.321699354010936,0.0878504143147682,
-0.505726362920035));
#51196=CARTESIAN_POINT('Ctrl Pts',(-0.322468464145128,-0.000258307126375657,
-0.500277344927309));
#51197=CARTESIAN_POINT('Ctrl Pts',(-0.322443941546287,-0.000264174642983971,
-0.600622655072689));
#51198=CARTESIAN_POINT('Ctrl Pts',(-0.32261252448504,-0.0193364043208577,
-0.599443379325814));
#51199=CARTESIAN_POINT('Ctrl Pts',(-0.312428596949323,-0.144576424763027,
-0.591688415902709));
#51200=CARTESIAN_POINT('Ctrl Pts',(-0.148517520713027,-0.349934323902057,
-0.577357764803375));
#51201=CARTESIAN_POINT('Ctrl Pts',(0.211566678587274,-0.315833857421815,
-0.557630701774681));
#51202=CARTESIAN_POINT('Ctrl Pts',(0.380123626347935,0.00418493532934027,
-0.537903638745991));
#51203=CARTESIAN_POINT('Ctrl Pts',(0.204561954486446,0.320415186635358,
-0.518176575717298));
#51204=CARTESIAN_POINT('Ctrl Pts',(-0.156185726714996,0.346579721946209,
-0.498449512688607));
#51205=CARTESIAN_POINT('Ctrl Pts',(-0.313912311423948,0.139791502294731,
-0.484264872473737));
#51206=CARTESIAN_POINT('Ctrl Pts',(-0.322652539437768,0.0169479973441946,
-0.476655919935097));
#51207=CARTESIAN_POINT('Ctrl Pts',(-0.322510990731018,0.000246190671888582,
-0.475622655072689));
#51208=CARTESIAN_POINT('Origin',(0.,0.,-2.18777734492731));
#51209=CARTESIAN_POINT('',(-0.322515189627379,0.000244863147638563,-0.750277344927309));
#51210=CARTESIAN_POINT('',(-0.321763022562619,2.70116077047966E-5,-0.72562265507269));
#51211=CARTESIAN_POINT('',(-0.322275,-3.08760083991297E-14,-2.18777734492731));
#51212=CARTESIAN_POINT('Ctrl Pts',(-0.322515189627379,0.000244863147638597,
-0.750277344927309));
#51213=CARTESIAN_POINT('Ctrl Pts',(-0.321757324772481,-0.0894912350280718,
-0.744725594025239));
#51214=CARTESIAN_POINT('Ctrl Pts',(-0.236284363982717,-0.286780837770945,
-0.73259815544694));
#51215=CARTESIAN_POINT('Ctrl Pts',(0.0969854205621785,-0.36756677904974,
-0.713895029192408));
#51216=CARTESIAN_POINT('Ctrl Pts',(0.36070162869546,-0.120024347192654,
-0.694167966163718));
#51217=CARTESIAN_POINT('Ctrl Pts',(0.297881578716796,0.236173821419171,
-0.674440903135024));
#51218=CARTESIAN_POINT('Ctrl Pts',(-0.0346049444254762,0.378568364610783,
-0.654713840106333));
#51219=CARTESIAN_POINT('Ctrl Pts',(-0.284786878082418,0.212159852647683,
-0.638325987370427));
#51220=CARTESIAN_POINT('Ctrl Pts',(-0.32178112616501,0.0526388896416031,
-0.628513822310753));
#51221=CARTESIAN_POINT('Ctrl Pts',(-0.32176143791031,1.33594009879487E-5,
-0.625277344927309));
#51222=CARTESIAN_POINT('Ctrl Pts',(-0.321763022562619,2.70116077047897E-5,
-0.72562265507269));
#51223=CARTESIAN_POINT('Ctrl Pts',(-0.32172129192177,-0.0551236550340476,
-0.722230838716532));
#51224=CARTESIAN_POINT('Ctrl Pts',(-0.282147174958169,-0.217250635635261,
-0.712263334684144));
#51225=CARTESIAN_POINT('Ctrl Pts',(-0.0257284602956936,-0.379275007515933,
-0.695720142975526));
#51226=CARTESIAN_POINT('Ctrl Pts',(0.303331595228502,-0.22913190160076,
-0.675993079946833));
#51227=CARTESIAN_POINT('Ctrl Pts',(0.357791382294441,0.128439914943824,
-0.656266016918142));
#51228=CARTESIAN_POINT('Ctrl Pts',(0.0883495014317826,0.369737542850607,
-0.63653895388945));
#51229=CARTESIAN_POINT('Ctrl Pts',(-0.240185123468634,0.281903402878257,
-0.617991166607633));
#51230=CARTESIAN_POINT('Ctrl Pts',(-0.321672499426679,0.0870110941191312,
-0.606019067002045));
#51231=CARTESIAN_POINT('Ctrl Pts',(-0.322443941546287,-0.000264174642983971,
-0.600622655072689));
#51232=CARTESIAN_POINT('Origin',(0.,0.,-2.18777734492731));
#51233=CARTESIAN_POINT('',(-0.32243959144629,-0.00026514217618365,-0.875277344927309));
#51234=CARTESIAN_POINT('',(-0.322538390303182,0.000236984608253048,-0.850622655072689));
#51235=CARTESIAN_POINT('',(-0.322275,-3.08760083991297E-14,-2.18777734492731));
#51236=CARTESIAN_POINT('Ctrl Pts',(-0.32243959144629,-0.00026514217618364,
-0.875277344927309));
#51237=CARTESIAN_POINT('Ctrl Pts',(-0.322609842324708,-0.0194889104434921,
-0.874088741092187));
#51238=CARTESIAN_POINT('Ctrl Pts',(-0.312331827063556,-0.144882247836869,
-0.866324449580835));
#51239=CARTESIAN_POINT('Ctrl Pts',(-0.148025153650298,-0.350142917605659,
-0.851984470393253));
#51240=CARTESIAN_POINT('Ctrl Pts',(0.212010751987255,-0.315535972441172,
-0.832257407364559));
#51241=CARTESIAN_POINT('Ctrl Pts',(0.380117394971352,0.00471962951840088,
-0.81253034433587));
#51242=CARTESIAN_POINT('Ctrl Pts',(0.204111059463726,0.320702641503297,
-0.792803281307175));
#51243=CARTESIAN_POINT('Ctrl Pts',(-0.156673098749063,0.346359710403747,
-0.773076218278485));
#51244=CARTESIAN_POINT('Ctrl Pts',(-0.314005130821476,0.139485946692706,
-0.758900906151862));
#51245=CARTESIAN_POINT('Ctrl Pts',(-0.322654966376816,0.0167953338932892,
-0.75130128170147));
#51246=CARTESIAN_POINT('Ctrl Pts',(-0.322515189627379,0.000244863147638597,
-0.750277344927309));
#51247=CARTESIAN_POINT('Ctrl Pts',(-0.322538390303182,0.000236984608253082,
-0.85062265507269));
#51248=CARTESIAN_POINT('Ctrl Pts',(-0.321789907494861,-0.0903324194305184,
-0.845018298107249));
#51249=CARTESIAN_POINT('Ctrl Pts',(-0.234941113718784,-0.288426386720931,
-0.832838253465578));
#51250=CARTESIAN_POINT('Ctrl Pts',(0.0998981666172007,-0.366785824837531,
-0.814082521147678));
#51251=CARTESIAN_POINT('Ctrl Pts',(0.361642369567447,-0.117159214442841,
-0.794355458118984));
#51252=CARTESIAN_POINT('Ctrl Pts',(0.295998679758828,0.238529383045872,
-0.774628395090294));
#51253=CARTESIAN_POINT('Ctrl Pts',(-0.0376069309429452,0.37828191040585,
-0.754901332061601));
#51254=CARTESIAN_POINT('Ctrl Pts',(-0.285662062070785,0.210434559988762,
-0.738566085389067));
#51255=CARTESIAN_POINT('Ctrl Pts',(-0.321802194786766,0.0517965083508985,
-0.728806526392763));
#51256=CARTESIAN_POINT('Ctrl Pts',(-0.321763022562619,2.70116077047897E-5,
-0.72562265507269));
#51257=CARTESIAN_POINT('Origin',(0.,0.,-2.18777734492731));
#51258=CARTESIAN_POINT('',(-0.321763448536774,2.94270121017112E-5,-1.00027734492731));
#51259=CARTESIAN_POINT('',(-0.322414722935121,-0.000270183965801862,-0.97562265507269));
#51260=CARTESIAN_POINT('',(-0.322275,-3.08760083991297E-14,-2.18777734492731));
#51261=CARTESIAN_POINT('Ctrl Pts',(-0.321763448536774,2.94270121016932E-5,
-1.00027734492731));
#51262=CARTESIAN_POINT('Ctrl Pts',(-0.321717858026619,-0.0552727465775086,
-0.996876200482905));
#51263=CARTESIAN_POINT('Ctrl Pts',(-0.281986038527001,-0.217556162740986,
-0.986899368362269));
#51264=CARTESIAN_POINT('Ctrl Pts',(-0.0251949327277424,-0.379310854349625,
-0.970346848565404));
#51265=CARTESIAN_POINT('Ctrl Pts',(0.303653626791853,-0.228705014808928,
-0.950619785536712));
#51266=CARTESIAN_POINT('Ctrl Pts',(0.357610388862838,0.128943082947354,
-0.930892722508019));
#51267=CARTESIAN_POINT('Ctrl Pts',(0.0878293328830358,0.3698614837313,-0.911165659479328));
#51268=CARTESIAN_POINT('Ctrl Pts',(-0.240416277942781,0.281609698819248,
-0.892627200285757));
#51269=CARTESIAN_POINT('Ctrl Pts',(-0.321667967016886,0.0868623332180409,
-0.880664428768418));
#51270=CARTESIAN_POINT('Ctrl Pts',(-0.32243959144629,-0.00026514217618364,
-0.875277344927309));
#51271=CARTESIAN_POINT('Ctrl Pts',(-0.322414722935121,-0.000270183965801866,
-0.97562265507269));
#51272=CARTESIAN_POINT('Ctrl Pts',(-0.322594207704359,-0.0203487694477343,
-0.974381445174198));
#51273=CARTESIAN_POINT('Ctrl Pts',(-0.311781374671243,-0.146607127922807,
-0.966564547599475));
#51274=CARTESIAN_POINT('Ctrl Pts',(-0.145242896892136,-0.351306114233161,
-0.952171962348521));
#51275=CARTESIAN_POINT('Ctrl Pts',(0.214507123315248,-0.313844195489162,
-0.932444899319828));
#51276=CARTESIAN_POINT('Ctrl Pts',(0.380067963842326,0.00773484686148907,
-0.912717836291137));
#51277=CARTESIAN_POINT('Ctrl Pts',(0.20156057492959,0.322311680876253,-0.892990773262445));
#51278=CARTESIAN_POINT('Ctrl Pts',(-0.159415732015043,0.345105939359686,
-0.873263710233753));
#51279=CARTESIAN_POINT('Ctrl Pts',(-0.314523961336012,0.137762968037702,
-0.859141004170502));
#51280=CARTESIAN_POINT('Ctrl Pts',(-0.322668115148103,0.015934208061963,
-0.85159398578348));
#51281=CARTESIAN_POINT('Ctrl Pts',(-0.322538390303182,0.000236984608253082,
-0.85062265507269));
#51282=CARTESIAN_POINT('Origin',(0.,0.,-2.18777734492731));
#51283=CARTESIAN_POINT('',(-0.322542478777324,0.000235518785689083,-1.12527734492731));
#51284=CARTESIAN_POINT('',(-0.321766314000566,4.30053259428964E-5,-1.10062265507269));
#51285=CARTESIAN_POINT('',(-0.322275,-3.08760083991297E-14,-2.18777734492731));
#51286=CARTESIAN_POINT('Ctrl Pts',(-0.322542478777324,0.000235518785689073,
-1.12527734492731));
#51287=CARTESIAN_POINT('Ctrl Pts',(-0.321795926838285,-0.0904816611753488,
-1.11966365987362));
#51288=CARTESIAN_POINT('Ctrl Pts',(-0.234701773596145,-0.288717865815097,
-1.1074742871437));
#51289=CARTESIAN_POINT('Ctrl Pts',(0.100414012462523,-0.366644971278448,
-1.08870922673756));
#51290=CARTESIAN_POINT('Ctrl Pts',(0.361806842748681,-0.116650406783812,
-1.06898216370886));
#51291=CARTESIAN_POINT('Ctrl Pts',(0.295662885863291,0.2389455310015,-1.04925510068017));
#51292=CARTESIAN_POINT('Ctrl Pts',(-0.0381390041496891,0.378228667904838,
-1.02952803765148));
#51293=CARTESIAN_POINT('Ctrl Pts',(-0.285816294598986,0.210128591668202,
-1.01320211906719));
#51294=CARTESIAN_POINT('Ctrl Pts',(-0.321806001579673,0.0516470938721495,
-1.00345188815914));
#51295=CARTESIAN_POINT('Ctrl Pts',(-0.321763448536774,2.94270121016932E-5,
-1.00027734492731));
#51296=CARTESIAN_POINT('Ctrl Pts',(-0.321766314000566,4.30053259428721E-5,
-1.10062265507269));
#51297=CARTESIAN_POINT('Ctrl Pts',(-0.321698621501294,-0.0561132696767489,
-1.09716890456491));
#51298=CARTESIAN_POINT('Ctrl Pts',(-0.281071497630043,-0.219278629537744,
-1.08713946638091));
#51299=CARTESIAN_POINT('Ctrl Pts',(-0.022185169729932,-0.379498752618868,
-1.07053434052067));
#51300=CARTESIAN_POINT('Ctrl Pts',(0.305458301062517,-0.226288999527647,
-1.05080727749198));
#51301=CARTESIAN_POINT('Ctrl Pts',(0.356576237443244,0.131775839538367,
-1.03108021446329));
#51302=CARTESIAN_POINT('Ctrl Pts',(0.0848925531951284,0.370546541485998,
-1.0113531514346));
#51303=CARTESIAN_POINT('Ctrl Pts',(-0.241713188057519,0.279951469622511,
-0.992867298304396));
#51304=CARTESIAN_POINT('Ctrl Pts',(-0.321643332444194,0.0860236557722655,
-0.980957132850428));
#51305=CARTESIAN_POINT('Ctrl Pts',(-0.322414722935121,-0.000270183965801866,
-0.97562265507269));
#51306=CARTESIAN_POINT('Origin',(0.,0.,-2.18777734492731));
#51307=CARTESIAN_POINT('',(-0.322410319385532,-0.000271004193501387,-1.25027734492731));
#51308=CARTESIAN_POINT('',(-0.322565009168808,0.000226870584957552,-1.22562265507269));
#51309=CARTESIAN_POINT('',(-0.322275,-3.08760083991297E-14,-2.18777734492731));
#51310=CARTESIAN_POINT('Ctrl Pts',(-0.322410319385532,-0.000271004193501456,
-1.25027734492731));
#51311=CARTESIAN_POINT('Ctrl Pts',(-0.32259140864452,-0.0205012064117319,
-1.24902680694057));
#51312=CARTESIAN_POINT('Ctrl Pts',(-0.311682991233502,-0.146913042759608,
-1.2412005812776));
#51313=CARTESIAN_POINT('Ctrl Pts',(-0.144748603181605,-0.351510100480195,
-1.2267986679384));
#51314=CARTESIAN_POINT('Ctrl Pts',(0.214948395308735,-0.313542176137101,
-1.20707160490971));
#51315=CARTESIAN_POINT('Ctrl Pts',(0.380056739056546,0.00826945949266903,
-1.18734454188101));
#51316=CARTESIAN_POINT('Ctrl Pts',(0.201107014947573,0.322594912237434,
-1.16761747885232));
#51317=CARTESIAN_POINT('Ctrl Pts',(-0.15990102805103,0.344881385538304,
-1.14789041582363));
#51318=CARTESIAN_POINT('Ctrl Pts',(-0.314615202650056,0.137457515057215,
-1.13377703784863));
#51319=CARTESIAN_POINT('Ctrl Pts',(-0.322670413443474,0.0157814862202043,
-1.12623934754985));
#51320=CARTESIAN_POINT('Ctrl Pts',(-0.322542478777324,0.000235518785689073,
-1.12527734492731));
#51321=CARTESIAN_POINT('Ctrl Pts',(-0.322565009168808,0.00022687058495755,
-1.22562265507269));
#51322=CARTESIAN_POINT('Ctrl Pts',(-0.321830898403645,-0.0913237050652294,
-1.21995636395563));
#51323=CARTESIAN_POINT('Ctrl Pts',(-0.233345219009216,-0.290359580072423,
-1.20771438516234));
#51324=CARTESIAN_POINT('Ctrl Pts',(0.103319337909045,-0.365836848074736,
-1.18889671869282));
#51325=CARTESIAN_POINT('Ctrl Pts',(0.362720784217591,-0.113776613114465,
-1.16916965566413));
#51326=CARTESIAN_POINT('Ctrl Pts',(0.293758069692678,0.241283404911434,
-1.14944259263544));
#51327=CARTESIAN_POINT('Ctrl Pts',(-0.0411381844576584,0.377914189697542,
-1.12971552960675));
#51328=CARTESIAN_POINT('Ctrl Pts',(-0.286680415754695,0.208402634031067,
-1.11344221708583));
#51329=CARTESIAN_POINT('Ctrl Pts',(-0.321827503055486,0.050804159548938,
-1.10374459224114));
#51330=CARTESIAN_POINT('Ctrl Pts',(-0.321766314000566,4.30053259428721E-5,
-1.10062265507269));
#51331=CARTESIAN_POINT('Origin',(0.,0.,-2.18777734492731));
#51332=CARTESIAN_POINT('',(-0.321766966566369,4.5403904709377E-5,-1.37527734492731));
#51333=CARTESIAN_POINT('',(-0.322385193379531,-0.000275211153700466,-1.35062265507269));
#51334=CARTESIAN_POINT('',(-0.322275,-3.08760083991297E-14,-2.18777734492731));
#51335=CARTESIAN_POINT('Ctrl Pts',(-0.321766966566369,4.54039047093589E-5,
-1.37527734492731));
#51336=CARTESIAN_POINT('Ctrl Pts',(-0.321695297543061,-0.0562622719711204,
-1.37181426633129));
#51337=CARTESIAN_POINT('Ctrl Pts',(-0.280908354535491,-0.21958399720779,
-1.36177550005904));
#51338=CARTESIAN_POINT('Ctrl Pts',(-0.0216513306458494,-0.379529615109383,
-1.34516104611055));
#51339=CARTESIAN_POINT('Ctrl Pts',(0.305776331751614,-0.225859123798109,
-1.32543398308186));
#51340=CARTESIAN_POINT('Ctrl Pts',(0.356390552660915,0.132277295241747,
-1.30570692005317));
#51341=CARTESIAN_POINT('Ctrl Pts',(0.0843712498095106,0.370665618945638,
-1.28597985702447));
#51342=CARTESIAN_POINT('Ctrl Pts',(-0.241942017400318,0.279657158481209,
-1.26750333198252));
#51343=CARTESIAN_POINT('Ctrl Pts',(-0.321639189342704,0.0858750035272477,
-1.2556024946168));
#51344=CARTESIAN_POINT('Ctrl Pts',(-0.322410319385532,-0.000271004193501456,
-1.25027734492731));
#51345=CARTESIAN_POINT('Ctrl Pts',(-0.322385193379531,-0.000275211153700449,
-1.35062265507269));
#51346=CARTESIAN_POINT('Ctrl Pts',(-0.322575125249444,-0.0213606665813696,
-1.34931951102258));
#51347=CARTESIAN_POINT('Ctrl Pts',(-0.311123410622023,-0.148638429323664,
-1.34144067929624));
#51348=CARTESIAN_POINT('Ctrl Pts',(-0.141955604305407,-0.352647262007924,
-1.32698615989367));
#51349=CARTESIAN_POINT('Ctrl Pts',(0.217428857727536,-0.311827158571008,
-1.30725909686498));
#51350=CARTESIAN_POINT('Ctrl Pts',(0.37997915002097,0.0112840836821547,
-1.28753203383628));
#51351=CARTESIAN_POINT('Ctrl Pts',(0.198541614321699,0.324180061659845,
-1.26780497080759));
#51352=CARTESIAN_POINT('Ctrl Pts',(-0.16263183234255,0.343602054860151,
-1.2480779077789));
#51353=CARTESIAN_POINT('Ctrl Pts',(-0.31512516123277,0.135735123126218,
-1.23401713586727));
#51354=CARTESIAN_POINT('Ctrl Pts',(-0.32268282835425,0.0149200405556859,
-1.22653205163186));
#51355=CARTESIAN_POINT('Ctrl Pts',(-0.322565009168808,0.00022687058495755,
-1.22562265507269));
#51356=CARTESIAN_POINT('Origin',(0.,0.,-2.18777734492731));
#51357=CARTESIAN_POINT('',(-0.322568970321137,0.00022527015596577,-1.50027734492731));
#51358=CARTESIAN_POINT('',(-0.321771106026149,5.88663889491414E-5,-1.47562265507269));
#51359=CARTESIAN_POINT('',(-0.322275,-3.08760083991297E-14,-2.18777734492731));
#51360=CARTESIAN_POINT('Ctrl Pts',(-0.322568970321137,0.000225270155965756,
-1.50027734492731));
#51361=CARTESIAN_POINT('Ctrl Pts',(-0.321837345546539,-0.0914731051590046,
-1.49460172572201));
#51362=CARTESIAN_POINT('Ctrl Pts',(-0.233103515511503,-0.290650369905947,
-1.48235041884047));
#51363=CARTESIAN_POINT('Ctrl Pts',(0.103833845766363,-0.365691183090615,
-1.4635234242827));
#51364=CARTESIAN_POINT('Ctrl Pts',(0.362880498319019,-0.113266291538057,
-1.44379636125401));
#51365=CARTESIAN_POINT('Ctrl Pts',(0.293418403901249,0.24169639861178,-1.42406929822532));
#51366=CARTESIAN_POINT('Ctrl Pts',(-0.0416697372088447,0.377855980330849,
-1.40434223519663));
#51367=CARTESIAN_POINT('Ctrl Pts',(-0.286832692350314,0.208096552551141,
-1.38807825076396));
#51368=CARTESIAN_POINT('Ctrl Pts',(-0.321831382561136,0.0506546460448801,
-1.37838995400752));
#51369=CARTESIAN_POINT('Ctrl Pts',(-0.321766966566369,4.54039047093589E-5,
-1.37527734492731));
#51370=CARTESIAN_POINT('Ctrl Pts',(-0.321771106026149,5.88663889491171E-5,
-1.47562265507269));
#51371=CARTESIAN_POINT('Ctrl Pts',(-0.321676704902483,-0.0571022987504526,
-1.4721069704133));
#51372=CARTESIAN_POINT('Ctrl Pts',(-0.279982466127999,-0.221305532991997,
-1.46201559807767));
#51373=CARTESIAN_POINT('Ctrl Pts',(-0.0186399440734759,-0.37968939607062,
-1.44534853806582));
#51374=CARTESIAN_POINT('Ctrl Pts',(0.307558363392102,-0.223426359459979,
-1.42562147503713));
#51375=CARTESIAN_POINT('Ctrl Pts',(0.355329990338077,0.135100270022,-1.40589441200844));
#51376=CARTESIAN_POINT('Ctrl Pts',(0.0814282002323064,0.371323219316239,
-1.38616734897974));
#51377=CARTESIAN_POINT('Ctrl Pts',(-0.243225838729499,0.277995556675306,
-1.36774343000116));
#51378=CARTESIAN_POINT('Ctrl Pts',(-0.321616725710878,0.085036910410772,
-1.35589519869881));
#51379=CARTESIAN_POINT('Ctrl Pts',(-0.322385193379531,-0.000275211153700449,
-1.35062265507269));
#51380=CARTESIAN_POINT('Origin',(0.,0.,-2.18777734492731));
#51381=CARTESIAN_POINT('',(-0.322380752027636,-0.000275883433438568,-1.62527734492731));
#51382=CARTESIAN_POINT('',(-0.322590734421357,0.00021587490590607,-1.60062265507269));
#51383=CARTESIAN_POINT('',(-0.322275,-3.08760083991297E-14,-2.18777734492731));
#51384=CARTESIAN_POINT('Ctrl Pts',(-0.322380752027636,-0.000275883433438602,
-1.62527734492731));
#51385=CARTESIAN_POINT('Ctrl Pts',(-0.322572213417517,-0.0215130334452361,
-1.62396487278895));
#51386=CARTESIAN_POINT('Ctrl Pts',(-0.31102340500336,-0.148944440860085,
-1.61607671297436));
#51387=CARTESIAN_POINT('Ctrl Pts',(-0.141459425625526,-0.352846615539549,
-1.60161286548355));
#51388=CARTESIAN_POINT('Ctrl Pts',(0.217867289073768,-0.311521035102426,
-1.58188580245485));
#51389=CARTESIAN_POINT('Ctrl Pts',(0.379962933199995,0.0118185701951804,
-1.56215873942616));
#51390=CARTESIAN_POINT('Ctrl Pts',(0.198085428729991,0.324459043670616,
-1.54243167639747));
#51391=CARTESIAN_POINT('Ctrl Pts',(-0.163115009928593,0.343372979052334,
-1.52270461336878));
#51392=CARTESIAN_POINT('Ctrl Pts',(-0.315214834387717,0.135429775293384,
-1.50865316954539));
#51393=CARTESIAN_POINT('Ctrl Pts',(-0.322684995087483,0.0147672634558229,
-1.50117741339824));
#51394=CARTESIAN_POINT('Ctrl Pts',(-0.322568970321137,0.000225270155965756,
-1.50027734492731));
#51395=CARTESIAN_POINT('Ctrl Pts',(-0.322590734421357,0.000215874905906053,
-1.60062265507269));
#51396=CARTESIAN_POINT('Ctrl Pts',(-0.321874753260051,-0.0923160744138115,
-1.59489442980401));
#51397=CARTESIAN_POINT('Ctrl Pts',(-0.231733610569791,-0.292288142917499,
-1.58259051685911));
#51398=CARTESIAN_POINT('Ctrl Pts',(0.106731497010161,-0.36485596183739,
-1.56371091623797));
#51399=CARTESIAN_POINT('Ctrl Pts',(0.363767560759545,-0.110384087378192,
-1.54398385320928));
#51400=CARTESIAN_POINT('Ctrl Pts',(0.291491836616472,0.244016380761125,
-1.52425679018059));
#51401=CARTESIAN_POINT('Ctrl Pts',(-0.0446658496794004,0.377513505615764,
-1.50452972715189));
#51402=CARTESIAN_POINT('Ctrl Pts',(-0.287685814152671,0.206369985421987,
-1.4883183487826));
#51403=CARTESIAN_POINT('Ctrl Pts',(-0.321853271450867,0.0498111492921424,
-1.47868265808953));
#51404=CARTESIAN_POINT('Ctrl Pts',(-0.321771106026149,5.88663889491171E-5,
-1.47562265507269));
#51405=CARTESIAN_POINT('Origin',(0.,0.,-2.18777734492731));
#51406=CARTESIAN_POINT('',(-0.321771926585611,6.15374733540274E-5,-1.75027734492731));
#51407=CARTESIAN_POINT('',(-0.32235545627002,-0.000279252447957873,-1.72562265507269));
#51408=CARTESIAN_POINT('',(-0.322275,-3.08760083991297E-14,-2.18777734492731));
#51409=CARTESIAN_POINT('Ctrl Pts',(-0.32177192658561,6.15374733539953E-5,
-1.75027734492731));
#51410=CARTESIAN_POINT('Ctrl Pts',(-0.321673471884271,-0.0572510717560738,
-1.74675233217967));
#51411=CARTESIAN_POINT('Ctrl Pts',(-0.279817409473859,-0.221611271876293,
-1.7366516317558));
#51412=CARTESIAN_POINT('Ctrl Pts',(-0.0181057689026194,-0.379714901981348,
-1.7199752436557));
#51413=CARTESIAN_POINT('Ctrl Pts',(0.307872328352363,-0.22299372509844,
-1.70024818062701));
#51414=CARTESIAN_POINT('Ctrl Pts',(0.355139649765817,0.135600070284936,
-1.68052111759831));
#51415=CARTESIAN_POINT('Ctrl Pts',(0.0809057973768194,0.371437370479693,
-1.66079405456962));
#51416=CARTESIAN_POINT('Ctrl Pts',(-0.243452347477783,0.277700678203372,
-1.64237946367929));
#51417=CARTESIAN_POINT('Ctrl Pts',(-0.321612962348392,0.084888360938352,
-1.63054056046518));
#51418=CARTESIAN_POINT('Ctrl Pts',(-0.322380752027636,-0.000275883433438602,
-1.62527734492731));
#51419=CARTESIAN_POINT('Ctrl Pts',(-0.32235545627002,-0.000279252447957852,
-1.72562265507269));
#51420=CARTESIAN_POINT('Ctrl Pts',(-0.322555307131201,-0.0223720893850791,
-1.72425757687096));
#51421=CARTESIAN_POINT('Ctrl Pts',(-0.310454657452169,-0.150670362690872,
-1.716316810993));
#51422=CARTESIAN_POINT('Ctrl Pts',(-0.138655911363643,-0.353957599768978,
-1.70180035743881));
#51423=CARTESIAN_POINT('Ctrl Pts',(0.220331617412842,-0.309782948961838,
-1.68207329441012));
#51424=CARTESIAN_POINT('Ctrl Pts',(0.379857197625088,0.0148323499972791,
-1.66234623138143));
#51425=CARTESIAN_POINT('Ctrl Pts',(0.195505333378129,0.326020158763575,
-1.64261916835274));
#51426=CARTESIAN_POINT('Ctrl Pts',(-0.165833745799237,0.342068203520708,
-1.62289210532405));
#51427=CARTESIAN_POINT('Ctrl Pts',(-0.31571597672073,0.133707984795308,
-1.60889326756403));
#51428=CARTESIAN_POINT('Ctrl Pts',(-0.322696660269288,0.0139055160893734,
-1.60147011748025));
#51429=CARTESIAN_POINT('Ctrl Pts',(-0.322590734421357,0.000215874905906053,
-1.60062265507269));
#51430=CARTESIAN_POINT('Origin',(0.,0.,-2.18777734492731));
#51431=CARTESIAN_POINT('',(-0.322590464231506,0.000235348495535938,-1.87527734492731));
#51432=CARTESIAN_POINT('',(-0.321776643047528,7.65958109301412E-5,-1.85062265507269));
#51433=CARTESIAN_POINT('',(-0.322275,-3.08760083991297E-14,-2.18777734492731));
#51434=CARTESIAN_POINT('Ctrl Pts',(-0.322590464231506,0.000235348495535932,
-1.87527734492731));
#51435=CARTESIAN_POINT('Ctrl Pts',(-0.321876848463517,-0.092440732628234,
-1.86953979157039));
#51436=CARTESIAN_POINT('Ctrl Pts',(-0.231495856970855,-0.292611071270677,
-1.85722655053723));
#51437=CARTESIAN_POINT('Ctrl Pts',(0.107248148204929,-0.364687178636194,
-1.83833762182785));
#51438=CARTESIAN_POINT('Ctrl Pts',(0.363920662047043,-0.109881854276511,
-1.81861055879916));
#51439=CARTESIAN_POINT('Ctrl Pts',(0.291149288473172,0.244431170965113,
-1.79888349577046));
#51440=CARTESIAN_POINT('Ctrl Pts',(-0.0451973364463865,0.377447732614952,
-1.77915643274177));
#51441=CARTESIAN_POINT('Ctrl Pts',(-0.287836020952351,0.206064450530742,
-1.76295438246072));
#51442=CARTESIAN_POINT('Ctrl Pts',(-0.321857132884277,0.0496619652123383,
-1.7533280198559));
#51443=CARTESIAN_POINT('Ctrl Pts',(-0.32177192658561,6.15374733539953E-5,
-1.75027734492731));
#51444=CARTESIAN_POINT('Ctrl Pts',(-0.321776643047528,7.65958109301274E-5,
-1.85062265507269));
#51445=CARTESIAN_POINT('Ctrl Pts',(-0.321655231279037,-0.0580897489734325,
-1.84704503626168));
#51446=CARTESIAN_POINT('Ctrl Pts',(-0.27888134199293,-0.223334951199449,
-1.83689172977444));
#51447=CARTESIAN_POINT('Ctrl Pts',(-0.0150921858664401,-0.37984442379687,
-1.82016273561096));
#51448=CARTESIAN_POINT('Ctrl Pts',(0.309631125843552,-0.220545534491785,
-1.80043567258228));
#51449=CARTESIAN_POINT('Ctrl Pts',(0.354052996640771,0.138413596659764,
-1.78070860955358));
#51450=CARTESIAN_POINT('Ctrl Pts',(0.0779566158343278,0.372067153582978,
-1.76098154652489));
#51451=CARTESIAN_POINT('Ctrl Pts',(-0.244723080491218,0.276035928694378,
-1.74261956169792));
#51452=CARTESIAN_POINT('Ctrl Pts',(-0.321592610017374,0.084050821329131,
-1.73083326454719));
#51453=CARTESIAN_POINT('Ctrl Pts',(-0.32235545627002,-0.000279252447957852,
-1.72562265507269));
#51454=CARTESIAN_POINT('Origin',(5.160062080289E-17,2.1385152528819E-17,
-0.0249999999999999));
#51455=CARTESIAN_POINT('',(-0.268747084003623,-0.287158309717044,-0.0249999999999999));
#51456=CARTESIAN_POINT('Ctrl Pts',(-0.104132061245197,0.305520369126829,
-0.0249999999999997));
#51457=CARTESIAN_POINT('Ctrl Pts',(-0.112382861583866,0.303711558952992,
-0.0249999999999997));
#51458=CARTESIAN_POINT('Ctrl Pts',(-0.12054122005697,0.301562047182125,
-0.0249999999999994));
#51459=CARTESIAN_POINT('Ctrl Pts',(-0.128586133842392,0.299069778023146,
-0.0249999999999996));
#51460=CARTESIAN_POINT('Ctrl Pts',(-0.143668026017499,0.294397492436297,
-0.0249999999999999));
#51461=CARTESIAN_POINT('Ctrl Pts',(-0.158351562516306,0.28852241268013,
-0.0250000000000008));
#51462=CARTESIAN_POINT('Ctrl Pts',(-0.172564002552817,0.281564854373729,
-0.0250000000000009));
#51463=CARTESIAN_POINT('Ctrl Pts',(-0.17986959675151,0.277988473578474,
-0.025000000000001));
#51464=CARTESIAN_POINT('Ctrl Pts',(-0.187054604234899,0.274122843885494,
-0.0250000000000012));
#51465=CARTESIAN_POINT('Ctrl Pts',(-0.194083144462788,0.269997831741318,
-0.0250000000000011));
#51466=CARTESIAN_POINT('Ctrl Pts',(-0.207302501963761,0.262239462512193,
-0.025000000000001));
#51467=CARTESIAN_POINT('Ctrl Pts',(-0.219985327166613,0.253558036789537,
-0.0250000000000006));
#51468=CARTESIAN_POINT('Ctrl Pts',(-0.232067036805025,0.24405627624154,
-0.0250000000000008));
#51469=CARTESIAN_POINT('Ctrl Pts',(-0.239195615380843,0.238449946615834,
-0.0250000000000009));
#51470=CARTESIAN_POINT('Ctrl Pts',(-0.246114852768324,0.232557607409542,
-0.0250000000000013));
#51471=CARTESIAN_POINT('Ctrl Pts',(-0.252810300802026,0.226397178208491,
-0.0250000000000013));
#51472=CARTESIAN_POINT('Ctrl Pts',(-0.257040953740688,0.222504587634768,
-0.0250000000000012));
#51473=CARTESIAN_POINT('Ctrl Pts',(-0.261176314178513,0.218510243733399,
-0.0250000000000011));
#51474=CARTESIAN_POINT('Ctrl Pts',(-0.26520952408131,0.21442325237044,-0.025000000000001));
#51475=CARTESIAN_POINT('Ctrl Pts',(-0.279321174873982,0.200123427591488,
-0.025000000000001));
#51476=CARTESIAN_POINT('Ctrl Pts',(-0.292199058467302,0.184679362555137,
-0.0250000000000009));
#51477=CARTESIAN_POINT('Ctrl Pts',(-0.303703189948864,0.168295762170721,
-0.0250000000000008));
#51478=CARTESIAN_POINT('Ctrl Pts',(-0.311111775688651,0.15774483024084,
-0.0250000000000008));
#51479=CARTESIAN_POINT('Ctrl Pts',(-0.317950298791598,0.146803153286562,
-0.0250000000000007));
#51480=CARTESIAN_POINT('Ctrl Pts',(-0.324174543496671,0.135516327909584,
-0.0250000000000006));
#51481=CARTESIAN_POINT('Ctrl Pts',(-0.32697171144007,0.130444042415813,
-0.0250000000000005));
#51482=CARTESIAN_POINT('Ctrl Pts',(-0.329644730323056,0.125301970959981,
-0.0250000000000003));
#51483=CARTESIAN_POINT('Ctrl Pts',(-0.332189090490657,0.120093907801464,
-0.0250000000000003));
#51484=CARTESIAN_POINT('Ctrl Pts',(-0.33440192208225,0.115564452091959,
-0.0250000000000003));
#51485=CARTESIAN_POINT('Ctrl Pts',(-0.336515604770219,0.110988494106281,
-0.0250000000000002));
#51486=CARTESIAN_POINT('Ctrl Pts',(-0.338523889172115,0.10637780910622,
-0.0250000000000002));
#51487=CARTESIAN_POINT('Ctrl Pts',(-0.344841785747123,0.0918729755563301,
-0.0250000000000004));
#51488=CARTESIAN_POINT('Ctrl Pts',(-0.350129984567197,0.0770003032114229,
-0.0249999999999999));
#51489=CARTESIAN_POINT('Ctrl Pts',(-0.354318642179587,0.0618495857195709,
-0.0250000000000001));
#51490=CARTESIAN_POINT('Ctrl Pts',(-0.358443070227919,0.0469311918191192,
-0.0250000000000002));
#51491=CARTESIAN_POINT('Ctrl Pts',(-0.361501838911406,0.0317428915652387,
-0.0250000000000007));
#51492=CARTESIAN_POINT('Ctrl Pts',(-0.363538379759458,0.0163776637643565,
-0.025000000000001));
#51493=CARTESIAN_POINT('Ctrl Pts',(-0.364528551563602,0.00890704742624304,
-0.0250000000000011));
#51494=CARTESIAN_POINT('Ctrl Pts',(-0.365276802527859,0.00139448624501336,
-0.0250000000000007));
#51495=CARTESIAN_POINT('Ctrl Pts',(-0.365786589585033,-0.00614981576697971,
-0.0250000000000008));
#51496=CARTESIAN_POINT('Ctrl Pts',(-0.3662576514167,-0.0131210259505516,
-0.0250000000000008));
#51497=CARTESIAN_POINT('Ctrl Pts',(-0.366524835382005,-0.0201241583178749,
-0.0250000000000003));
#51498=CARTESIAN_POINT('Ctrl Pts',(-0.366590738824205,-0.0271210817527391,
-0.0250000000000003));
#51499=CARTESIAN_POINT('Ctrl Pts',(-0.366785036131083,-0.0477494940852813,
-0.0250000000000004));
#51500=CARTESIAN_POINT('Ctrl Pts',(-0.365238886576527,-0.0683667701686375,
-0.025000000000001));
#51501=CARTESIAN_POINT('Ctrl Pts',(-0.36205686275022,-0.0887617369955776,
-0.025000000000001));
#51502=CARTESIAN_POINT('Ctrl Pts',(-0.359210072782657,-0.107008045043846,
-0.0250000000000011));
#51503=CARTESIAN_POINT('Ctrl Pts',(-0.355053174048432,-0.125077451846666,
-0.0250000000000003));
#51504=CARTESIAN_POINT('Ctrl Pts',(-0.34962800436616,-0.142823830653435,
-0.0250000000000004));
#51505=CARTESIAN_POINT('Ctrl Pts',(-0.348118456848888,-0.147761741103659,
-0.0250000000000004));
#51506=CARTESIAN_POINT('Ctrl Pts',(-0.346510536019648,-0.152674628656446,
-0.0250000000000007));
#51507=CARTESIAN_POINT('Ctrl Pts',(-0.344804729560613,-0.157559276549724,
-0.0250000000000007));
#51508=CARTESIAN_POINT('Ctrl Pts',(-0.342956790976082,-0.162850925708409,
-0.0250000000000007));
#51509=CARTESIAN_POINT('Ctrl Pts',(-0.340996925380781,-0.168100787300376,
-0.0250000000000002));
#51510=CARTESIAN_POINT('Ctrl Pts',(-0.33892857690435,-0.173300715737075,
-0.0250000000000002));
#51511=CARTESIAN_POINT('Ctrl Pts',(-0.330624815413151,-0.194176775067354,
-0.0250000000000002));
#51512=CARTESIAN_POINT('Ctrl Pts',(-0.320569495551667,-0.214270328721061,
-0.0250000000000002));
#51513=CARTESIAN_POINT('Ctrl Pts',(-0.30885225511758,-0.233331936432522,
-0.0250000000000001));
#51514=CARTESIAN_POINT('Ctrl Pts',(-0.297135014683494,-0.252393544143984,
-0.025));
#51515=CARTESIAN_POINT('Ctrl Pts',(-0.283755567106122,-0.270425122759551,
-0.0249999999999999));
#51516=CARTESIAN_POINT('Ctrl Pts',(-0.268747084003623,-0.287158309717044,
-0.0249999999999999));
#51517=CARTESIAN_POINT('',(-0.3933,-4.81653586104654E-17,-0.025));
#51518=CARTESIAN_POINT('Origin',(0.,0.,-0.025));
#51519=CARTESIAN_POINT('',(0.0664872943522231,-0.388263316286114,-0.0249999999999998));
#51520=CARTESIAN_POINT('Origin',(0.,0.,-0.025));
#51521=CARTESIAN_POINT('Ctrl Pts',(0.0664872943522175,-0.388263316286115,
-0.0250000000000001));
#51522=CARTESIAN_POINT('Ctrl Pts',(0.0763674397481634,-0.385721382737377,
-0.0250000000000001));
#51523=CARTESIAN_POINT('Ctrl Pts',(0.0861252300852847,-0.382774239928317,
-0.0250000000000006));
#51524=CARTESIAN_POINT('Ctrl Pts',(0.0957372764438226,-0.379413846983949,
-0.0250000000000004));
#51525=CARTESIAN_POINT('Ctrl Pts',(0.110536106803841,-0.374240142730792,
-0.0250000000000001));
#51526=CARTESIAN_POINT('Ctrl Pts',(0.124989950584507,-0.368087330733362,
-0.025));
#51527=CARTESIAN_POINT('Ctrl Pts',(0.139034449099689,-0.361026667091296,
-0.0249999999999998));
#51528=CARTESIAN_POINT('Ctrl Pts',(0.145280104385201,-0.357886756389064,
-0.0249999999999998));
#51529=CARTESIAN_POINT('Ctrl Pts',(0.151444690667498,-0.35456715588149,
-0.0249999999999999));
#51530=CARTESIAN_POINT('Ctrl Pts',(0.157521916343542,-0.35107350179203,
-0.0249999999999999));
#51531=CARTESIAN_POINT('Ctrl Pts',(0.163617093981208,-0.347569527542108,
-0.0249999999999999));
#51532=CARTESIAN_POINT('Ctrl Pts',(0.169617845149672,-0.343894082667936,
-0.0249999999999997));
#51533=CARTESIAN_POINT('Ctrl Pts',(0.175512137101354,-0.340057896274778,
-0.0249999999999997));
#51534=CARTESIAN_POINT('Ctrl Pts',(0.193576222159083,-0.328301234427794,
-0.0249999999999996));
#51535=CARTESIAN_POINT('Ctrl Pts',(0.210662951284164,-0.315026093188845,
-0.0249999999999999));
#51536=CARTESIAN_POINT('Ctrl Pts',(0.226591694629148,-0.30040837774134,
-0.0249999999999998));
#51537=CARTESIAN_POINT('Ctrl Pts',(0.230914684688862,-0.296441194818828,
-0.0249999999999998));
#51538=CARTESIAN_POINT('Ctrl Pts',(0.235153530321517,-0.292373552875338,
-0.0249999999999999));
#51539=CARTESIAN_POINT('Ctrl Pts',(0.239299599657318,-0.288213122078874,
-0.0249999999999999));
#51540=CARTESIAN_POINT('Ctrl Pts',(0.254163153237533,-0.273298083025847,
-0.0249999999999999));
#51541=CARTESIAN_POINT('Ctrl Pts',(0.267772763215115,-0.257259583514981,
-0.025));
#51542=CARTESIAN_POINT('Ctrl Pts',(0.27996909329752,-0.240266943756375,
-0.0249999999999999));
#51543=CARTESIAN_POINT('Ctrl Pts',(0.291835834713897,-0.223733506186666,
-0.0249999999999999));
#51544=CARTESIAN_POINT('Ctrl Pts',(0.302365270717635,-0.206295554373272,
-0.0249999999999997));
#51545=CARTESIAN_POINT('Ctrl Pts',(0.311365267785366,-0.188092496425583,
-0.0249999999999994));
#51546=CARTESIAN_POINT('Ctrl Pts',(0.313924553682842,-0.182916180350604,
-0.0249999999999994));
#51547=CARTESIAN_POINT('Ctrl Pts',(0.316359844881218,-0.177677952152454,
-0.025));
#51548=CARTESIAN_POINT('Ctrl Pts',(0.318665922757951,-0.172380970932363,
-0.025));
#51549=CARTESIAN_POINT('Ctrl Pts',(0.320708024180543,-0.167690334508447,
-0.025));
#51550=CARTESIAN_POINT('Ctrl Pts',(0.322644714126049,-0.16296297370313,
-0.025));
#51551=CARTESIAN_POINT('Ctrl Pts',(0.324473225180541,-0.15820205171735,
-0.0249999999999999));
#51552=CARTESIAN_POINT('Ctrl Pts',(0.329742881883041,-0.144481366578025,
-0.0249999999999999));
#51553=CARTESIAN_POINT('Ctrl Pts',(0.334116071089045,-0.130480116961365,
-0.0249999999999995));
#51554=CARTESIAN_POINT('Ctrl Pts',(0.33752407445594,-0.116254171752792,
-0.0249999999999995));
#51555=CARTESIAN_POINT('Ctrl Pts',(0.341948241078035,-0.0977864810894237,
-0.0249999999999996));
#51556=CARTESIAN_POINT('Ctrl Pts',(0.344746961684114,-0.0789392408706085,
-0.025));
#51557=CARTESIAN_POINT('Ctrl Pts',(0.345959731177688,-0.0599047281750491,
-0.025));
#51558=CARTESIAN_POINT('Ctrl Pts',(0.346400164826157,-0.052992087382431,
-0.025));
#51559=CARTESIAN_POINT('Ctrl Pts',(0.346631052578019,-0.0460548358467735,
-0.0249999999999997));
#51560=CARTESIAN_POINT('Ctrl Pts',(0.34665305150596,-0.0391026545023186,
-0.0249999999999997));
#51561=CARTESIAN_POINT('Ctrl Pts',(0.346668273612427,-0.0342921089662239,
-0.0249999999999997));
#51562=CARTESIAN_POINT('Ctrl Pts',(0.346583436030999,-0.0294839208695866,
-0.0249999999999996));
#51563=CARTESIAN_POINT('Ctrl Pts',(0.346399784667637,-0.024681649273416,
-0.0249999999999996));
#51564=CARTESIAN_POINT('Ctrl Pts',(0.34561706202097,-0.00421435371424099,
-0.0249999999999996));
#51565=CARTESIAN_POINT('Ctrl Pts',(0.343043935277294,0.0161498773801879,
-0.0250000000000001));
#51566=CARTESIAN_POINT('Ctrl Pts',(0.338740270637847,0.0361681817656505,
-0.0250000000000001));
#51567=CARTESIAN_POINT('Ctrl Pts',(0.33524286737294,0.0524361972782629,
-0.0250000000000002));
#51568=CARTESIAN_POINT('Ctrl Pts',(0.330601279695819,0.0684760729038806,
-0.0249999999999997));
#51569=CARTESIAN_POINT('Ctrl Pts',(0.324822539663527,0.0841424234540789,
-0.0249999999999998));
#51570=CARTESIAN_POINT('Ctrl Pts',(0.322815809216327,0.0895827343990095,
-0.0249999999999998));
#51571=CARTESIAN_POINT('Ctrl Pts',(0.320670868222856,0.0949792610338929,
-0.0249999999999995));
#51572=CARTESIAN_POINT('Ctrl Pts',(0.318396443334708,0.100306333711764,
-0.0249999999999996));
#51573=CARTESIAN_POINT('Ctrl Pts',(0.310719203745818,0.118287676366146,
-0.0249999999999997));
#51574=CARTESIAN_POINT('Ctrl Pts',(0.301552401900112,0.135532171812037,
-0.0249999999999999));
#51575=CARTESIAN_POINT('Ctrl Pts',(0.290927725018398,0.151813099285338,
-0.025));
#51576=CARTESIAN_POINT('Ctrl Pts',(0.281011201280672,0.167008874701251,
-0.025));
#51577=CARTESIAN_POINT('Ctrl Pts',(0.269823771969094,0.181365979603481,
-0.0249999999999998));
#51578=CARTESIAN_POINT('Ctrl Pts',(0.257360178851843,0.194662425271939,
-0.0249999999999996));
#51579=CARTESIAN_POINT('Ctrl Pts',(0.256470135840318,0.195611943475398,
-0.0249999999999996));
#51580=CARTESIAN_POINT('Ctrl Pts',(0.255573574088629,0.196556033243165,
-0.0249999999999999));
#51581=CARTESIAN_POINT('Ctrl Pts',(0.254670486854674,0.19749460435719,-0.0249999999999999));
#51582=CARTESIAN_POINT('Ctrl Pts',(-0.143290239521314,0.288667772504872,
-1.99770630286919));
#51583=CARTESIAN_POINT('Ctrl Pts',(-0.238703631141289,0.241306033367412,
-1.99113061519296));
#51584=CARTESIAN_POINT('Ctrl Pts',(-0.377312127630152,0.0454238067759526,
-1.9779792398405));
#51585=CARTESIAN_POINT('Ctrl Pts',(-0.244303043357189,-0.291566061927666,
-1.95825217681181));
#51586=CARTESIAN_POINT('Ctrl Pts',(0.110179288406698,-0.36371910581051,
-1.93852511378312));
#51587=CARTESIAN_POINT('Ctrl Pts',(0.364759182106444,-0.107046497669421,
-1.91879805075442));
#51588=CARTESIAN_POINT('Ctrl Pts',(0.289212400745945,0.246761743044216,
-1.89907098772573));
#51589=CARTESIAN_POINT('Ctrl Pts',(-0.0481959974222359,0.377062323270783,
-1.87934392469704));
#51590=CARTESIAN_POINT('Ctrl Pts',(-0.341950950802492,0.166077696107313,
-1.85961686166835));
#51591=CARTESIAN_POINT('Ctrl Pts',(-0.326156034555877,-0.195286272819796,
-1.83988979863966));
#51592=CARTESIAN_POINT('Ctrl Pts',(-0.0150921858664401,-0.37984442379687,
-1.82016273561096));
#51593=CARTESIAN_POINT('Ctrl Pts',(0.309631125843552,-0.220545534491785,
-1.80043567258228));
#51594=CARTESIAN_POINT('Ctrl Pts',(0.354052996640771,0.138413596659764,
-1.78070860955358));
#51595=CARTESIAN_POINT('Ctrl Pts',(0.0779566158343278,0.372067153582978,
-1.76098154652489));
#51596=CARTESIAN_POINT('Ctrl Pts',(-0.268711937019807,0.268896715095413,
-1.7412544834962));
#51597=CARTESIAN_POINT('Ctrl Pts',(-0.372120970834768,-0.077701410624822,
-1.72152742046751));
#51598=CARTESIAN_POINT('Ctrl Pts',(-0.138655911363643,-0.353957599768978,
-1.70180035743881));
#51599=CARTESIAN_POINT('Ctrl Pts',(0.220331617412842,-0.309782948961838,
-1.68207329441012));
#51600=CARTESIAN_POINT('Ctrl Pts',(0.379857197625088,0.0148323499972791,
-1.66234623138143));
#51601=CARTESIAN_POINT('Ctrl Pts',(0.195505333378129,0.326020158763575,
-1.64261916835274));
#51602=CARTESIAN_POINT('Ctrl Pts',(-0.165833745799237,0.342068203520708,
-1.62289210532405));
#51603=CARTESIAN_POINT('Ctrl Pts',(-0.377046724116218,0.0484484589439102,
-1.60316504229535));
#51604=CARTESIAN_POINT('Ctrl Pts',(-0.246926540796393,-0.289030738284479,
-1.58343797926666));
#51605=CARTESIAN_POINT('Ctrl Pts',(0.106731497010161,-0.36485596183739,
-1.56371091623797));
#51606=CARTESIAN_POINT('Ctrl Pts',(0.363767560759545,-0.110384087378192,
-1.54398385320928));
#51607=CARTESIAN_POINT('Ctrl Pts',(0.291491836616472,0.244016380761125,
-1.52425679018059));
#51608=CARTESIAN_POINT('Ctrl Pts',(-0.0446658496794004,0.377513505615764,
-1.50452972715189));
#51609=CARTESIAN_POINT('Ctrl Pts',(-0.340388400050172,0.169254902744056,
-1.48480266412321));
#51610=CARTESIAN_POINT('Ctrl Pts',(-0.327963868087676,-0.192226913337763,
-1.46507560109451));
#51611=CARTESIAN_POINT('Ctrl Pts',(-0.0186399440734759,-0.37968939607062,
-1.44534853806582));
#51612=CARTESIAN_POINT('Ctrl Pts',(0.307558363392102,-0.223426359459979,
-1.42562147503713));
#51613=CARTESIAN_POINT('Ctrl Pts',(0.355329990338077,0.135100270022,-1.40589441200844));
#51614=CARTESIAN_POINT('Ctrl Pts',(0.0814282002323064,0.371323219316239,
-1.38616734897974));
#51615=CARTESIAN_POINT('Ctrl Pts',(-0.266188975926808,0.271394388464428,
-1.36644028595105));
#51616=CARTESIAN_POINT('Ctrl Pts',(-0.372830383652258,-0.0742225708309672,
-1.34671322292236));
#51617=CARTESIAN_POINT('Ctrl Pts',(-0.141955604305407,-0.352647262007924,
-1.32698615989367));
#51618=CARTESIAN_POINT('Ctrl Pts',(0.217428857727536,-0.311827158571008,
-1.30725909686498));
#51619=CARTESIAN_POINT('Ctrl Pts',(0.37997915002097,0.0112840836821547,
-1.28753203383628));
#51620=CARTESIAN_POINT('Ctrl Pts',(0.198541614321699,0.324180061659845,
-1.26780497080759));
#51621=CARTESIAN_POINT('Ctrl Pts',(-0.16263183234255,0.343602054860151,
-1.2480779077789));
#51622=CARTESIAN_POINT('Ctrl Pts',(-0.376577804112661,0.0519677057883744,
-1.22835084475021));
#51623=CARTESIAN_POINT('Ctrl Pts',(-0.249615121026705,-0.286712009427665,
-1.20862378172152));
#51624=CARTESIAN_POINT('Ctrl Pts',(0.103319337909045,-0.365836848074736,
-1.18889671869282));
#51625=CARTESIAN_POINT('Ctrl Pts',(0.362720784217591,-0.113776613114465,
-1.16916965566413));
#51626=CARTESIAN_POINT('Ctrl Pts',(0.293758069692678,0.241283404911434,
-1.14944259263544));
#51627=CARTESIAN_POINT('Ctrl Pts',(-0.0411381844576584,0.377914189697542,
-1.12971552960675));
#51628=CARTESIAN_POINT('Ctrl Pts',(-0.338792830171386,0.172426515419424,
-1.10998846657806));
#51629=CARTESIAN_POINT('Ctrl Pts',(-0.329744832374935,-0.189155572260636,
-1.09026140354936));
#51630=CARTESIAN_POINT('Ctrl Pts',(-0.022185169729932,-0.379498752618868,
-1.07053434052067));
#51631=CARTESIAN_POINT('Ctrl Pts',(0.305458301062517,-0.226288999527647,
-1.05080727749198));
#51632=CARTESIAN_POINT('Ctrl Pts',(0.356576237443244,0.131775839538367,
-1.03108021446329));
#51633=CARTESIAN_POINT('Ctrl Pts',(0.0848925531951284,0.370546541485998,
-1.0113531514346));
#51634=CARTESIAN_POINT('Ctrl Pts',(-0.263642729317636,0.273868574818599,
-0.991626088405904));
#51635=CARTESIAN_POINT('Ctrl Pts',(-0.373507311558931,-0.0707373536912577,
-0.971899025377214));
#51636=CARTESIAN_POINT('Ctrl Pts',(-0.145242896892136,-0.351306114233161,
-0.952171962348521));
#51637=CARTESIAN_POINT('Ctrl Pts',(0.214507123315248,-0.313844195489162,
-0.932444899319828));
#51638=CARTESIAN_POINT('Ctrl Pts',(0.380067963842326,0.00773484686148907,
-0.912717836291137));
#51639=CARTESIAN_POINT('Ctrl Pts',(0.20156057492959,0.322311680876253,-0.892990773262445));
#51640=CARTESIAN_POINT('Ctrl Pts',(-0.159415732015043,0.345105939359686,
-0.873263710233753));
#51641=CARTESIAN_POINT('Ctrl Pts',(-0.376076037935125,0.0554824178117764,
-0.853536647205062));
#51642=CARTESIAN_POINT('Ctrl Pts',(-0.252281928284525,-0.284368271184151,
-0.833809584176369));
#51643=CARTESIAN_POINT('Ctrl Pts',(0.0998981666172007,-0.366785824837531,
-0.814082521147678));
#51644=CARTESIAN_POINT('Ctrl Pts',(0.361642369567447,-0.117159214442841,
-0.794355458118984));
#51645=CARTESIAN_POINT('Ctrl Pts',(0.295998679758828,0.238529383045872,
-0.774628395090294));
#51646=CARTESIAN_POINT('Ctrl Pts',(-0.0376069309429452,0.37828191040585,
-0.754901332061601));
#51647=CARTESIAN_POINT('Ctrl Pts',(-0.337167709206362,0.175583088205384,
-0.73517426903291));
#51648=CARTESIAN_POINT('Ctrl Pts',(-0.331497034762949,-0.186067732126079,
-0.715447206004218));
#51649=CARTESIAN_POINT('Ctrl Pts',(-0.0257284602956936,-0.379275007515933,
-0.695720142975526));
#51650=CARTESIAN_POINT('Ctrl Pts',(0.303331595228502,-0.22913190160076,
-0.675993079946833));
#51651=CARTESIAN_POINT('Ctrl Pts',(0.357791382294441,0.128439914943824,
-0.656266016918142));
#51652=CARTESIAN_POINT('Ctrl Pts',(0.0883495014317826,0.369737542850607,
-0.63653895388945));
#51653=CARTESIAN_POINT('Ctrl Pts',(-0.261073486552964,0.276318873066526,
-0.616811890860758));
#51654=CARTESIAN_POINT('Ctrl Pts',(-0.374151660404283,-0.0672459665012387,
-0.597084827832066));
#51655=CARTESIAN_POINT('Ctrl Pts',(-0.148517520713027,-0.349934323902057,
-0.577357764803375));
#51656=CARTESIAN_POINT('Ctrl Pts',(0.211566678587274,-0.315833857421815,
-0.557630701774681));
#51657=CARTESIAN_POINT('Ctrl Pts',(0.380123626347935,0.00418493532934027,
-0.537903638745991));
#51658=CARTESIAN_POINT('Ctrl Pts',(0.204561954486446,0.320415186635358,
-0.518176575717298));
#51659=CARTESIAN_POINT('Ctrl Pts',(-0.156185726714996,0.346579721946209,
-0.498449512688607));
#51660=CARTESIAN_POINT('Ctrl Pts',(-0.375541468610517,0.0589922906922721,
-0.478722449659914));
#51661=CARTESIAN_POINT('Ctrl Pts',(-0.254926730386367,-0.281999729568725,
-0.458995386631223));
#51662=CARTESIAN_POINT('Ctrl Pts',(0.096468281849101,-0.367702807740199,
-0.43926832360253));
#51663=CARTESIAN_POINT('Ctrl Pts',(0.360532410560641,-0.120531598662528,
-0.419541260573839));
#51664=CARTESIAN_POINT('Ctrl Pts',(0.298213471837286,0.235754559490252,
-0.399814197545147));
#51665=CARTESIAN_POINT('Ctrl Pts',(-0.0340723979536573,0.378616627998834,
-0.380087134516455));
#51666=CARTESIAN_POINT('Ctrl Pts',(-0.335513177399885,0.178724360357116,
-0.360360071487763));
#51667=CARTESIAN_POINT('Ctrl Pts',(-0.333220325281847,-0.182963690163682,
-0.340633008459071));
#51668=CARTESIAN_POINT('Ctrl Pts',(-0.029269501228293,-0.379018126859581,
-0.320905945430379));
#51669=CARTESIAN_POINT('Ctrl Pts',(0.301178420896456,-0.231954920047871,
-0.301178882401687));
#51670=CARTESIAN_POINT('Ctrl Pts',(0.358975339007382,0.125092983298727,
-0.281451819372995));
#51671=CARTESIAN_POINT('Ctrl Pts',(0.0917987048867537,0.368895918259873,
-0.261724756344303));
#51672=CARTESIAN_POINT('Ctrl Pts',(-0.258481397918661,0.278745789386344,
-0.241997693315611));
#51673=CARTESIAN_POINT('Ctrl Pts',(-0.374763515422673,-0.0637500932034806,
-0.222270630286919));
#51674=CARTESIAN_POINT('Ctrl Pts',(-0.151778919131785,-0.348529367587568,
-0.202543567258227));
#51675=CARTESIAN_POINT('Ctrl Pts',(0.208607260742278,-0.317801035232212,
-0.182816504229535));
#51676=CARTESIAN_POINT('Ctrl Pts',(0.380147127696309,0.000644362698709406,
-0.163089441200843));
#51677=CARTESIAN_POINT('Ctrl Pts',(0.207543584467282,0.318472150029413,
-0.143362378172152));
#51678=CARTESIAN_POINT('Ctrl Pts',(-0.152938443007933,0.348058907694893,
-0.12363531514346));
#51679=CARTESIAN_POINT('Ctrl Pts',(-0.374981161716835,0.0624286949386616,
-0.103908252114768));
#51680=CARTESIAN_POINT('Ctrl Pts',(-0.257535709165863,-0.279475261928206,
-0.084181189086076));
#51681=CARTESIAN_POINT('Ctrl Pts',(0.0930026936990432,-0.368843116278878,
-0.0644541260573834));
#51682=CARTESIAN_POINT('Ctrl Pts',(0.359454556187757,-0.123370117592038,
-0.0447270630286919));
#51683=CARTESIAN_POINT('Ctrl Pts',(0.319948400855436,0.113318339423062,
-0.0315756876762305));
#51684=CARTESIAN_POINT('Ctrl Pts',(0.254670486854674,0.19749460435719,-0.0249999999999999));
#51685=CARTESIAN_POINT('Ctrl Pts',(-0.15381664219191,0.309873914818279,
-1.98403753524613));
#51686=CARTESIAN_POINT('Ctrl Pts',(-0.256239302438379,0.25903288261099,
-1.9774618475699));
#51687=CARTESIAN_POINT('Ctrl Pts',(-0.405030270897994,0.0487607352544926,
-1.96431047221744));
#51688=CARTESIAN_POINT('Ctrl Pts',(-0.262250059264355,-0.312985118683967,
-1.94458340918874));
#51689=CARTESIAN_POINT('Ctrl Pts',(0.118273290898445,-0.390438677077484,
-1.92485634616005));
#51690=CARTESIAN_POINT('Ctrl Pts',(0.391555159567835,-0.114910358758007,
-1.90512928313136));
#51691=CARTESIAN_POINT('Ctrl Pts',(0.310458552596572,0.264889380206798,
-1.88540222010267));
#51692=CARTESIAN_POINT('Ctrl Pts',(-0.0517365768620641,0.404762115384463,
-1.86567515707398));
#51693=CARTESIAN_POINT('Ctrl Pts',(-0.367071387573103,0.178278113314174,
-1.84594809404529));
#51694=CARTESIAN_POINT('Ctrl Pts',(-0.35011614352527,-0.209632413566078,
-1.82622103101659));
#51695=CARTESIAN_POINT('Ctrl Pts',(-0.0162008896144463,-0.407748594872476,
-1.8064939679879));
#51696=CARTESIAN_POINT('Ctrl Pts',(0.332377280228303,-0.236747273779951,
-1.78676690495921));
#51697=CARTESIAN_POINT('Ctrl Pts',(0.380062475177643,0.148581750878735,
-1.76703984193052));
#51698=CARTESIAN_POINT('Ctrl Pts',(0.0836834729590768,0.399399990014835,
-1.74731277890183));
#51699=CARTESIAN_POINT('Ctrl Pts',(-0.288452081644563,0.288650433906628,
-1.72758571587313));
#51700=CARTESIAN_POINT('Ctrl Pts',(-0.399457760795247,-0.0834095198375802,
-1.70785865284444));
#51701=CARTESIAN_POINT('Ctrl Pts',(-0.148841866530923,-0.379960070250804,
-1.68813158981575));
#51702=CARTESIAN_POINT('Ctrl Pts',(0.236517641902015,-0.332540256592501,
-1.66840452678706));
#51703=CARTESIAN_POINT('Ctrl Pts',(0.407762307093009,0.0159219656552873,
-1.64867746375837));
#51704=CARTESIAN_POINT('Ctrl Pts',(0.209867566774228,0.349970286011197,
-1.62895040072967));
#51705=CARTESIAN_POINT('Ctrl Pts',(-0.178016241902864,0.367197253922858,
-1.60922333770098));
#51706=CARTESIAN_POINT('Ctrl Pts',(-0.40474537028316,0.0520075847386445,
-1.58949627467229));
#51707=CARTESIAN_POINT('Ctrl Pts',(-0.265066284348811,-0.310263544828221,
-1.5697692116436));
#51708=CARTESIAN_POINT('Ctrl Pts',(0.114572217487129,-0.391659048941573,
-1.5500421486149));
#51709=CARTESIAN_POINT('Ctrl Pts',(0.390490691629088,-0.118493134833562,
-1.53031508558622));
#51710=CARTESIAN_POINT('Ctrl Pts',(0.312905440625146,0.261942337830458,
-1.51058802255752));
#51711=CARTESIAN_POINT('Ctrl Pts',(-0.0479470970338614,0.4052464425344,
-1.49086095952883));
#51712=CARTESIAN_POINT('Ctrl Pts',(-0.365394048552809,0.181688724239568,
-1.47113389650014));
#51713=CARTESIAN_POINT('Ctrl Pts',(-0.352056784314427,-0.206348307095488,
-1.45140683347145));
#51714=CARTESIAN_POINT('Ctrl Pts',(-0.0200092736086255,-0.407582178483068,
-1.43167977044275));
#51715=CARTESIAN_POINT('Ctrl Pts',(0.330152248283289,-0.239839730215439,
-1.41195270741406));
#51716=CARTESIAN_POINT('Ctrl Pts',(0.381433279520466,0.145025020290467,
-1.39222564438537));
#51717=CARTESIAN_POINT('Ctrl Pts',(0.087410087255813,0.398601404770623,
-1.37249858135668));
#51718=CARTESIAN_POINT('Ctrl Pts',(-0.285743778517969,0.291331591619795,
-1.35277151832799));
#51719=CARTESIAN_POINT('Ctrl Pts',(-0.400219288571868,-0.0796751171483121,
-1.3330444552993));
#51720=CARTESIAN_POINT('Ctrl Pts',(-0.152383961863179,-0.378553472319109,
-1.3133173922706));
#51721=CARTESIAN_POINT('Ctrl Pts',(0.233401639378917,-0.334734638143327,
-1.29359032924191));
#51722=CARTESIAN_POINT('Ctrl Pts',(0.407893218368644,0.0121130362263305,
-1.27386326621322));
#51723=CARTESIAN_POINT('Ctrl Pts',(0.213126899308332,0.347995011500187,
-1.25413620318453));
#51724=CARTESIAN_POINT('Ctrl Pts',(-0.174579109142516,0.368843785210984,
-1.23440914015583));
#51725=CARTESIAN_POINT('Ctrl Pts',(-0.404242002428904,0.0557853628655306,
-1.21468207712715));
#51726=CARTESIAN_POINT('Ctrl Pts',(-0.267952373343229,-0.307774477267861,
-1.19495501409845));
#51727=CARTESIAN_POINT('Ctrl Pts',(0.110909393994673,-0.392711993147018,
-1.17522795106976));
#51728=CARTESIAN_POINT('Ctrl Pts',(0.389367016678535,-0.122134882652859,
-1.15550088804106));
#51729=CARTESIAN_POINT('Ctrl Pts',(0.315338155954333,0.259008591820991,
-1.13577382501238));
#51730=CARTESIAN_POINT('Ctrl Pts',(-0.0441602820979793,0.405676561712403,
-1.11604676198368));
#51731=CARTESIAN_POINT('Ctrl Pts',(-0.363681264751502,0.185093330259408,
-1.09631969895499));
#51732=CARTESIAN_POINT('Ctrl Pts',(-0.353968581987773,-0.203051338836603,
-1.0765926359263));
#51733=CARTESIAN_POINT('Ctrl Pts',(-0.023814939005727,-0.40737752996198,
-1.05686557289761));
#51734=CARTESIAN_POINT('Ctrl Pts',(0.327897910953617,-0.242912665849322,
-1.03713850986892));
#51735=CARTESIAN_POINT('Ctrl Pts',(0.382771078561759,0.141456370144433,
-1.01741144684022));
#51736=CARTESIAN_POINT('Ctrl Pts',(0.0911289388809415,0.397767670551799,
-0.997684383811531));
#51737=CARTESIAN_POINT('Ctrl Pts',(-0.28301047927216,0.293987536912559,
-0.977957320782842));
#51738=CARTESIAN_POINT('Ctrl Pts',(-0.400945945027732,-0.0759338686199355,
-0.958230257754147));
#51739=CARTESIAN_POINT('Ctrl Pts',(-0.155912745884214,-0.377113801005234,
-0.938503194725458));
#51740=CARTESIAN_POINT('Ctrl Pts',(0.230265268205443,-0.336899850840047,
-0.918776131696764));
#51741=CARTESIAN_POINT('Ctrl Pts',(0.4079885566403,0.00830306499645114,
-0.899049068668072));
#51742=CARTESIAN_POINT('Ctrl Pts',(0.216367639118431,0.345989375530647,
-0.879322005639381));
#51743=CARTESIAN_POINT('Ctrl Pts',(-0.171126747313949,0.370458148232049,
-0.859594942610688));
#51744=CARTESIAN_POINT('Ctrl Pts',(-0.403703375451576,0.0595582730338527,
-0.839867879581998));
#51745=CARTESIAN_POINT('Ctrl Pts',(-0.270815089876757,-0.305258563078602,
-0.820140816553304));
#51746=CARTESIAN_POINT('Ctrl Pts',(0.107236896256985,-0.393730683740731,
-0.800413753524614));
#51747=CARTESIAN_POINT('Ctrl Pts',(0.388209379417758,-0.125765976996359,
-0.780686690495921));
#51748=CARTESIAN_POINT('Ctrl Pts',(0.317743365953199,0.256052253711019,
-0.76095962746723));
#51749=CARTESIAN_POINT('Ctrl Pts',(-0.0403696152655688,0.406071295958122,
-0.741232564438537));
#51750=CARTESIAN_POINT('Ctrl Pts',(-0.361936758978947,0.188481791527898,
-0.721505501409845));
#51751=CARTESIAN_POINT('Ctrl Pts',(-0.3558495048522,-0.199736659464793,
-0.701778438381154));
#51752=CARTESIAN_POINT('Ctrl Pts',(-0.0276185271562979,-0.407137348072724,
-0.68205137535246));
#51753=CARTESIAN_POINT('Ctrl Pts',(0.325614972831586,-0.245964413494015,
-0.662324312323771));
#51754=CARTESIAN_POINT('Ctrl Pts',(0.384075490512023,0.137875381505904,
-0.642597249295077));
#51755=CARTESIAN_POINT('Ctrl Pts',(0.0948398418131284,0.39689924117343,
-0.622870186266386));
#51756=CARTESIAN_POINT('Ctrl Pts',(-0.280252494524853,0.296617839228501,
-0.603143123237693));
#51757=CARTESIAN_POINT('Ctrl Pts',(-0.40163762909584,-0.0721859967763643,
-0.583416060209001));
#51758=CARTESIAN_POINT('Ctrl Pts',(-0.1594279304652,-0.375641236068315,
-0.563688997180311));
#51759=CARTESIAN_POINT('Ctrl Pts',(0.227108812217102,-0.339035677527198,
-0.543961934151617));
#51760=CARTESIAN_POINT('Ctrl Pts',(0.408048308230761,0.00449236948936304,
-0.524234871122926));
#51761=CARTESIAN_POINT('Ctrl Pts',(0.219589506336472,0.343953560830042,
-0.504507808094233));
#51762=CARTESIAN_POINT('Ctrl Pts',(-0.167659459024287,0.372040197990199,
-0.484780745065542));
#51763=CARTESIAN_POINT('Ctrl Pts',(-0.403129535538929,0.0633259885656422,
-0.46505368203685));
#51764=CARTESIAN_POINT('Ctrl Pts',(-0.273654184709222,-0.30271602340951,
-0.445326619008158));
#51765=CARTESIAN_POINT('Ctrl Pts',(0.10355504493273,-0.394715030137994,
-0.425599555979466));
#51766=CARTESIAN_POINT('Ctrl Pts',(0.387017880485466,-0.129386103660856,
-0.405872492950774));
#51767=CARTESIAN_POINT('Ctrl Pts',(0.320120861320641,0.253073585775043,
-0.386145429922083));
#51768=CARTESIAN_POINT('Ctrl Pts',(-0.0365754280414766,0.406430602610184,
-0.36641836689339));
#51769=CARTESIAN_POINT('Ctrl Pts',(-0.360160681782608,0.191853828145357,
-0.346691303864698));
#51770=CARTESIAN_POINT('Ctrl Pts',(-0.357699391920736,-0.19640458804476,
-0.326964240836007));
#51771=CARTESIAN_POINT('Ctrl Pts',(-0.0314197004109189,-0.406861596422534,
-0.307237177807315));
#51772=CARTESIAN_POINT('Ctrl Pts',(0.323303621779935,-0.248994816819678,
-0.287510114778622));
#51773=CARTESIAN_POINT('Ctrl Pts',(0.385346423177733,0.134282577215712,
-0.267783051749931));
#51774=CARTESIAN_POINT('Ctrl Pts',(0.0985424310156646,0.395995789068351,
-0.248055988721239));
#51775=CARTESIAN_POINT('Ctrl Pts',(-0.277469985602234,0.29922304193067,
-0.228328925692547));
#51776=CARTESIAN_POINT('Ctrl Pts',(-0.402294432272047,-0.0684333092661341,
-0.208601862663855));
#51777=CARTESIAN_POINT('Ctrl Pts',(-0.162928918078169,-0.374133068705046,
-0.188874799635163));
#51778=CARTESIAN_POINT('Ctrl Pts',(0.223931989306618,-0.341147368361133,
-0.169147736606471));
#51779=CARTESIAN_POINT('Ctrl Pts',(0.408073536037664,0.000691698939159734,
-0.149420673577779));
#51780=CARTESIAN_POINT('Ctrl Pts',(0.22279017313306,0.341867784664262,-0.129693610549087));
#51781=CARTESIAN_POINT('Ctrl Pts',(-0.164173623019451,0.373628047838177,
-0.109966547520395));
#51782=CARTESIAN_POINT('Ctrl Pts',(-0.402528067321197,0.0670148383027876,
-0.0902394844917032));
#51783=CARTESIAN_POINT('Ctrl Pts',(-0.276454824562659,-0.300006103061243,
-0.0705124214630116));
#51784=CARTESIAN_POINT('Ctrl Pts',(0.0998348673809113,-0.395939108142667,
-0.050785358434319));
#51785=CARTESIAN_POINT('Ctrl Pts',(0.385860844661094,-0.132433146166989,
-0.0310582954056275));
#51786=CARTESIAN_POINT('Ctrl Pts',(0.343452483983984,0.121642943211257,
-0.0179069200531661));
#51787=CARTESIAN_POINT('Ctrl Pts',(0.273379116988209,0.212002973787509,
-0.0113312323769355));
#51788=CARTESIAN_POINT('Ctrl Pts',(-0.164343044862507,0.331080057131685,
-1.97036876762306));
#51789=CARTESIAN_POINT('Ctrl Pts',(-0.273774973735468,0.276759731854568,
-1.96379307994683));
#51790=CARTESIAN_POINT('Ctrl Pts',(-0.432748414165835,0.0520976637330328,
-1.95064170459437));
#51791=CARTESIAN_POINT('Ctrl Pts',(-0.280197075171522,-0.334404175440268,
-1.93091464156568));
#51792=CARTESIAN_POINT('Ctrl Pts',(0.126367293390191,-0.417158248344458,
-1.91118757853699));
#51793=CARTESIAN_POINT('Ctrl Pts',(0.418351137029226,-0.122774219846594,
-1.8914605155083));
#51794=CARTESIAN_POINT('Ctrl Pts',(0.331704704447198,0.28301701736938,-1.8717334524796));
#51795=CARTESIAN_POINT('Ctrl Pts',(-0.055277156301892,0.432461907498141,
-1.85200638945091));
#51796=CARTESIAN_POINT('Ctrl Pts',(-0.392191824343714,0.190478530521036,
-1.83227932642222));
#51797=CARTESIAN_POINT('Ctrl Pts',(-0.374076252494662,-0.22397855431236,
-1.81255226339353));
#51798=CARTESIAN_POINT('Ctrl Pts',(-0.0173095933624528,-0.435652765948081,
-1.79282520036484));
#51799=CARTESIAN_POINT('Ctrl Pts',(0.355123434613053,-0.252949013068117,
-1.77309813733615));
#51800=CARTESIAN_POINT('Ctrl Pts',(0.406071953714516,0.158749905097707,
-1.75337107430745));
#51801=CARTESIAN_POINT('Ctrl Pts',(0.0894103300838258,0.426732826446693,
-1.73364401127876));
#51802=CARTESIAN_POINT('Ctrl Pts',(-0.30819222626932,0.308404152717844,
-1.71391694825007));
#51803=CARTESIAN_POINT('Ctrl Pts',(-0.426794550755725,-0.0891176290503394,
-1.69418988522138));
#51804=CARTESIAN_POINT('Ctrl Pts',(-0.159027821698202,-0.405962540732628,
-1.67446282219268));
#51805=CARTESIAN_POINT('Ctrl Pts',(0.252703666391189,-0.355297564223164,
-1.65473575916399));
#51806=CARTESIAN_POINT('Ctrl Pts',(0.435667416560929,0.0170115813132962,
-1.6350086961353));
#51807=CARTESIAN_POINT('Ctrl Pts',(0.224229800170327,0.373920413258818,
-1.61528163310661));
#51808=CARTESIAN_POINT('Ctrl Pts',(-0.19019873800649,0.392326304325009,
-1.59555457007792));
#51809=CARTESIAN_POINT('Ctrl Pts',(-0.432444016450103,0.0555667105333784,
-1.57582750704923));
#51810=CARTESIAN_POINT('Ctrl Pts',(-0.283206027901227,-0.331496351371963,
-1.55610044402053));
#51811=CARTESIAN_POINT('Ctrl Pts',(0.122412937964096,-0.418462136045755,
-1.53637338099184));
#51812=CARTESIAN_POINT('Ctrl Pts',(0.417213822498632,-0.126602182288933,
-1.51664631796315));
#51813=CARTESIAN_POINT('Ctrl Pts',(0.33431904463382,0.27986829489979,-1.49691925493446));
#51814=CARTESIAN_POINT('Ctrl Pts',(-0.0512283443883222,0.432979379453035,
-1.47719219190577));
#51815=CARTESIAN_POINT('Ctrl Pts',(-0.390399697055447,0.194122545735081,
-1.45746512887707));
#51816=CARTESIAN_POINT('Ctrl Pts',(-0.376149700541177,-0.220469700853213,
-1.43773806584838));
#51817=CARTESIAN_POINT('Ctrl Pts',(-0.0213786031437756,-0.435474960895517,
-1.41801100281969));
#51818=CARTESIAN_POINT('Ctrl Pts',(0.352746133174477,-0.256253100970898,
-1.398283939791));
#51819=CARTESIAN_POINT('Ctrl Pts',(0.407536568702855,0.154949770558933,
-1.37855687676231));
#51820=CARTESIAN_POINT('Ctrl Pts',(0.0933919742793201,0.425879590225008,
-1.35882981373362));
#51821=CARTESIAN_POINT('Ctrl Pts',(-0.30529858110913,0.311268794775162,
-1.33910275070492));
#51822=CARTESIAN_POINT('Ctrl Pts',(-0.427608193491478,-0.085127663465657,
-1.31937568767623));
#51823=CARTESIAN_POINT('Ctrl Pts',(-0.162812319420953,-0.404459682630294,
-1.29964862464754));
#51824=CARTESIAN_POINT('Ctrl Pts',(0.249374421030298,-0.357642117715646,
-1.27992156161885));
#51825=CARTESIAN_POINT('Ctrl Pts',(0.435807286716317,0.0129419887705061,
-1.26019449859016));
#51826=CARTESIAN_POINT('Ctrl Pts',(0.227712184294964,0.371809961340529,
-1.24046743556146));
#51827=CARTESIAN_POINT('Ctrl Pts',(-0.186526385942482,0.394085515561816,
-1.22074037253277));
#51828=CARTESIAN_POINT('Ctrl Pts',(-0.431906200745147,0.0596030199426871,
-1.20101330950408));
#51829=CARTESIAN_POINT('Ctrl Pts',(-0.286289625659754,-0.328836945108058,
-1.18128624647539));
#51830=CARTESIAN_POINT('Ctrl Pts',(0.118499450080301,-0.4195871382193,-1.16155918344669));
#51831=CARTESIAN_POINT('Ctrl Pts',(0.416013249139481,-0.130493152191252,
-1.141832120418));
#51832=CARTESIAN_POINT('Ctrl Pts',(0.336918242215987,0.276733778730547,
-1.12210505738931));
#51833=CARTESIAN_POINT('Ctrl Pts',(-0.047182379738299,0.433438933727265,
-1.10237799436062));
#51834=CARTESIAN_POINT('Ctrl Pts',(-0.38856969933162,0.197760145099391,
-1.08265093133193));
#51835=CARTESIAN_POINT('Ctrl Pts',(-0.378192331600609,-0.21694710541257,
-1.06292386830324));
#51836=CARTESIAN_POINT('Ctrl Pts',(-0.0254447082815231,-0.435256307305093,
-1.04319680527454));
#51837=CARTESIAN_POINT('Ctrl Pts',(0.350337520844719,-0.259536332170997,
-1.02346974224585));
#51838=CARTESIAN_POINT('Ctrl Pts',(0.408965919680273,0.1511369007505,-1.00374267921716));
#51839=CARTESIAN_POINT('Ctrl Pts',(0.0973653245667549,0.424988799617599,
-0.984015616188466));
#51840=CARTESIAN_POINT('Ctrl Pts',(-0.302378229226684,0.314106499006519,
-0.964288553159777));
#51841=CARTESIAN_POINT('Ctrl Pts',(-0.428384578496533,-0.0811303835486135,
-0.944561490131084));
#51842=CARTESIAN_POINT('Ctrl Pts',(-0.166582594876293,-0.402921487777307,
-0.924834427102392));
#51843=CARTESIAN_POINT('Ctrl Pts',(0.246023413095639,-0.359955506190932,
-0.905107364073701));
#51844=CARTESIAN_POINT('Ctrl Pts',(0.435909149438275,0.00887128313141311,
-0.885380301045008));
#51845=CARTESIAN_POINT('Ctrl Pts',(0.231174703307272,0.369667070185041,
-0.865653238016316));
#51846=CARTESIAN_POINT('Ctrl Pts',(-0.182837762612857,0.395810357104412,
-0.845926174987624));
#51847=CARTESIAN_POINT('Ctrl Pts',(-0.431330712968026,0.0636341282559295,
-0.826199111958933));
#51848=CARTESIAN_POINT('Ctrl Pts',(-0.289348251468989,-0.326148854973054,
-0.80647204893024));
#51849=CARTESIAN_POINT('Ctrl Pts',(0.114575625896769,-0.420675542643931,
-0.786744985901549));
#51850=CARTESIAN_POINT('Ctrl Pts',(0.414776389268069,-0.134372739549877,
-0.767017922872856));
#51851=CARTESIAN_POINT('Ctrl Pts',(0.339488052147569,0.273575124376166,
-0.747290859844165));
#51852=CARTESIAN_POINT('Ctrl Pts',(-0.0431322995881918,0.433860681510395,
-0.727563796815472));
#51853=CARTESIAN_POINT('Ctrl Pts',(-0.386705808751533,0.201380494850412,
-0.707836733786781));
#51854=CARTESIAN_POINT('Ctrl Pts',(-0.38020197494145,-0.213405586803507,
-0.688109670758089));
#51855=CARTESIAN_POINT('Ctrl Pts',(-0.0295085940169031,-0.434999688629514,
-0.668382607729396));
#51856=CARTESIAN_POINT('Ctrl Pts',(0.347898350434672,-0.26279692538727,
-0.648655544700706));
#51857=CARTESIAN_POINT('Ctrl Pts',(0.410359598729604,0.147310848067984,
-0.628928481672012));
#51858=CARTESIAN_POINT('Ctrl Pts',(0.101330182194475,0.424060939496253,
-0.609201418643322));
#51859=CARTESIAN_POINT('Ctrl Pts',(-0.299431502496743,0.316916805390477,
-0.589474355614628));
#51860=CARTESIAN_POINT('Ctrl Pts',(-0.429123597787398,-0.0771260270514894,
-0.569747292585937));
#51861=CARTESIAN_POINT('Ctrl Pts',(-0.170338340217374,-0.401348148234573,
-0.550020229557245));
#51862=CARTESIAN_POINT('Ctrl Pts',(0.242650945846931,-0.36223749763258,
-0.530293166528553));
#51863=CARTESIAN_POINT('Ctrl Pts',(0.435972990113586,0.00479980364938559,
-0.510566103499861));
#51864=CARTESIAN_POINT('Ctrl Pts',(0.234617058186499,0.367491935024725,
-0.490839040471169));
#51865=CARTESIAN_POINT('Ctrl Pts',(-0.179133191333578,0.397500674034188,
-0.471111977442477));
#51866=CARTESIAN_POINT('Ctrl Pts',(-0.430717602467341,0.0676596864390125,
-0.451384914413786));
#51867=CARTESIAN_POINT('Ctrl Pts',(-0.292381639032076,-0.323432317250295,
-0.431657851385093));
#51868=CARTESIAN_POINT('Ctrl Pts',(0.11064180801636,-0.42172725253579,-0.411930788356402));
#51869=CARTESIAN_POINT('Ctrl Pts',(0.41350335041029,-0.138240608659184,
-0.39220372532771));
#51870=CARTESIAN_POINT('Ctrl Pts',(0.342028250803996,0.270392612059835,
-0.372476662299018));
#51871=CARTESIAN_POINT('Ctrl Pts',(-0.0390784581292962,0.434244577221532,
-0.352749599270326));
#51872=CARTESIAN_POINT('Ctrl Pts',(-0.38480818616533,0.204983295933599,
-0.333022536241634));
#51873=CARTESIAN_POINT('Ctrl Pts',(-0.382178458559626,-0.209845485925839,
-0.313295473212942));
#51874=CARTESIAN_POINT('Ctrl Pts',(-0.0335698995935445,-0.434705065985486,
-0.29356841018425));
#51875=CARTESIAN_POINT('Ctrl Pts',(0.345428822663414,-0.266034713591485,
-0.273841347155558));
#51876=CARTESIAN_POINT('Ctrl Pts',(0.411717507348085,0.143472171132698,
-0.254114284126866));
#51877=CARTESIAN_POINT('Ctrl Pts',(0.105286157144576,0.423095659876829,
-0.234387221098174));
#51878=CARTESIAN_POINT('Ctrl Pts',(-0.296458573285809,0.319700294474994,
-0.214660158069482));
#51879=CARTESIAN_POINT('Ctrl Pts',(-0.42982534912142,-0.0731165253287872,
-0.19493309504079));
#51880=CARTESIAN_POINT('Ctrl Pts',(-0.174078917024553,-0.399736769822525,
-0.175206032012098));
#51881=CARTESIAN_POINT('Ctrl Pts',(0.239256717870959,-0.364493701490054,
-0.155478968983406));
#51882=CARTESIAN_POINT('Ctrl Pts',(0.435999944379018,0.000739035179609862,
-0.135751905954714));
#51883=CARTESIAN_POINT('Ctrl Pts',(0.238036761798838,0.365263419299111,
-0.116024842926023));
#51884=CARTESIAN_POINT('Ctrl Pts',(-0.175408803030969,0.399197187981461,
-0.0962977798973306));
#51885=CARTESIAN_POINT('Ctrl Pts',(-0.43007497292556,0.0716009816669133,
-0.076570716868639));
#51886=CARTESIAN_POINT('Ctrl Pts',(-0.295373939959455,-0.320536944194281,
-0.056843653839947));
#51887=CARTESIAN_POINT('Ctrl Pts',(0.106667041062779,-0.423035100006457,
-0.0371165908112548));
#51888=CARTESIAN_POINT('Ctrl Pts',(0.412267133134432,-0.14149617474194,
-0.017389527782563));
#51889=CARTESIAN_POINT('Ctrl Pts',(0.366956567112532,0.129967546999451,
-0.00423815243010174));
#51890=CARTESIAN_POINT('Ctrl Pts',(0.292087747121744,0.226511343217827,
0.00233753524612886));
#51891=CARTESIAN_POINT('Ctrl Pts',(-0.174869447533103,0.352286199445092,
-1.9567));
#51892=CARTESIAN_POINT('Ctrl Pts',(-0.291310645032558,0.294486581098146,
-1.95012431232377));
#51893=CARTESIAN_POINT('Ctrl Pts',(-0.460466557433677,0.055434592211573,
-1.93697293697131));
#51894=CARTESIAN_POINT('Ctrl Pts',(-0.298144091078689,-0.355823232196569,
-1.91724587394261));
#51895=CARTESIAN_POINT('Ctrl Pts',(0.134461295881938,-0.443877819611432,
-1.89751881091393));
#51896=CARTESIAN_POINT('Ctrl Pts',(0.445147114490617,-0.130638080935181,
-1.87779174788523));
#51897=CARTESIAN_POINT('Ctrl Pts',(0.352950856297826,0.301144654531963,
-1.85806468485654));
#51898=CARTESIAN_POINT('Ctrl Pts',(-0.0588177357417202,0.46016169961182,
-1.83833762182785));
#51899=CARTESIAN_POINT('Ctrl Pts',(-0.417312261114324,0.202678947727898,
-1.81861055879916));
#51900=CARTESIAN_POINT('Ctrl Pts',(-0.398036361464054,-0.238324695058641,
-1.79888349577047));
#51901=CARTESIAN_POINT('Ctrl Pts',(-0.0184182971104594,-0.463556937023687,
-1.77915643274177));
#51902=CARTESIAN_POINT('Ctrl Pts',(0.377869588997804,-0.269150752356283,
-1.75942936971308));
#51903=CARTESIAN_POINT('Ctrl Pts',(0.432081432251388,0.168918059316679,
-1.73970230668439));
#51904=CARTESIAN_POINT('Ctrl Pts',(0.0951371872085753,0.45406566287855,
-1.7199752436557));
#51905=CARTESIAN_POINT('Ctrl Pts',(-0.327932370894076,0.32815787152906,
-1.700248180627));
#51906=CARTESIAN_POINT('Ctrl Pts',(-0.454131340716204,-0.0948257382630977,
-1.68052111759831));
#51907=CARTESIAN_POINT('Ctrl Pts',(-0.169213776865482,-0.431965011214454,
-1.66079405456962));
#51908=CARTESIAN_POINT('Ctrl Pts',(0.268889690880362,-0.378054871853828,
-1.64106699154093));
#51909=CARTESIAN_POINT('Ctrl Pts',(0.463572526028849,0.0181011969713046,
-1.62133992851224));
#51910=CARTESIAN_POINT('Ctrl Pts',(0.238592033566427,0.39787054050644,-1.60161286548354));
#51911=CARTESIAN_POINT('Ctrl Pts',(-0.202381234110116,0.41745535472716,
-1.58188580245485));
#51912=CARTESIAN_POINT('Ctrl Pts',(-0.460142662617045,0.0591258363281124,
-1.56215873942616));
#51913=CARTESIAN_POINT('Ctrl Pts',(-0.301345771453645,-0.352729157915705,
-1.54243167639747));
#51914=CARTESIAN_POINT('Ctrl Pts',(0.130253658441064,-0.445265223149938,
-1.52270461336878));
#51915=CARTESIAN_POINT('Ctrl Pts',(0.443936953368175,-0.134711229744303,
-1.50297755034009));
#51916=CARTESIAN_POINT('Ctrl Pts',(0.355732648642495,0.297794251969122,
-1.48325048731139));
#51917=CARTESIAN_POINT('Ctrl Pts',(-0.0545095917427835,0.460712316371671,
-1.4635234242827));
#51918=CARTESIAN_POINT('Ctrl Pts',(-0.415405345558084,0.206556367230593,
-1.44379636125401));
#51919=CARTESIAN_POINT('Ctrl Pts',(-0.400242616767928,-0.234591094610938,
-1.42406929822532));
#51920=CARTESIAN_POINT('Ctrl Pts',(-0.0227479326789253,-0.463367743307965,
-1.40434223519663));
#51921=CARTESIAN_POINT('Ctrl Pts',(0.375340018065664,-0.272666471726358,
-1.38461517216793));
#51922=CARTESIAN_POINT('Ctrl Pts',(0.433639857885243,0.1648745208274,-1.36488810913924));
#51923=CARTESIAN_POINT('Ctrl Pts',(0.0993738613028271,0.453157775679392,
-1.34516104611055));
#51924=CARTESIAN_POINT('Ctrl Pts',(-0.324853383700292,0.331205997930529,
-1.32543398308186));
#51925=CARTESIAN_POINT('Ctrl Pts',(-0.454997098411088,-0.0905802097830019,
-1.30570692005317));
#51926=CARTESIAN_POINT('Ctrl Pts',(-0.173240676978726,-0.430365892941479,
-1.28597985702447));
#51927=CARTESIAN_POINT('Ctrl Pts',(0.265347202681679,-0.380549597287965,
-1.26625279399578));
#51928=CARTESIAN_POINT('Ctrl Pts',(0.463721355063991,0.0137709413146816,
-1.24652573096709));
#51929=CARTESIAN_POINT('Ctrl Pts',(0.242297469281596,0.395624911180872,
-1.2267986679384));
#51930=CARTESIAN_POINT('Ctrl Pts',(-0.198473662742448,0.419327245912648,
-1.20707160490971));
#51931=CARTESIAN_POINT('Ctrl Pts',(-0.45957039906139,0.0634206770198437,
-1.18734454188102));
#51932=CARTESIAN_POINT('Ctrl Pts',(-0.304626877976278,-0.349899412948255,
-1.16761747885232));
#51933=CARTESIAN_POINT('Ctrl Pts',(0.126089506165929,-0.446462283291582,
-1.14789041582363));
#51934=CARTESIAN_POINT('Ctrl Pts',(0.442659481600427,-0.138851421729646,
-1.12816335279494));
#51935=CARTESIAN_POINT('Ctrl Pts',(0.358498328477641,0.294458965640105,
-1.10843628976625));
#51936=CARTESIAN_POINT('Ctrl Pts',(-0.0502044773786194,0.461201305742126,
-1.08870922673755));
#51937=CARTESIAN_POINT('Ctrl Pts',(-0.413458133911737,0.210426959939374,
-1.06898216370886));
#51938=CARTESIAN_POINT('Ctrl Pts',(-0.402416081213446,-0.230842871988537,
-1.04925510068017));
#51939=CARTESIAN_POINT('Ctrl Pts',(-0.0270744775573185,-0.463135084648206,
-1.02952803765148));
#51940=CARTESIAN_POINT('Ctrl Pts',(0.37277713073582,-0.276159998492671,
-1.00980097462279));
#51941=CARTESIAN_POINT('Ctrl Pts',(0.435160760798787,0.160817431356566,
-0.990073911594096));
#51942=CARTESIAN_POINT('Ctrl Pts',(0.103601710252568,0.4522099286834,-0.970346848565403));
#51943=CARTESIAN_POINT('Ctrl Pts',(-0.321745979181209,0.334225461100479,
-0.950619785536713));
#51944=CARTESIAN_POINT('Ctrl Pts',(-0.455823211965335,-0.0863268984772914,
-0.930892722508018));
#51945=CARTESIAN_POINT('Ctrl Pts',(-0.177252443868371,-0.42872917454938,
-0.911165659479329));
#51946=CARTESIAN_POINT('Ctrl Pts',(0.261781557985834,-0.383011161541817,
-0.891438596450636));
#51947=CARTESIAN_POINT('Ctrl Pts',(0.463829742236249,0.00943950126637505,
-0.871711533421944));
#51948=CARTESIAN_POINT('Ctrl Pts',(0.245981767496114,0.393344764839436,
-0.851984470393252));
#51949=CARTESIAN_POINT('Ctrl Pts',(-0.194548777911764,0.421162565976776,
-0.83225740736456));
#51950=CARTESIAN_POINT('Ctrl Pts',(-0.458958050484476,0.0677099834780056,
-0.812530344335869));
#51951=CARTESIAN_POINT('Ctrl Pts',(-0.307881413061222,-0.347039146867505,
-0.792803281307175));
#51952=CARTESIAN_POINT('Ctrl Pts',(0.121914355536553,-0.447620401547131,
-0.773076218278485));
#51953=CARTESIAN_POINT('Ctrl Pts',(0.44134339911838,-0.142979502103395,
-0.753349155249792));
#51954=CARTESIAN_POINT('Ctrl Pts',(0.36123273834194,0.291097995041313,-0.733622092221101));
#51955=CARTESIAN_POINT('Ctrl Pts',(-0.0458949839108151,0.461650067062667,
-0.713895029192408));
#51956=CARTESIAN_POINT('Ctrl Pts',(-0.411474858524119,0.214279198172926,
-0.694167966163717));
#51957=CARTESIAN_POINT('Ctrl Pts',(-0.404554445030701,-0.227074514142221,
-0.674440903135024));
#51958=CARTESIAN_POINT('Ctrl Pts',(-0.0313986608775075,-0.462862029186305,
-0.654713840106333));
#51959=CARTESIAN_POINT('Ctrl Pts',(0.370181728037756,-0.279629437280525,
-0.63498677707764));
#51960=CARTESIAN_POINT('Ctrl Pts',(0.436643706947187,0.156746314630063,
-0.615259714048949));
#51961=CARTESIAN_POINT('Ctrl Pts',(0.10782052257582,0.451222637819076,-0.595532651020257));
#51962=CARTESIAN_POINT('Ctrl Pts',(-0.318610510468633,0.337215771552452,
-0.575805587991564));
#51963=CARTESIAN_POINT('Ctrl Pts',(-0.456609566478955,-0.0820660573266146,
-0.556078524962873));
#51964=CARTESIAN_POINT('Ctrl Pts',(-0.181248749969547,-0.427055060400831,
-0.53635146193418));
#51965=CARTESIAN_POINT('Ctrl Pts',(0.258193079476759,-0.385439317737961,
-0.51662439890549));
#51966=CARTESIAN_POINT('Ctrl Pts',(0.46389767199641,0.00510723780940766,
-0.496897335876797));
#51967=CARTESIAN_POINT('Ctrl Pts',(0.249644610036525,0.391030309219409,
-0.477170272848105));
#51968=CARTESIAN_POINT('Ctrl Pts',(-0.190606923642869,0.422961150078178,
-0.457443209819413));
#51969=CARTESIAN_POINT('Ctrl Pts',(-0.458305669395753,0.0719933843123827,
-0.437716146790721));
#51970=CARTESIAN_POINT('Ctrl Pts',(-0.31110909335493,-0.344148611091079,
-0.41798908376203));
#51971=CARTESIAN_POINT('Ctrl Pts',(0.117728571099989,-0.448739474933585,
-0.398262020733337));
#51972=CARTESIAN_POINT('Ctrl Pts',(0.439988820335115,-0.147095113657511,
-0.378534957704645));
#51973=CARTESIAN_POINT('Ctrl Pts',(0.363935640287352,0.287711638344625,
-0.358807894675954));
#51974=CARTESIAN_POINT('Ctrl Pts',(-0.0415814882171155,0.462058551832881,
-0.339080831647261));
#51975=CARTESIAN_POINT('Ctrl Pts',(-0.409455690548052,0.21811276372184,
-0.31935376861857));
#51976=CARTESIAN_POINT('Ctrl Pts',(-0.406657525198516,-0.223286383806917,
-0.299626705589878));
#51977=CARTESIAN_POINT('Ctrl Pts',(-0.0357200987761702,-0.462548535548439,
-0.279899642561186));
#51978=CARTESIAN_POINT('Ctrl Pts',(0.367554023546892,-0.283074610363292,
-0.260172579532494));
#51979=CARTESIAN_POINT('Ctrl Pts',(0.438088591518437,0.152661765049684,
-0.240445516503802));
#51980=CARTESIAN_POINT('Ctrl Pts',(0.112029883273486,0.450195530685307,
-0.22071845347511));
#51981=CARTESIAN_POINT('Ctrl Pts',(-0.315447160969382,0.340177547019319,
-0.200991390446418));
#51982=CARTESIAN_POINT('Ctrl Pts',(-0.457356265970795,-0.0777997413914402,
-0.181264327417726));
#51983=CARTESIAN_POINT('Ctrl Pts',(-0.185228915970936,-0.425340470940003,
-0.161537264389034));
#51984=CARTESIAN_POINT('Ctrl Pts',(0.254581446435298,-0.387840034618976,
-0.141810201360342));
#51985=CARTESIAN_POINT('Ctrl Pts',(0.463926352720374,0.000786371420059956,
-0.12208313833165));
#51986=CARTESIAN_POINT('Ctrl Pts',(0.253283350464616,0.38865905393396,-0.102356075302958));
#51987=CARTESIAN_POINT('Ctrl Pts',(-0.186643983042487,0.424766328124745,
-0.0826290122742664));
#51988=CARTESIAN_POINT('Ctrl Pts',(-0.457621878529922,0.0761871250310393,
-0.0629019492455744));
#51989=CARTESIAN_POINT('Ctrl Pts',(-0.314293055356251,-0.341067785327318,
-0.0431748862168827));
#51990=CARTESIAN_POINT('Ctrl Pts',(0.113499214744647,-0.450131091870246,
-0.0234478231881903));
#51991=CARTESIAN_POINT('Ctrl Pts',(0.43867342160777,-0.150559203316891,
-0.00372076015949866));
#51992=CARTESIAN_POINT('Ctrl Pts',(0.390460650241079,0.138292150787645,
0.00943061519296265));
#51993=CARTESIAN_POINT('Ctrl Pts',(0.310796377255278,0.241019712648146,
0.0160063028691932));
#51994=CARTESIAN_POINT('Ctrl Pts',(-0.39355449651014,0.000302947205131077,
-0.0596163522034978));
#51995=CARTESIAN_POINT('Ctrl Pts',(-0.392615901123677,-0.10780295630061,
-0.0541358635412927));
#51996=CARTESIAN_POINT('Ctrl Pts',(-0.346215696154532,-0.216592774920967,
-0.0486553748790877));
#51997=CARTESIAN_POINT('Ctrl Pts',(-0.266882480868379,-0.289702518024748,
-0.0431748862168825));
#51998=CARTESIAN_POINT('Ctrl Pts',(-0.179185181721266,-0.370520205652994,
-0.037116590811255));
#51999=CARTESIAN_POINT('Ctrl Pts',(-0.0512445669495005,-0.407737732630776,
-0.0310582954056274));
#52000=CARTESIAN_POINT('Ctrl Pts',(0.0664872943522231,-0.388263316286114,
-0.0249999999999998));
#52001=CARTESIAN_POINT('',(-0.187158653173901,-0.262360084935059,-1.9567));
#52002=CARTESIAN_POINT('Ctrl Pts',(-0.187552813085389,-0.262697816057798,
-1.9567));
#52003=CARTESIAN_POINT('Ctrl Pts',(-0.194935548663329,-0.258593826308098,
-1.9567));
#52004=CARTESIAN_POINT('Ctrl Pts',(-0.202131816688224,-0.254190080955628,
-1.9567));
#52005=CARTESIAN_POINT('Ctrl Pts',(-0.209120909772877,-0.24949064758629,
-1.9567));
#52006=CARTESIAN_POINT('Ctrl Pts',(-0.222223442058356,-0.240680566407027,
-1.9567));
#52007=CARTESIAN_POINT('Ctrl Pts',(-0.234598714218232,-0.230832940046298,
-1.9567));
#52008=CARTESIAN_POINT('Ctrl Pts',(-0.246211636410528,-0.22008391613474,
-1.9567));
#52009=CARTESIAN_POINT('Ctrl Pts',(-0.25218100502691,-0.214558615531508,
-1.9567));
#52010=CARTESIAN_POINT('Ctrl Pts',(-0.257951737717882,-0.208790930776044,
-1.9567));
#52011=CARTESIAN_POINT('Ctrl Pts',(-0.263498052368722,-0.202819781274129,
-1.9567));
#52012=CARTESIAN_POINT('Ctrl Pts',(-0.27392963993244,-0.191589158273713,
-1.9567));
#52013=CARTESIAN_POINT('Ctrl Pts',(-0.283582022411786,-0.179628639232479,
-1.9567));
#52014=CARTESIAN_POINT('Ctrl Pts',(-0.292422866190421,-0.167055175905498,
-1.9567));
#52015=CARTESIAN_POINT('Ctrl Pts',(-0.297639339867104,-0.159636298011915,
-1.9567));
#52016=CARTESIAN_POINT('Ctrl Pts',(-0.302573086946691,-0.152003640288341,
-1.9567));
#52017=CARTESIAN_POINT('Ctrl Pts',(-0.307215418838992,-0.144178520553397,
-1.9567));
#52018=CARTESIAN_POINT('Ctrl Pts',(-0.310148605333973,-0.139234338176816,
-1.9567));
#52019=CARTESIAN_POINT('Ctrl Pts',(-0.312961281228168,-0.13422009210485,
-1.9567));
#52020=CARTESIAN_POINT('Ctrl Pts',(-0.315649496491177,-0.129146472523924,
-1.9567));
#52021=CARTESIAN_POINT('Ctrl Pts',(-0.325055516088252,-0.111393963689168,
-1.9567));
#52022=CARTESIAN_POINT('Ctrl Pts',(-0.332950944425937,-0.0929001179375588,
-1.9567));
#52023=CARTESIAN_POINT('Ctrl Pts',(-0.339260540400532,-0.073901239993573,
-1.9567));
#52024=CARTESIAN_POINT('Ctrl Pts',(-0.343323872756722,-0.0616661054791059,
-1.9567));
#52025=CARTESIAN_POINT('Ctrl Pts',(-0.346728888529677,-0.0492205679713237,
-1.9567));
#52026=CARTESIAN_POINT('Ctrl Pts',(-0.349446343340807,-0.0366210092019528,
-1.9567));
#52027=CARTESIAN_POINT('Ctrl Pts',(-0.350667565657802,-0.0309587761850763,
-1.9567));
#52028=CARTESIAN_POINT('Ctrl Pts',(-0.351749819276766,-0.0252653862353323,
-1.9567));
#52029=CARTESIAN_POINT('Ctrl Pts',(-0.352689875393039,-0.0195457697562147,
-1.9567));
#52030=CARTESIAN_POINT('Ctrl Pts',(-0.353507442449902,-0.014571417767787,
-1.9567));
#52031=CARTESIAN_POINT('Ctrl Pts',(-0.354216678467517,-0.00958102422836672,
-1.9567));
#52032=CARTESIAN_POINT('Ctrl Pts',(-0.35481498228772,-0.00458766379930495,
-1.9567));
#52033=CARTESIAN_POINT('Ctrl Pts',(-0.356697198872877,0.0111210539087855,
-1.9567));
#52034=CARTESIAN_POINT('Ctrl Pts',(-0.357487439202542,0.0268861216299494,
-1.9567));
#52035=CARTESIAN_POINT('Ctrl Pts',(-0.357144615700508,0.0426014586103036,
-1.9567));
#52036=CARTESIAN_POINT('Ctrl Pts',(-0.356807049244469,0.0580758078846414,
-1.9567));
#52037=CARTESIAN_POINT('Ctrl Pts',(-0.355371211339537,0.073502369822222,
-1.9567));
#52038=CARTESIAN_POINT('Ctrl Pts',(-0.352905425918931,0.0888045736652499,
-1.9567));
#52039=CARTESIAN_POINT('Ctrl Pts',(-0.351706553656186,0.0962445510424256,
-1.9567));
#52040=CARTESIAN_POINT('Ctrl Pts',(-0.350263912372945,0.103655167772351,
-1.9567));
#52041=CARTESIAN_POINT('Ctrl Pts',(-0.348583746098634,0.111027644159136,
-1.9567));
#52042=CARTESIAN_POINT('Ctrl Pts',(-0.347031212449488,0.117840075668466,
-1.9567));
#52043=CARTESIAN_POINT('Ctrl Pts',(-0.345274228680375,0.124624481655365,
-1.9567));
#52044=CARTESIAN_POINT('Ctrl Pts',(-0.343326242497342,0.131345086743347,
-1.9567));
#52045=CARTESIAN_POINT('Ctrl Pts',(-0.337583166709954,0.151158853747225,
-1.9567));
#52046=CARTESIAN_POINT('Ctrl Pts',(-0.33017628709199,0.170461698596435,
-1.9567));
#52047=CARTESIAN_POINT('Ctrl Pts',(-0.321266461276679,0.189081419077276,
-1.9567));
#52048=CARTESIAN_POINT('Ctrl Pts',(-0.31329530345099,0.20573951472354,-1.9567));
#52049=CARTESIAN_POINT('Ctrl Pts',(-0.304120165756624,0.221851611522826,
-1.9567));
#52050=CARTESIAN_POINT('Ctrl Pts',(-0.293823122110593,0.237289775994537,
-1.9567));
#52051=CARTESIAN_POINT('Ctrl Pts',(-0.290958000853211,0.241585398575482,
-1.9567));
#52052=CARTESIAN_POINT('Ctrl Pts',(-0.28800585086645,0.24582877974099,-1.9567));
#52053=CARTESIAN_POINT('Ctrl Pts',(-0.284968063826039,0.250016978740807,
-1.9567));
#52054=CARTESIAN_POINT('Ctrl Pts',(-0.281677119186157,0.254554206290288,
-1.9567));
#52055=CARTESIAN_POINT('Ctrl Pts',(-0.27829098021799,0.259019238257219,
-1.9567));
#52056=CARTESIAN_POINT('Ctrl Pts',(-0.274815287336952,0.263405262319202,
-1.9567));
#52057=CARTESIAN_POINT('Ctrl Pts',(-0.260861563440262,0.2810136560582,-1.9567));
#52058=CARTESIAN_POINT('Ctrl Pts',(-0.245455106563924,0.297369120256383,
-1.9567));
#52059=CARTESIAN_POINT('Ctrl Pts',(-0.228753469246794,0.312258507679545,
-1.9567));
#52060=CARTESIAN_POINT('Ctrl Pts',(-0.212051831929664,0.327147895102707,
-1.9567));
#52061=CARTESIAN_POINT('Ctrl Pts',(-0.194054188732127,0.340572959327143,
-1.9567));
#52062=CARTESIAN_POINT('Ctrl Pts',(-0.174869447533103,0.352286199445092,
-1.9567));
#52063=CARTESIAN_POINT('Ctrl Pts',(-0.187552813085386,-0.2626978160578,
-1.9567));
#52064=CARTESIAN_POINT('Ctrl Pts',(-0.107650951219408,-0.319062579074347,
-1.95064170459437));
#52065=CARTESIAN_POINT('Ctrl Pts',(0.116856291925146,-0.356987215547139,
-1.93800772151252));
#52066=CARTESIAN_POINT('Ctrl Pts',(0.364759182106444,-0.107046497669421,
-1.91879805075442));
#52067=CARTESIAN_POINT('Ctrl Pts',(0.289212400745945,0.246761743044216,
-1.89907098772573));
#52068=CARTESIAN_POINT('Ctrl Pts',(-0.0481959974222359,0.377062323270783,
-1.87934392469704));
#52069=CARTESIAN_POINT('Ctrl Pts',(-0.288676763686436,0.204340998144533,
-1.86319448047936));
#52070=CARTESIAN_POINT('Ctrl Pts',(-0.321878386934234,0.0488203878451577,
-1.85362072393791));
#52071=CARTESIAN_POINT('Ctrl Pts',(-0.321776643047528,7.65958109301274E-5,
-1.85062265507269));
#52072=CARTESIAN_POINT('Origin',(-5.160062080289E-17,2.1385152528819E-17,
-1.9567));
#52073=CARTESIAN_POINT('',(-0.3933,-4.81653586104654E-17,-1.9567));
#52074=CARTESIAN_POINT('Origin',(0.,0.,-1.9567));
#52075=CARTESIAN_POINT('Origin',(0.,0.,-1.9567));
#52076=CARTESIAN_POINT('',(0.1871586531739,-0.26236008493506,-1.9567));
#52077=CARTESIAN_POINT('Ctrl Pts',(0.175279276633882,0.352769203968885,
-1.9567));
#52078=CARTESIAN_POINT('Ctrl Pts',(0.18401188138755,0.347494710900982,-1.9567));
#52079=CARTESIAN_POINT('Ctrl Pts',(0.192510825180566,0.341867276831141,
-1.9567));
#52080=CARTESIAN_POINT('Ctrl Pts',(0.200751394782037,0.335885922983975,
-1.9567));
#52081=CARTESIAN_POINT('Ctrl Pts',(0.213438686096218,0.326676950500004,
-1.9567));
#52082=CARTESIAN_POINT('Ctrl Pts',(0.225514123628146,0.31662934757912,-1.9567));
#52083=CARTESIAN_POINT('Ctrl Pts',(0.236936545916664,0.305829861134869,
-1.9567));
#52084=CARTESIAN_POINT('Ctrl Pts',(0.242016167800701,0.301027262676071,
-1.9567));
#52085=CARTESIAN_POINT('Ctrl Pts',(0.24696649261074,0.296075857763358,-1.9567));
#52086=CARTESIAN_POINT('Ctrl Pts',(0.251783114237367,0.290982853163268,
-1.9567));
#52087=CARTESIAN_POINT('Ctrl Pts',(0.256613931187417,0.285874838696699,
-1.9567));
#52088=CARTESIAN_POINT('Ctrl Pts',(0.261305021417189,0.28062973144462,-1.9567));
#52089=CARTESIAN_POINT('Ctrl Pts',(0.265847944049976,0.275261265940149,
-1.9567));
#52090=CARTESIAN_POINT('Ctrl Pts',(0.279770568182666,0.258808613445338,
-1.9567));
#52091=CARTESIAN_POINT('Ctrl Pts',(0.292320623894356,0.241182479441691,
-1.9567));
#52092=CARTESIAN_POINT('Ctrl Pts',(0.303375664813956,0.222603261998498,
-1.9567));
#52093=CARTESIAN_POINT('Ctrl Pts',(0.306375953356426,0.217560945680695,
-1.9567));
#52094=CARTESIAN_POINT('Ctrl Pts',(0.309266773479844,0.212446594923143,
-1.9567));
#52095=CARTESIAN_POINT('Ctrl Pts',(0.312042062173041,0.207270037278723,
-1.9567));
#52096=CARTESIAN_POINT('Ctrl Pts',(0.321991404607397,0.188712204084018,
-1.9567));
#52097=CARTESIAN_POINT('Ctrl Pts',(0.330416802963934,0.169438735026911,
-1.9567));
#52098=CARTESIAN_POINT('Ctrl Pts',(0.337214313055224,0.14965760095231,-1.9567));
#52099=CARTESIAN_POINT('Ctrl Pts',(0.343828133188892,0.13041101491531,-1.9567));
#52100=CARTESIAN_POINT('Ctrl Pts',(0.348901095948526,0.110682458297764,
-1.9567));
#52101=CARTESIAN_POINT('Ctrl Pts',(0.352289246031495,0.0906606792142431,
-1.9567));
#52102=CARTESIAN_POINT('Ctrl Pts',(0.353252716161339,0.0849671929102308,
-1.9567));
#52103=CARTESIAN_POINT('Ctrl Pts',(0.354079629151872,0.0792500462139911,
-1.9567));
#52104=CARTESIAN_POINT('Ctrl Pts',(0.354765894650996,0.0735137648268453,
-1.9567));
#52105=CARTESIAN_POINT('Ctrl Pts',(0.355373602604548,0.0684341217044198,
-1.9567));
#52106=CARTESIAN_POINT('Ctrl Pts',(0.355869792336237,0.0633496018900003,
-1.9567));
#52107=CARTESIAN_POINT('Ctrl Pts',(0.356252722462039,0.0582640302401743,
-1.9567));
#52108=CARTESIAN_POINT('Ctrl Pts',(0.357356305926245,0.0436076937426857,
-1.9567));
#52109=CARTESIAN_POINT('Ctrl Pts',(0.357520611329765,0.02894029824759,-1.9567));
#52110=CARTESIAN_POINT('Ctrl Pts',(0.356695878885865,0.014335105717066,
-1.9567));
#52111=CARTESIAN_POINT('Ctrl Pts',(0.355625235707653,-0.00462492170141671,
-1.9567));
#52112=CARTESIAN_POINT('Ctrl Pts',(0.352888647131212,-0.0234812913700506,
-1.9567));
#52113=CARTESIAN_POINT('Ctrl Pts',(0.348579205973286,-0.0420611896612138,
-1.9567));
#52114=CARTESIAN_POINT('Ctrl Pts',(0.347014174789672,-0.0488087281815105,
-1.9567));
#52115=CARTESIAN_POINT('Ctrl Pts',(0.345241366742302,-0.0555196103104209,
-1.9567));
#52116=CARTESIAN_POINT('Ctrl Pts',(0.343264193680855,-0.0621847523977205,
-1.9567));
#52117=CARTESIAN_POINT('Ctrl Pts',(0.341896092993538,-0.0667966832643223,
-1.9567));
#52118=CARTESIAN_POINT('Ctrl Pts',(0.340432832629664,-0.0713775965145813,
-1.9567));
#52119=CARTESIAN_POINT('Ctrl Pts',(0.338876628876197,-0.0759244413272143,
-1.9567));
#52120=CARTESIAN_POINT('Ctrl Pts',(0.332244083465024,-0.0953031085680316,
-1.9567));
#52121=CARTESIAN_POINT('Ctrl Pts',(0.323926310238762,-0.114068452668091,
-1.9567));
#52122=CARTESIAN_POINT('Ctrl Pts',(0.3140504528883,-0.132005064082091,-1.9567));
#52123=CARTESIAN_POINT('Ctrl Pts',(0.306024769014135,-0.146581375573242,
-1.9567));
#52124=CARTESIAN_POINT('Ctrl Pts',(0.29696875672258,-0.160610304807908,
-1.9567));
#52125=CARTESIAN_POINT('Ctrl Pts',(0.286930938141069,-0.173954621270129,
-1.9567));
#52126=CARTESIAN_POINT('Ctrl Pts',(0.283445195364828,-0.178588581760084,
-1.9567));
#52127=CARTESIAN_POINT('Ctrl Pts',(0.279839658893929,-0.183140879903125,
-1.9567));
#52128=CARTESIAN_POINT('Ctrl Pts',(0.27613006525648,-0.187589437428766,
-1.9567));
#52129=CARTESIAN_POINT('Ctrl Pts',(0.263608466539964,-0.202605381935755,
-1.9567));
#52130=CARTESIAN_POINT('Ctrl Pts',(0.249871950203262,-0.216487429108968,
-1.9567));
#52131=CARTESIAN_POINT('Ctrl Pts',(0.235016030681469,-0.229027530560931,
-1.9567));
#52132=CARTESIAN_POINT('Ctrl Pts',(0.221150303831382,-0.240731795729455,
-1.9567));
#52133=CARTESIAN_POINT('Ctrl Pts',(0.206308357805613,-0.251267486368473,
-1.9567));
#52134=CARTESIAN_POINT('Ctrl Pts',(0.19054896038177,-0.260420468537189,
-1.9567));
#52135=CARTESIAN_POINT('Ctrl Pts',(0.189423535078913,-0.261074110136054,
-1.9567));
#52136=CARTESIAN_POINT('Ctrl Pts',(0.188293426184883,-0.261720678387043,
-1.9567));
#52137=CARTESIAN_POINT('Ctrl Pts',(0.187158653173905,-0.262360084935056,
-1.9567));
#52138=CARTESIAN_POINT('Origin',(0.,0.,-1.9567));
#52139=CARTESIAN_POINT('Origin',(0.,0.,-2.18777734492731));
#52140=CARTESIAN_POINT('Ctrl Pts',(0.187158653173899,-0.26236008493506,
-1.9567));
#52141=CARTESIAN_POINT('Ctrl Pts',(0.273876561834578,-0.200498514052405,
-1.95012431232377));
#52142=CARTESIAN_POINT('Ctrl Pts',(0.379746143677233,0.0148475562970276,
-1.93697293697131));
#52143=CARTESIAN_POINT('Ctrl Pts',(0.195093989204632,0.326547069892489,
-1.91724587394262));
#52144=CARTESIAN_POINT('Ctrl Pts',(-0.166339572492541,0.341705098143136,
-1.89751881091393));
#52145=CARTESIAN_POINT('Ctrl Pts',(-0.315802122696145,0.133412836380506,
-1.88352930124216));
#52146=CARTESIAN_POINT('Ctrl Pts',(-0.322694708293171,0.013773349684675,
-1.87611547924662));
#52147=CARTESIAN_POINT('Ctrl Pts',(-0.322590464231506,0.000235348495535932,
-1.87527734492731));
#52148=CARTESIAN_POINT('Ctrl Pts',(0.228405859260858,-0.320180657528385,
-1.99770630286919));
#52149=CARTESIAN_POINT('Ctrl Pts',(0.334235208345475,-0.2446856429348,-1.99113061519296));
#52150=CARTESIAN_POINT('Ctrl Pts',(0.463436997310544,0.0181197545314356,
-1.9779792398405));
#52151=CARTESIAN_POINT('Ctrl Pts',(0.238090034765911,0.398513575637932,
-1.95825217681181));
#52152=CARTESIAN_POINT('Ctrl Pts',(-0.202998538084909,0.417012225893093,
-1.93852511378312));
#52153=CARTESIAN_POINT('Ctrl Pts',(-0.46020960849542,0.0585607239402074,
-1.91879805075443));
#52154=CARTESIAN_POINT('Ctrl Pts',(-0.300857582100874,-0.353195579667294,
-1.89907098772573));
#52155=CARTESIAN_POINT('Ctrl Pts',(0.130884172489321,-0.445059242440821,
-1.87934392469704));
#52156=CARTESIAN_POINT('Ctrl Pts',(0.444123796084404,-0.134098311339552,
-1.85961686166835));
#52157=CARTESIAN_POINT('Ctrl Pts',(0.355314607575829,0.298300456258092,
-1.83988979863966));
#52158=CARTESIAN_POINT('Ctrl Pts',(-0.0551582109203669,0.460632047901516,
-1.82016273561097));
#52159=CARTESIAN_POINT('Ctrl Pts',(-0.415695200902475,0.205973509912391,
-1.80043567258227));
#52160=CARTESIAN_POINT('Ctrl Pts',(-0.399912434497174,-0.235154744428263,
-1.78070860955358));
#52161=CARTESIAN_POINT('Ctrl Pts',(-0.0220960326100466,-0.463398870372397,
-1.76098154652489));
#52162=CARTESIAN_POINT('Ctrl Pts',(0.375723176606882,-0.272138490671688,
-1.7412544834962));
#52163=CARTESIAN_POINT('Ctrl Pts',(0.433407568855471,0.165484470229036,
-1.72152742046751));
#52164=CARTESIAN_POINT('Ctrl Pts',(0.0987363280065334,0.453297084197232,
-1.70180035743881));
#52165=CARTESIAN_POINT('Ctrl Pts',(-0.325318971049406,0.330748778547112,
-1.68207329441012));
#52166=CARTESIAN_POINT('Ctrl Pts',(-0.454869275255104,-0.0912201632159526,
-1.66234623138143));
#52167=CARTESIAN_POINT('Ctrl Pts',(-0.172635147307492,-0.430609181263529,
-1.64261916835274));
#52168=CARTESIAN_POINT('Ctrl Pts',(0.26588225829714,-0.38017600839589,-1.62289210532405));
#52169=CARTESIAN_POINT('Ctrl Pts',(0.463701564277583,0.0144232213412824,
-1.60316504229535));
#52170=CARTESIAN_POINT('Ctrl Pts',(0.241740746627904,0.395965377009238,
-1.58343797926666));
#52171=CARTESIAN_POINT('Ctrl Pts',(-0.199063326056669,0.419047684931453,
-1.56371091623797));
#52172=CARTESIAN_POINT('Ctrl Pts',(-0.459659192619251,0.062774168035161,
-1.54398385320928));
#52173=CARTESIAN_POINT('Ctrl Pts',(-0.304134418435672,-0.35032759652435,
-1.52425679018059));
#52174=CARTESIAN_POINT('Ctrl Pts',(0.126717404514493,-0.446284515738235,
-1.50452972715189));
#52175=CARTESIAN_POINT('Ctrl Pts',(0.442854394504287,-0.13822863226102,
-1.4848026641232));
#52176=CARTESIAN_POINT('Ctrl Pts',(0.358083804993756,0.294962977500616,
-1.46507560109451));
#52177=CARTESIAN_POINT('Ctrl Pts',(-0.0508531770824176,0.461130267827548,
-1.44534853806582));
#52178=CARTESIAN_POINT('Ctrl Pts',(-0.413753754459456,0.209845181461624,
-1.42562147503713));
#52179=CARTESIAN_POINT('Ctrl Pts',(-0.402091002995042,-0.23140871812004,
-1.40589441200844));
#52180=CARTESIAN_POINT('Ctrl Pts',(-0.0264229876441398,-0.46317274880931,
-1.38616734897974));
#52181=CARTESIAN_POINT('Ctrl Pts',(0.373165251036872,-0.275635384034748,
-1.36644028595105));
#52182=CARTESIAN_POINT('Ctrl Pts',(0.434934153631336,0.161429401035068,
-1.34671322292236));
#52183=CARTESIAN_POINT('Ctrl Pts',(0.102965518734258,0.452355249185692,
-1.32698615989367));
#52184=CARTESIAN_POINT('Ctrl Pts',(-0.322215823085459,0.333772576565373,
-1.30725909686498));
#52185=CARTESIAN_POINT('Ctrl Pts',(-0.455701367591052,-0.0869680003761401,
-1.28753203383628));
#52186=CARTESIAN_POINT('Ctrl Pts',(-0.176649214587937,-0.428978116573918,
-1.26780497080759));
#52187=CARTESIAN_POINT('Ctrl Pts',(0.262320080288335,-0.382642581257384,
-1.2480779077789));
#52188=CARTESIAN_POINT('Ctrl Pts',(0.463816043661282,0.0100919352058466,
-1.22835084475021));
#52189=CARTESIAN_POINT('Ctrl Pts',(0.24542824910056,0.393690416516892,-1.20862378172152));
#52190=CARTESIAN_POINT('Ctrl Pts',(-0.19514102655331,0.420888523565948,
-1.18889671869283));
#52191=CARTESIAN_POINT('Ctrl Pts',(-0.45905287804943,0.0670643323111496,
-1.16916965566413));
#52192=CARTESIAN_POINT('Ctrl Pts',(-0.307392973975953,-0.347471911187113,
-1.14944259263544));
#52193=CARTESIAN_POINT('Ctrl Pts',(0.122543886747367,-0.447448505791062,
-1.12971552960675));
#52194=CARTESIAN_POINT('Ctrl Pts',(0.441544119938114,-0.142358560198823,
-1.10998846657806));
#52195=CARTESIAN_POINT('Ctrl Pts',(0.360822940066819,0.291605856311808,
-1.09026140354936));
#52196=CARTESIAN_POINT('Ctrl Pts',(-0.0465443187714532,0.461585090643,-1.07053434052067));
#52197=CARTESIAN_POINT('Ctrl Pts',(-0.411775899589728,0.213700205968258,
-1.05080727749198));
#52198=CARTESIAN_POINT('Ctrl Pts',(-0.40423466560533,-0.227643371607329,
-1.03108021446329));
#52199=CARTESIAN_POINT('Ctrl Pts',(-0.0307475511343536,-0.462905776171616,
-1.0113531514346));
#52200=CARTESIAN_POINT('Ctrl Pts',(0.370574730951002,-0.279108470481276,
-0.991626088405904));
#52201=CARTESIAN_POINT('Ctrl Pts',(0.436422825039965,0.157360373976237,
-0.971899025377213));
#52202=CARTESIAN_POINT('Ctrl Pts',(0.107185715996899,0.451373893573872,
-0.952171962348521));
#52203=CARTESIAN_POINT('Ctrl Pts',(-0.319084563512467,0.336767294792508,
-0.932444899319829));
#52204=CARTESIAN_POINT('Ctrl Pts',(-0.456493714871459,-0.0827082692157297,
-0.912717836291138));
#52205=CARTESIAN_POINT('Ctrl Pts',(-0.180647871943726,-0.42730962530232,
-0.892990773262446));
#52206=CARTESIAN_POINT('Ctrl Pts',(0.258735020577411,-0.385075782983832,
-0.873263710233753));
#52207=CARTESIAN_POINT('Ctrl Pts',(0.463890067309698,0.00575977128100029,
-0.853536647205063));
#52208=CARTESIAN_POINT('Ctrl Pts',(0.249094343920831,0.39138111520672,-0.833809584176368));
#52209=CARTESIAN_POINT('Ctrl Pts',(-0.191201705804062,0.422692651002389,
-0.814082521147679));
#52210=CARTESIAN_POINT('Ctrl Pts',(-0.458406522800986,0.071348646569588,
-0.794355458118984));
#52211=CARTESIAN_POINT('Ctrl Pts',(-0.310624717223144,-0.344585917535574,
-0.774628395090295));
#52212=CARTESIAN_POINT('Ctrl Pts',(0.11835968010892,-0.44857346738116,-0.754901332061601));
#52213=CARTESIAN_POINT('Ctrl Pts',(0.440195331831274,-0.146476070904889,
-0.73517426903291));
#52214=CARTESIAN_POINT('Ctrl Pts',(0.363530602464719,0.288223299865512,
-0.715447206004218));
#52215=CARTESIAN_POINT('Ctrl Pts',(-0.0422314006439752,0.461999651854537,
-0.695720142975526));
#52216=CARTESIAN_POINT('Ctrl Pts',(-0.409762127694936,0.217536590532415,
-0.675993079946833));
#52217=CARTESIAN_POINT('Ctrl Pts',(-0.40634306897038,-0.223858168966707,
-0.656266016918143));
#52218=CARTESIAN_POINT('Ctrl Pts',(-0.0350694326791201,-0.46259842672363,
-0.636538953889449));
#52219=CARTESIAN_POINT('Ctrl Pts',(0.367951887597995,-0.2825572117724,-0.616811890860759));
#52220=CARTESIAN_POINT('Ctrl Pts',(0.437873429602004,0.153277621199368,
-0.597084827832066));
#52221=CARTESIAN_POINT('Ctrl Pts',(0.111396564017626,0.450353167026888,
-0.577357764803374));
#52222=CARTESIAN_POINT('Ctrl Pts',(-0.315925471884904,0.339732638569118,
-0.557630701774683));
#52223=CARTESIAN_POINT('Ctrl Pts',(-0.457246244630668,-0.0784413238010682,
-0.53790363874599));
#52224=CARTESIAN_POINT('Ctrl Pts',(-0.184630772338759,-0.425603862177253,
-0.518176575717299));
#52225=CARTESIAN_POINT('Ctrl Pts',(0.25512739277303,-0.387475396406749,
-0.498449512688606));
#52226=CARTESIAN_POINT('Ctrl Pts',(0.463923628310023,0.00142710460425383,
-0.478722449659915));
#52227=CARTESIAN_POINT('Ctrl Pts',(0.252738711523979,0.389037676484367,
-0.458995386631223));
#52228=CARTESIAN_POINT('Ctrl Pts',(-0.187245707469103,0.42445990788846,
-0.43926832360253));
#52229=CARTESIAN_POINT('Ctrl Pts',(-0.457720183329313,0.0756267399820685,
-0.419541260573839));
#52230=CARTESIAN_POINT('Ctrl Pts',(-0.313829366046916,-0.341669872308943,
-0.399814197545147));
#52231=CARTESIAN_POINT('Ctrl Pts',(0.114165149051204,-0.449659293039122,
-0.380087134516455));
#52232=CARTESIAN_POINT('Ctrl Pts',(0.438808148842419,-0.15058082300791,
-0.360360071487763));
#52233=CARTESIAN_POINT('Ctrl Pts',(0.366206554061265,0.284815637206989,
-0.340633008459071));
#52234=CARTESIAN_POINT('Ctrl Pts',(-0.0379147951462677,0.462373850167741,
-0.320905945430379));
#52235=CARTESIAN_POINT('Ctrl Pts',(-0.407712621610348,0.221354125346273,
-0.301178882401688));
#52236=CARTESIAN_POINT('Ctrl Pts',(-0.408416015413171,-0.220053679584459,
-0.281451819372995));
#52237=CARTESIAN_POINT('Ctrl Pts',(-0.0393882817008329,-0.462250268776744,
-0.261724756344303));
#52238=CARTESIAN_POINT('Ctrl Pts',(0.365297000348705,-0.285982185859218,
-0.241997693315612));
#52239=CARTESIAN_POINT('Ctrl Pts',(0.439285743818393,0.149183183090122,
-0.222270630286919));
#52240=CARTESIAN_POINT('Ctrl Pts',(0.115597881363113,0.449289930457205,
-0.202543567258228));
#52241=CARTESIAN_POINT('Ctrl Pts',(-0.312739179970523,0.342674536363465,
-0.182816504229535));
#52242=CARTESIAN_POINT('Ctrl Pts',(-0.457958208506169,-0.0741793948098823,
-0.163089441200844));
#52243=CARTESIAN_POINT('Ctrl Pts',(-0.188598876777895,-0.423838246939006,
-0.143362378172152));
#52244=CARTESIAN_POINT('Ctrl Pts',(0.251500018239493,-0.389884781736394,
-0.123635315143459));
#52245=CARTESIAN_POINT('Ctrl Pts',(0.463911928887255,-0.00282212260801893,
-0.103908252114768));
#52246=CARTESIAN_POINT('Ctrl Pts',(0.256370137272232,0.386499619306331,
-0.0841811890860756));
#52247=CARTESIAN_POINT('Ctrl Pts',(-0.183290037428914,0.42650286845679,
-0.0644541260573842));
#52248=CARTESIAN_POINT('Ctrl Pts',(-0.456969028708115,0.0792558059832603,
-0.0447270630286917));
#52249=CARTESIAN_POINT('Ctrl Pts',(-0.36366155271696,-0.198329305529085,
-0.0315756876762305));
#52250=CARTESIAN_POINT('Ctrl Pts',(-0.268747084003623,-0.287158309717044,
-0.0249999999999999));
#52251=CARTESIAN_POINT('Ctrl Pts',(0.214656790565205,-0.30090713333061,
-1.98403753524613));
#52252=CARTESIAN_POINT('Ctrl Pts',(0.314115659508509,-0.229956599974001,
-1.9774618475699));
#52253=CARTESIAN_POINT('Ctrl Pts',(0.435540046099441,0.0170290217866327,
-1.96431047221744));
#52254=CARTESIAN_POINT('Ctrl Pts',(0.223758019578818,0.374524740389451,
-1.94458340918874));
#52255=CARTESIAN_POINT('Ctrl Pts',(-0.190778882887453,0.391909849976441,
-1.92485634616005));
#52256=CARTESIAN_POINT('Ctrl Pts',(-0.432506932469158,0.0550356155260572,
-1.90512928313136));
#52257=CARTESIAN_POINT('Ctrl Pts',(-0.282747225486995,-0.331934696502731,
-1.88540222010267));
#52258=CARTESIAN_POINT('Ctrl Pts',(0.123005497727857,-0.418268554505945,
-1.86567515707398));
#52259=CARTESIAN_POINT('Ctrl Pts',(0.417389418071951,-0.126026158985205,
-1.84594809404529));
#52260=CARTESIAN_POINT('Ctrl Pts',(0.333926167874943,0.280344027827099,
-1.82622103101659));
#52261=CARTESIAN_POINT('Ctrl Pts',(-0.0518379194290401,0.432903942805994,
-1.8064939679879));
#52262=CARTESIAN_POINT('Ctrl Pts',(-0.390672104331497,0.193574773967371,
-1.78676690495921));
#52263=CARTESIAN_POINT('Ctrl Pts',(-0.375839393849523,-0.22099942133053,
-1.76703984193052));
#52264=CARTESIAN_POINT('Ctrl Pts',(-0.0207659447075708,-0.435504214242047,
-1.74731277890183));
#52265=CARTESIAN_POINT('Ctrl Pts',(0.353106227188709,-0.255756902147272,
-1.72758571587313));
#52266=CARTESIAN_POINT('Ctrl Pts',(0.407318262492253,0.155523003581003,
-1.70785865284444));
#52267=CARTESIAN_POINT('Ctrl Pts',(0.0927928177966288,0.426010512958052,
-1.68813158981575));
#52268=CARTESIAN_POINT('Ctrl Pts',(-0.305736142064931,0.310839098068842,
-1.66840452678706));
#52269=CARTESIAN_POINT('Ctrl Pts',(-0.427488064749981,-0.0857290944029937,
-1.64867746375837));
#52270=CARTESIAN_POINT('Ctrl Pts',(-0.16224324008017,-0.404688326022203,
-1.62895040072967));
#52271=CARTESIAN_POINT('Ctrl Pts',(0.249877268556016,-0.357291017298069,
-1.60922333770098));
#52272=CARTESIAN_POINT('Ctrl Pts',(0.43578868725172,0.0135550042925818,
-1.58949627467229));
#52273=CARTESIAN_POINT('Ctrl Pts',(0.227188973995266,0.372129932563031,
-1.5697692116436));
#52274=CARTESIAN_POINT('Ctrl Pts',(-0.187080554013977,0.393822782971747,
-1.55004214861491));
#52275=CARTESIAN_POINT('Ctrl Pts',(-0.431989649305596,0.0589954280701643,
-1.53031508558622));
#52276=CARTESIAN_POINT('Ctrl Pts',(-0.285826810104969,-0.329239353840106,
-1.51058802255752));
#52277=CARTESIAN_POINT('Ctrl Pts',(0.11908955159845,-0.419420071522361,
-1.49086095952883));
#52278=CARTESIAN_POINT('Ctrl Pts',(0.416196429109198,-0.129907852020033,
-1.47113389650014));
#52279=CARTESIAN_POINT('Ctrl Pts',(0.336528671296254,0.277207451204337,
-1.45140683347145));
#52280=CARTESIAN_POINT('Ctrl Pts',(-0.0477920304578935,0.433372171995315,
-1.43167977044275));
#52281=CARTESIAN_POINT('Ctrl Pts',(-0.388847524770091,0.19721338723049,
-1.41195270741406));
#52282=CARTESIAN_POINT('Ctrl Pts',(-0.377886821718897,-0.217478889995221,
-1.39222564438537));
#52283=CARTESIAN_POINT('Ctrl Pts',(-0.024832435311376,-0.435291704242668,
-1.37249858135668));
#52284=CARTESIAN_POINT('Ctrl Pts',(0.350702277941786,-0.259043297289202,
-1.35277151832799));
#52285=CARTESIAN_POINT('Ctrl Pts',(0.408752953307863,0.151712032437295,
-1.33304445529929));
#52286=CARTESIAN_POINT('Ctrl Pts',(0.0967674290926755,0.425125372439008,
-1.31331739227061));
#52287=CARTESIAN_POINT('Ctrl Pts',(-0.302819790510968,0.313680876208938,
-1.29359032924191));
#52288=CARTESIAN_POINT('Ctrl Pts',(-0.428270068639315,-0.081732893819048,
-1.27386326621322));
#52289=CARTESIAN_POINT('Ctrl Pts',(-0.166015677452493,-0.403155444542677,
-1.25413620318453));
#52290=CARTESIAN_POINT('Ctrl Pts',(0.246529518628468,-0.359609112883956,
-1.23440914015584));
#52291=CARTESIAN_POINT('Ctrl Pts',(0.435896275459704,0.00948444330145363,
-1.21468207712714));
#52292=CARTESIAN_POINT('Ctrl Pts',(0.230654504382898,0.369991915090407,
-1.19495501409845));
#52293=CARTESIAN_POINT('Ctrl Pts',(-0.183394360385883,0.395552810890066,
-1.17522795106976));
#52294=CARTESIAN_POINT('Ctrl Pts',(-0.431419832313808,0.0630273425642208,
-1.15550088804107));
#52295=CARTESIAN_POINT('Ctrl Pts',(-0.2888892143551,-0.326555568707189,
-1.13577382501238));
#52296=CARTESIAN_POINT('Ctrl Pts',(0.115167261985753,-0.420513994286857,
-1.11604676198368));
#52297=CARTESIAN_POINT('Ctrl Pts',(0.414965027541636,-0.133789175727153,
-1.09631969895499));
#52298=CARTESIAN_POINT('Ctrl Pts',(0.339102921998976,0.274052414541705,
-1.0765926359263));
#52299=CARTESIAN_POINT('Ctrl Pts',(-0.0437425472308653,0.433799616396946,
-1.05686557289761));
#52300=CARTESIAN_POINT('Ctrl Pts',(-0.386988728415595,0.200836355532715,
-1.03713850986892));
#52301=CARTESIAN_POINT('Ctrl Pts',(-0.379901444887795,-0.21394020145019,
-1.01741144684022));
#52302=CARTESIAN_POINT('Ctrl Pts',(-0.0288966783321498,-0.435040802230952,
-0.997684383811534));
#52303=CARTESIAN_POINT('Ctrl Pts',(0.348267696231286,-0.262307318590494,
-0.97795732078284));
#52304=CARTESIAN_POINT('Ctrl Pts',(0.410152012980923,0.147887943633276,
-0.958230257754149));
#52305=CARTESIAN_POINT('Ctrl Pts',(0.100733588292278,0.424203090293014,
-0.938503194725457));
#52306=CARTESIAN_POINT('Ctrl Pts',(-0.299877019548172,0.316495325038597,
-0.918776131696764));
#52307=CARTESIAN_POINT('Ctrl Pts',(-0.429014719957699,-0.0777295804954616,
-0.899049068668073));
#52308=CARTESIAN_POINT('Ctrl Pts',(-0.169773632512583,-0.401587389403433,
-0.879322005639382));
#52309=CARTESIAN_POINT('Ctrl Pts',(0.243160264380692,-0.361895846136279,
-0.859594942610688));
#52310=CARTESIAN_POINT('Ctrl Pts',(0.435965843196916,0.00541305736013395,
-0.839867879581998));
#52311=CARTESIAN_POINT('Ctrl Pts',(0.234099915768463,0.367821623972246,
-0.820140816553305));
#52312=CARTESIAN_POINT('Ctrl Pts',(-0.179692170119063,0.397248337469508,
-0.800413753524614));
#52313=CARTESIAN_POINT('Ctrl Pts',(-0.43081238492325,0.0670537591870917,
-0.780686690495921));
#52314=CARTESIAN_POINT('Ctrl Pts',(-0.291926420299019,-0.323843299692569,
-0.76095962746723));
#52315=CARTESIAN_POINT('Ctrl Pts',(0.111234926926673,-0.421571237937353,
-0.741232564438537));
#52316=CARTESIAN_POINT('Ctrl Pts',(0.413697430786003,-0.137658829667478,
-0.721505501409845));
#52317=CARTESIAN_POINT('Ctrl Pts',(0.341647594548745,0.270873473716732,
-0.701778438381154));
#52318=CARTESIAN_POINT('Ctrl Pts',(-0.0396892485711421,0.434189222773285,
-0.682051375352461));
#52319=CARTESIAN_POINT('Ctrl Pts',(-0.38509617708935,0.204441805938325,
-0.66232431232377));
#52320=CARTESIAN_POINT('Ctrl Pts',(-0.3818829312692,-0.210382852032341,
-0.642597249295076));
#52321=CARTESIAN_POINT('Ctrl Pts',(-0.0329584008492724,-0.434751953922507,
-0.622870186266387));
#52322=CARTESIAN_POINT('Ctrl Pts',(0.345802736977903,-0.265548460211983,
-0.603143123237694));
#52323=CARTESIAN_POINT('Ctrl Pts',(0.411515297270889,0.144050955341513,
-0.583416060209001));
#52324=CARTESIAN_POINT('Ctrl Pts',(0.10469096103487,0.423243807175982,-0.56368899718031));
#52325=CARTESIAN_POINT('Ctrl Pts',(-0.296908091903022,0.319282167635671,
-0.543961934151618));
#52326=CARTESIAN_POINT('Ctrl Pts',(-0.429721950601603,-0.0737194871852802,
-0.524234871122926));
#52327=CARTESIAN_POINT('Ctrl Pts',(-0.17351677911445,-0.399984306018987,
-0.504507808094234));
#52328=CARTESIAN_POINT('Ctrl Pts',(0.239769800543433,-0.364151012959176,
-0.484780745065542));
#52329=CARTESIAN_POINT('Ctrl Pts',(0.435997383966672,0.00134119893045557,
-0.465053682036851));
#52330=CARTESIAN_POINT('Ctrl Pts',(0.237524907823671,0.365619250370034,
-0.445326619008158));
#52331=CARTESIAN_POINT('Ctrl Pts',(-0.175974306186799,0.398909212950094,
-0.425599555979466));
#52332=CARTESIAN_POINT('Ctrl Pts',(-0.430167360190942,0.0710743294326753,
-0.405872492950774));
#52333=CARTESIAN_POINT('Ctrl Pts',(-0.29493816278945,-0.321102788080838,
-0.386145429922083));
#52334=CARTESIAN_POINT('Ctrl Pts',(0.107292888934788,-0.422591701473647,
-0.36641836689339));
#52335=CARTESIAN_POINT('Ctrl Pts',(0.412393750358198,-0.14151649301881,
-0.346691303864698));
#52336=CARTESIAN_POINT('Ctrl Pts',(0.344162465153559,0.267670937967541,
-0.326964240836006));
#52337=CARTESIAN_POINT('Ctrl Pts',(-0.0356324845053147,0.434540895927412,
-0.307237177807315));
#52338=CARTESIAN_POINT('Ctrl Pts',(-0.383170042620709,0.208029541269045,
-0.287510114778622));
#52339=CARTESIAN_POINT('Ctrl Pts',(-0.383831095085414,-0.206807376853309,
-0.267783051749931));
#52340=CARTESIAN_POINT('Ctrl Pts',(-0.0370172733884296,-0.434424753614554,
-0.248055988721239));
#52341=CARTESIAN_POINT('Ctrl Pts',(0.343307662735546,-0.26876726531455,
-0.228328925692547));
#52342=CARTESIAN_POINT('Ctrl Pts',(0.412842596132401,0.140202985125062,
-0.208601862663855));
#52343=CARTESIAN_POINT('Ctrl Pts',(0.108639376808644,0.422244572960195,
-0.188874799635163));
#52344=CARTESIAN_POINT('Ctrl Pts',(-0.293913601313514,0.322046975599656,
-0.169147736606471));
#52345=CARTESIAN_POINT('Ctrl Pts',(-0.430391057256783,-0.0697141083310539,
-0.149420673577779));
#52346=CARTESIAN_POINT('Ctrl Pts',(-0.177246020414515,-0.398324973365955,
-0.129693610549087));
#52347=CARTESIAN_POINT('Ctrl Pts',(0.236360778646767,-0.366415363461262,
-0.109966547520395));
#52348=CARTESIAN_POINT('Ctrl Pts',(0.435986388799776,-0.00265224273833729,
-0.0902394844917035));
#52349=CARTESIAN_POINT('Ctrl Pts',(0.240937737069026,0.363233973521747,
-0.0705124214630113));
#52350=CARTESIAN_POINT('Ctrl Pts',(-0.172256750787346,0.400829195914927,
-0.0507853584343198));
#52351=CARTESIAN_POINT('Ctrl Pts',(-0.429461421907545,0.0744849409777822,
-0.0310582954056274));
#52352=CARTESIAN_POINT('Ctrl Pts',(-0.341770662148502,-0.186390718424075,
-0.0179069200531661));
#52353=CARTESIAN_POINT('Ctrl Pts',(-0.252569643846526,-0.2698725914802,
-0.0113312323769355));
#52354=CARTESIAN_POINT('Ctrl Pts',(0.200907721869552,-0.281633609132835,
-1.97036876762307));
#52355=CARTESIAN_POINT('Ctrl Pts',(0.293996110671544,-0.215227557013203,
-1.96379307994683));
#52356=CARTESIAN_POINT('Ctrl Pts',(0.407643094888337,0.0159382890418302,
-1.95064170459437));
#52357=CARTESIAN_POINT('Ctrl Pts',(0.209426004391725,0.35053590514097,-1.93091464156568));
#52358=CARTESIAN_POINT('Ctrl Pts',(-0.178559227689997,0.366807474059788,
-1.91118757853699));
#52359=CARTESIAN_POINT('Ctrl Pts',(-0.404804256442896,0.0515105071119071,
-1.8914605155083));
#52360=CARTESIAN_POINT('Ctrl Pts',(-0.264636868873115,-0.310673813338168,
-1.8717334524796));
#52361=CARTESIAN_POINT('Ctrl Pts',(0.115126822966393,-0.391477866571069,
-1.85200638945091));
#52362=CARTESIAN_POINT('Ctrl Pts',(0.390655040059497,-0.117954006630858,
-1.83227932642222));
#52363=CARTESIAN_POINT('Ctrl Pts',(0.312537728174058,0.262387599396106,
-1.81255226339353));
#52364=CARTESIAN_POINT('Ctrl Pts',(-0.0485176279377133,0.405175837710473,
-1.79282520036483));
#52365=CARTESIAN_POINT('Ctrl Pts',(-0.365649007760519,0.18117603802235,
-1.77309813733615));
#52366=CARTESIAN_POINT('Ctrl Pts',(-0.351766353201873,-0.206844098232797,
-1.75337107430745));
#52367=CARTESIAN_POINT('Ctrl Pts',(-0.019435856805095,-0.407609558111698,
-1.73364401127876));
#52368=CARTESIAN_POINT('Ctrl Pts',(0.330489277770536,-0.239375313622856,
-1.71391694825007));
#52369=CARTESIAN_POINT('Ctrl Pts',(0.381228956129035,0.145561536932969,
-1.69418988522138));
#52370=CARTESIAN_POINT('Ctrl Pts',(0.086849307586724,0.398723941718872,
-1.67446282219269));
#52371=CARTESIAN_POINT('Ctrl Pts',(-0.286153313080456,0.290929417590573,
-1.65473575916399));
#52372=CARTESIAN_POINT('Ctrl Pts',(-0.400106854244859,-0.0802380255900348,
-1.6350086961353));
#52373=CARTESIAN_POINT('Ctrl Pts',(-0.151851332852848,-0.378767470780876,
-1.61528163310661));
#52374=CARTESIAN_POINT('Ctrl Pts',(0.233872278814892,-0.334406026200248,
-1.59555457007792));
#52375=CARTESIAN_POINT('Ctrl Pts',(0.407875810225857,0.0126867872438813,
-1.57582750704923));
#52376=CARTESIAN_POINT('Ctrl Pts',(0.212637201362629,0.348294488116823,
-1.55610044402053));
#52377=CARTESIAN_POINT('Ctrl Pts',(-0.175097781971285,0.368597881012041,
-1.53637338099184));
#52378=CARTESIAN_POINT('Ctrl Pts',(-0.404320105991941,0.055216688105167,
-1.51664631796315));
#52379=CARTESIAN_POINT('Ctrl Pts',(-0.267519201774267,-0.308151111155861,
-1.49691925493446));
#52380=CARTESIAN_POINT('Ctrl Pts',(0.111461698682407,-0.392555627306488,
-1.47719219190577));
#52381=CARTESIAN_POINT('Ctrl Pts',(0.389538463714108,-0.121587071779045,
-1.45746512887707));
#52382=CARTESIAN_POINT('Ctrl Pts',(0.314973537598751,0.259451924908058,
-1.43773806584838));
#52383=CARTESIAN_POINT('Ctrl Pts',(-0.0447308838333691,0.405614076163082,
-1.41801100281969));
#52384=CARTESIAN_POINT('Ctrl Pts',(-0.363941295080726,0.184581592999357,
-1.398283939791));
#52385=CARTESIAN_POINT('Ctrl Pts',(-0.353682640442751,-0.203549061870403,
-1.37855687676231));
#52386=CARTESIAN_POINT('Ctrl Pts',(-0.0232418829786129,-0.407410659676025,
-1.35882981373361));
#52387=CARTESIAN_POINT('Ctrl Pts',(0.3282393048467,-0.242451210543656,-1.33910275070492));
#52388=CARTESIAN_POINT('Ctrl Pts',(0.382571752984389,0.141994663839521,
-1.31937568767623));
#52389=CARTESIAN_POINT('Ctrl Pts',(0.090569339451093,0.397895495692323,
-1.29964862464754));
#52390=CARTESIAN_POINT('Ctrl Pts',(-0.283423757936476,0.293589175852503,
-1.27992156161884));
#52391=CARTESIAN_POINT('Ctrl Pts',(-0.400838769687577,-0.0764977872619564,
-1.26019449859016));
#52392=CARTESIAN_POINT('Ctrl Pts',(-0.155382140317049,-0.377332772511435,
-1.24046743556146));
#52393=CARTESIAN_POINT('Ctrl Pts',(0.230738956968601,-0.336575644510529,
-1.22074037253277));
#52394=CARTESIAN_POINT('Ctrl Pts',(0.407976507258125,0.00887695139706183,
-1.20101330950408));
#52395=CARTESIAN_POINT('Ctrl Pts',(0.215880759665235,0.34629341366392,-1.18128624647539));
#52396=CARTESIAN_POINT('Ctrl Pts',(-0.171647694218456,0.370217098214186,
-1.16155918344669));
#52397=CARTESIAN_POINT('Ctrl Pts',(-0.403786786578187,0.0589903528172908,
-1.14183212041801));
#52398=CARTESIAN_POINT('Ctrl Pts',(-0.270385454734247,-0.305639226227264,
-1.12210505738931));
#52399=CARTESIAN_POINT('Ctrl Pts',(0.107790637224138,-0.393579482782653,
-1.10237799436062));
#52400=CARTESIAN_POINT('Ctrl Pts',(0.388385935145159,-0.125219791255482,
-1.08265093133193));
#52401=CARTESIAN_POINT('Ctrl Pts',(0.317382903931133,0.256498972771602,
-1.06292386830324));
#52402=CARTESIAN_POINT('Ctrl Pts',(-0.0409407756902769,0.406014142150892,
-1.04319680527454));
#52403=CARTESIAN_POINT('Ctrl Pts',(-0.362201557241462,0.187972505097171,
-1.02346974224585));
#52404=CARTESIAN_POINT('Ctrl Pts',(-0.355568224170259,-0.200237031293051,
-1.00374267921716));
#52405=CARTESIAN_POINT('Ctrl Pts',(-0.0270458055299464,-0.407175828290289,
-0.984015616188469));
#52406=CARTESIAN_POINT('Ctrl Pts',(0.32596066151157,-0.245506166699711,
-0.964288553159776));
#52407=CARTESIAN_POINT('Ctrl Pts',(0.38388120092188,0.138415513290315,-0.944561490131084));
#52408=CARTESIAN_POINT('Ctrl Pts',(0.094281460587657,0.397032287012157,
-0.924834427102393));
#52409=CARTESIAN_POINT('Ctrl Pts',(-0.280669475583878,0.296223355284686,
-0.9051073640737));
#52410=CARTESIAN_POINT('Ctrl Pts',(-0.401535725043939,-0.072750891775193,
-0.885380301045009));
#52411=CARTESIAN_POINT('Ctrl Pts',(-0.15889939308144,-0.375865153504546,
-0.865653238016317));
#52412=CARTESIAN_POINT('Ctrl Pts',(0.227585508183973,-0.338715909288726,
-0.845926174987624));
#52413=CARTESIAN_POINT('Ctrl Pts',(0.408041619084134,0.00506634343926735,
-0.826199111958933));
#52414=CARTESIAN_POINT('Ctrl Pts',(0.219105487616094,0.344262132737772,
-0.806472048930241));
#52415=CARTESIAN_POINT('Ctrl Pts',(-0.168182634434063,0.371804023936628,
-0.786744985901549));
#52416=CARTESIAN_POINT('Ctrl Pts',(-0.403218247045515,0.0627588718045951,
-0.767017922872856));
#52417=CARTESIAN_POINT('Ctrl Pts',(-0.273228123374893,-0.303100681849563,
-0.747290859844165));
#52418=CARTESIAN_POINT('Ctrl Pts',(0.104110173744426,-0.394569008493547,
-0.727563796815473));
#52419=CARTESIAN_POINT('Ctrl Pts',(0.387199529740732,-0.128841588430066,
-0.70783673378678));
#52420=CARTESIAN_POINT('Ctrl Pts',(0.31976458663277,0.253523647567951,-0.68810967075809));
#52421=CARTESIAN_POINT('Ctrl Pts',(-0.0371470964983091,0.406378793692034,
-0.668382607729396));
#52422=CARTESIAN_POINT('Ctrl Pts',(-0.360430226483763,0.191347021344234,
-0.648655544700705));
#52423=CARTESIAN_POINT('Ctrl Pts',(-0.357422793568019,-0.196907535097976,
-0.628928481672013));
#52424=CARTESIAN_POINT('Ctrl Pts',(-0.030847369019425,-0.406905481121384,
-0.609201418643321));
#52425=CARTESIAN_POINT('Ctrl Pts',(0.323653586357811,-0.248539708651565,
-0.589474355614629));
#52426=CARTESIAN_POINT('Ctrl Pts',(0.385157164939774,0.134824289483658,
-0.569747292585937));
#52427=CARTESIAN_POINT('Ctrl Pts',(0.0979853580521132,0.396134447325076,
-0.550020229557245));
#52428=CARTESIAN_POINT('Ctrl Pts',(-0.277890711921139,0.298831696702225,
-0.530293166528553));
#52429=CARTESIAN_POINT('Ctrl Pts',(-0.402197656572538,-0.0689976505694917,
-0.510566103499861));
#52430=CARTESIAN_POINT('Ctrl Pts',(-0.16240278589014,-0.374364749860721,
-0.49083904047117));
#52431=CARTESIAN_POINT('Ctrl Pts',(0.224412208313835,-0.340826629511603,
-0.471111977442478));
#52432=CARTESIAN_POINT('Ctrl Pts',(0.408071139623321,0.001255293256657,
-0.451384914413786));
#52433=CARTESIAN_POINT('Ctrl Pts',(0.222311104123364,0.342200824255702,
-0.431657851385094));
#52434=CARTESIAN_POINT('Ctrl Pts',(-0.164702904904495,0.373358518011727,
-0.411930788356401));
#52435=CARTESIAN_POINT('Ctrl Pts',(-0.402614537052571,0.0665219188832822,
-0.39220372532771));
#52436=CARTESIAN_POINT('Ctrl Pts',(-0.276046959531984,-0.300535703852733,
-0.372476662299018));
#52437=CARTESIAN_POINT('Ctrl Pts',(0.100420628818372,-0.395524109908172,
-0.352749599270327));
#52438=CARTESIAN_POINT('Ctrl Pts',(0.385979351873978,-0.132452163029709,
-0.333022536241633));
#52439=CARTESIAN_POINT('Ctrl Pts',(0.322118376245852,0.250526238728093,
-0.313295473212943));
#52440=CARTESIAN_POINT('Ctrl Pts',(-0.0333501738643609,0.406707941687084,
-0.29356841018425));
#52441=CARTESIAN_POINT('Ctrl Pts',(-0.358627463631072,0.194704957191817,
-0.273841347155559));
#52442=CARTESIAN_POINT('Ctrl Pts',(-0.359246174757656,-0.193561074122159,
-0.254114284126866));
#52443=CARTESIAN_POINT('Ctrl Pts',(-0.0346462650760267,-0.406599238452365,
-0.234387221098175));
#52444=CARTESIAN_POINT('Ctrl Pts',(0.321318325122388,-0.251552344769883,
-0.214660158069482));
#52445=CARTESIAN_POINT('Ctrl Pts',(0.386399448446409,0.131222787160003,
-0.194933095040791));
#52446=CARTESIAN_POINT('Ctrl Pts',(0.101680872254175,0.395199215463184,
-0.175206032012099));
#52447=CARTESIAN_POINT('Ctrl Pts',(-0.275088022656505,0.301419414835849,
-0.155478968983407));
#52448=CARTESIAN_POINT('Ctrl Pts',(-0.402823906007397,-0.0652488218522259,
-0.135751905954715));
#52449=CARTESIAN_POINT('Ctrl Pts',(-0.165893164051134,-0.372811699792905,
-0.116024842926023));
#52450=CARTESIAN_POINT('Ctrl Pts',(0.22122153905404,-0.342945945186129,
-0.0962977798973308));
#52451=CARTESIAN_POINT('Ctrl Pts',(0.408060848712296,-0.00248236286865586,
-0.076570716868639));
#52452=CARTESIAN_POINT('Ctrl Pts',(0.22550533686582,0.339968327737163,-0.056843653839947));
#52453=CARTESIAN_POINT('Ctrl Pts',(-0.161223464145778,0.375155523373064,
-0.0371165908112554));
#52454=CARTESIAN_POINT('Ctrl Pts',(-0.401953815106974,0.0697140759723039,
-0.017389527782563));
#52455=CARTESIAN_POINT('Ctrl Pts',(-0.319879771580044,-0.174452131319065,
-0.00423815243010174));
#52456=CARTESIAN_POINT('Ctrl Pts',(-0.236392203689429,-0.252586873243357,
0.00233753524612886));
#52457=CARTESIAN_POINT('Ctrl Pts',(0.187158653173899,-0.26236008493506,
-1.9567));
#52458=CARTESIAN_POINT('Ctrl Pts',(0.273876561834578,-0.200498514052405,
-1.95012431232377));
#52459=CARTESIAN_POINT('Ctrl Pts',(0.379746143677233,0.0148475562970276,
-1.93697293697131));
#52460=CARTESIAN_POINT('Ctrl Pts',(0.195093989204632,0.326547069892489,
-1.91724587394262));
#52461=CARTESIAN_POINT('Ctrl Pts',(-0.166339572492541,0.341705098143136,
-1.89751881091393));
#52462=CARTESIAN_POINT('Ctrl Pts',(-0.377101580416633,0.0479853986977567,
-1.87779174788523));
#52463=CARTESIAN_POINT('Ctrl Pts',(-0.246526512259235,-0.289412930173605,
-1.85806468485654));
#52464=CARTESIAN_POINT('Ctrl Pts',(0.107248148204929,-0.364687178636194,
-1.83833762182785));
#52465=CARTESIAN_POINT('Ctrl Pts',(0.363920662047043,-0.109881854276511,
-1.81861055879916));
#52466=CARTESIAN_POINT('Ctrl Pts',(0.291149288473172,0.244431170965113,
-1.79888349577046));
#52467=CARTESIAN_POINT('Ctrl Pts',(-0.0451973364463865,0.377447732614952,
-1.77915643274177));
#52468=CARTESIAN_POINT('Ctrl Pts',(-0.34062591118954,0.168777302077329,
-1.75942936971308));
#52469=CARTESIAN_POINT('Ctrl Pts',(-0.327693312554222,-0.192688775135064,
-1.73970230668439));
#52470=CARTESIAN_POINT('Ctrl Pts',(-0.0181057689026194,-0.379714901981348,
-1.7199752436557));
#52471=CARTESIAN_POINT('Ctrl Pts',(0.307872328352363,-0.22299372509844,
-1.70024818062701));
#52472=CARTESIAN_POINT('Ctrl Pts',(0.355139649765817,0.135600070284936,
-1.68052111759831));
#52473=CARTESIAN_POINT('Ctrl Pts',(0.0809057973768194,0.371437370479693,
-1.66079405456962));
#52474=CARTESIAN_POINT('Ctrl Pts',(-0.26657048409598,0.271019737112303,
-1.64106699154093));
#52475=CARTESIAN_POINT('Ctrl Pts',(-0.372725643739736,-0.0747469567770755,
-1.62133992851224));
#52476=CARTESIAN_POINT('Ctrl Pts',(-0.141459425625526,-0.352846615539549,
-1.60161286548355));
#52477=CARTESIAN_POINT('Ctrl Pts',(0.217867289073768,-0.311521035102426,
-1.58188580245485));
#52478=CARTESIAN_POINT('Ctrl Pts',(0.379962933199995,0.0118185701951804,
-1.56215873942616));
#52479=CARTESIAN_POINT('Ctrl Pts',(0.198085428729991,0.324459043670616,
-1.54243167639747));
#52480=CARTESIAN_POINT('Ctrl Pts',(-0.163115009928593,0.343372979052334,
-1.52270461336878));
#52481=CARTESIAN_POINT('Ctrl Pts',(-0.376650562678285,0.0514379481401701,
-1.50297755034009));
#52482=CARTESIAN_POINT('Ctrl Pts',(-0.249211593443565,-0.287062868471616,
-1.48325048731139));
#52483=CARTESIAN_POINT('Ctrl Pts',(0.103833845766363,-0.365691183090615,
-1.4635234242827));
#52484=CARTESIAN_POINT('Ctrl Pts',(0.362880498319019,-0.113266291538057,
-1.44379636125401));
#52485=CARTESIAN_POINT('Ctrl Pts',(0.293418403901249,0.24169639861178,-1.42406929822532));
#52486=CARTESIAN_POINT('Ctrl Pts',(-0.0416697372088447,0.377855980330849,
-1.40434223519663));
#52487=CARTESIAN_POINT('Ctrl Pts',(-0.339035065391361,0.171949798768224,
-1.38461517216793));
#52488=CARTESIAN_POINT('Ctrl Pts',(-0.329478459166605,-0.189619233745584,
-1.36488810913924));
#52489=CARTESIAN_POINT('Ctrl Pts',(-0.0216513306458494,-0.379529615109383,
-1.34516104611055));
#52490=CARTESIAN_POINT('Ctrl Pts',(0.305776331751614,-0.225859123798109,
-1.32543398308186));
#52491=CARTESIAN_POINT('Ctrl Pts',(0.356390552660915,0.132277295241747,
-1.30570692005317));
#52492=CARTESIAN_POINT('Ctrl Pts',(0.0843712498095106,0.370665618945638,
-1.28597985702447));
#52493=CARTESIAN_POINT('Ctrl Pts',(-0.264027725361984,0.273497475496068,
-1.26625279399578));
#52494=CARTESIAN_POINT('Ctrl Pts',(-0.37340747073584,-0.0712626807048641,
-1.24652573096709));
#52495=CARTESIAN_POINT('Ctrl Pts',(-0.144748603181605,-0.351510100480195,
-1.2267986679384));
#52496=CARTESIAN_POINT('Ctrl Pts',(0.214948395308735,-0.313542176137101,
-1.20707160490971));
#52497=CARTESIAN_POINT('Ctrl Pts',(0.380056739056546,0.00826945949266903,
-1.18734454188101));
#52498=CARTESIAN_POINT('Ctrl Pts',(0.201107014947573,0.322594912237434,
-1.16761747885232));
#52499=CARTESIAN_POINT('Ctrl Pts',(-0.15990102805103,0.344881385538304,
-1.14789041582363));
#52500=CARTESIAN_POINT('Ctrl Pts',(-0.376153740842564,0.0549533630703619,
-1.12816335279494));
#52501=CARTESIAN_POINT('Ctrl Pts',(-0.251881695113395,-0.28472288374734,
-1.10843628976625));
#52502=CARTESIAN_POINT('Ctrl Pts',(0.100414012462523,-0.366644971278448,
-1.08870922673756));
#52503=CARTESIAN_POINT('Ctrl Pts',(0.361806842748681,-0.116650406783812,
-1.06898216370886));
#52504=CARTESIAN_POINT('Ctrl Pts',(0.295662885863291,0.2389455310015,-1.04925510068017));
#52505=CARTESIAN_POINT('Ctrl Pts',(-0.0381390041496891,0.378228667904838,
-1.02952803765148));
#52506=CARTESIAN_POINT('Ctrl Pts',(-0.337414386067329,0.175108654661627,
-1.00980097462279));
#52507=CARTESIAN_POINT('Ctrl Pts',(-0.331235003452725,-0.186533861135912,
-0.990073911594096));
#52508=CARTESIAN_POINT('Ctrl Pts',(-0.0251949327277424,-0.379310854349625,
-0.970346848565404));
#52509=CARTESIAN_POINT('Ctrl Pts',(0.303653626791853,-0.228705014808928,
-0.950619785536712));
#52510=CARTESIAN_POINT('Ctrl Pts',(0.357610388862838,0.128943082947354,
-0.930892722508019));
#52511=CARTESIAN_POINT('Ctrl Pts',(0.0878293328830358,0.3698614837313,-0.911165659479328));
#52512=CARTESIAN_POINT('Ctrl Pts',(-0.261461931619583,0.275951385530775,
-0.891438596450636));
#52513=CARTESIAN_POINT('Ctrl Pts',(-0.374056730130178,-0.0677722030549249,
-0.871711533421944));
#52514=CARTESIAN_POINT('Ctrl Pts',(-0.148025153650298,-0.350142917605659,
-0.851984470393253));
#52515=CARTESIAN_POINT('Ctrl Pts',(0.212010751987255,-0.315535972441172,
-0.832257407364559));
#52516=CARTESIAN_POINT('Ctrl Pts',(0.380117394971352,0.00471962951840088,
-0.81253034433587));
#52517=CARTESIAN_POINT('Ctrl Pts',(0.204111059463726,0.320702641503297,
-0.792803281307175));
#52518=CARTESIAN_POINT('Ctrl Pts',(-0.156673098749063,0.346359710403747,
-0.773076218278485));
#52519=CARTESIAN_POINT('Ctrl Pts',(-0.37562410916778,0.0584639844220986,
-0.753349155249791));
#52520=CARTESIAN_POINT('Ctrl Pts',(-0.254529826450768,-0.282358064006557,
-0.733622092221101));
#52521=CARTESIAN_POINT('Ctrl Pts',(0.0969854205621785,-0.36756677904974,
-0.713895029192408));
#52522=CARTESIAN_POINT('Ctrl Pts',(0.36070162869546,-0.120024347192654,
-0.694167966163718));
#52523=CARTESIAN_POINT('Ctrl Pts',(0.297881578716796,0.236173821419171,
-0.674440903135024));
#52524=CARTESIAN_POINT('Ctrl Pts',(-0.0346049444254762,0.378568364610783,
-0.654713840106333));
#52525=CARTESIAN_POINT('Ctrl Pts',(-0.335764275878176,0.178252236750144,
-0.63498677707764));
#52526=CARTESIAN_POINT('Ctrl Pts',(-0.332962655866839,-0.18343221816361,
-0.615259714048949));
#52527=CARTESIAN_POINT('Ctrl Pts',(-0.0287363371895775,-0.37905900832026,
-0.595532651020257));
#52528=CARTESIAN_POINT('Ctrl Pts',(0.30150443573772,-0.231530957091147,
-0.575805587991564));
#52529=CARTESIAN_POINT('Ctrl Pts',(0.358799032608658,0.125597623625804,
-0.556078524962874));
#52530=CARTESIAN_POINT('Ctrl Pts',(0.0912797550693568,0.36902508747417,
-0.53635146193418));
#52531=CARTESIAN_POINT('Ctrl Pts',(-0.258873331939256,0.278381225768779,
-0.516624398905489));
#52532=CARTESIAN_POINT('Ctrl Pts',(-0.374673362543473,-0.0642758139537041,
-0.496897335876797));
#52533=CARTESIAN_POINT('Ctrl Pts',(-0.151288792665831,-0.348745193702454,
-0.477170272848105));
#52534=CARTESIAN_POINT('Ctrl Pts',(0.209054616084237,-0.317502246064031,
-0.457443209819413));
#52535=CARTESIAN_POINT('Ctrl Pts',(0.380144895279971,0.00116938758285907,
-0.437716146790722));
#52536=CARTESIAN_POINT('Ctrl Pts',(0.207097300423056,0.318782398141369,
-0.41798908376203));
#52537=CARTESIAN_POINT('Ctrl Pts',(-0.15343150362219,0.34780782307336,-0.398262020733337));
#52538=CARTESIAN_POINT('Ctrl Pts',(-0.3750617139142,0.0619695083338889,
-0.378534957704646));
#52539=CARTESIAN_POINT('Ctrl Pts',(-0.257155756274518,-0.279968619624628,
-0.358807894675954));
#52540=CARTESIAN_POINT('Ctrl Pts',(0.093548368701956,-0.368456518342696,
-0.339080831647262));
#52541=CARTESIAN_POINT('Ctrl Pts',(0.359564953389757,-0.12338783304061,
-0.319353768618569));
#52542=CARTESIAN_POINT('Ctrl Pts',(0.300074287338146,0.233381539488646,
-0.299626705589878));
#52543=CARTESIAN_POINT('Ctrl Pts',(-0.0310678632234075,0.378874987446754,
-0.279899642561186));
#52544=CARTESIAN_POINT('Ctrl Pts',(-0.334084884641434,0.18138037311459,
-0.260172579532494));
#52545=CARTESIAN_POINT('Ctrl Pts',(-0.334661254429897,-0.180314771391009,
-0.240445516503802));
#52546=CARTESIAN_POINT('Ctrl Pts',(-0.032275256763624,-0.378773723290174,
-0.22071845347511));
#52547=CARTESIAN_POINT('Ctrl Pts',(0.299328987509231,-0.234337424225216,
-0.200991390446418));
#52548=CARTESIAN_POINT('Ctrl Pts',(0.359956300760417,0.122242589194944,
-0.181264327417726));
#52549=CARTESIAN_POINT('Ctrl Pts',(0.0947223676997066,0.368153857966175,
-0.161537264389034));
#52550=CARTESIAN_POINT('Ctrl Pts',(-0.256262443999497,0.280791854072041,
-0.141810201360342));
#52551=CARTESIAN_POINT('Ctrl Pts',(-0.37525675475801,-0.0607835353733978,
-0.122083138331651));
#52552=CARTESIAN_POINT('Ctrl Pts',(-0.154540307687754,-0.347298426219855,
-0.102356075302959));
#52553=CARTESIAN_POINT('Ctrl Pts',(0.206082299461314,-0.319476526910996,
-0.0826290122742663));
#52554=CARTESIAN_POINT('Ctrl Pts',(0.380135308624816,-0.00231248299897462,
-0.0629019492455747));
#52555=CARTESIAN_POINT('Ctrl Pts',(0.210072936662614,0.316702681952579,
-0.0431748862168826));
#52556=CARTESIAN_POINT('Ctrl Pts',(-0.15019017750421,0.3494818508312,-0.0234478231881909));
#52557=CARTESIAN_POINT('Ctrl Pts',(-0.374446208306403,0.0649432109668261,
-0.00372076015949865));
#52558=CARTESIAN_POINT('Ctrl Pts',(-0.297988881011587,-0.162513544214055,
0.00943061519296265));
#52559=CARTESIAN_POINT('Ctrl Pts',(-0.220214763532331,-0.235301155006514,
0.0160063028691932));
#52560=CARTESIAN_POINT('Ctrl Pts',(-0.268747084003623,-0.287158309717044,
-0.0249999999999999));
#52561=CARTESIAN_POINT('Ctrl Pts',(-0.347093960934679,-0.213834662086023,
-0.030427882598834));
#52562=CARTESIAN_POINT('Ctrl Pts',(-0.392557762364837,-0.106467699857906,
-0.035855765197668));
#52563=CARTESIAN_POINT('Ctrl Pts',(-0.393507845663966,0.000361442601786235,
-0.041283647796502));
#52564=CARTESIAN_POINT('Origin',(0.,0.,-0.025));
#52565=CARTESIAN_POINT('',(-0.4183,5.12269756083338E-17,0.));
#52566=CARTESIAN_POINT('Origin',(-0.4183,-5.12269756083338E-17,-0.025));
#52567=CARTESIAN_POINT('Origin',(0.,0.,0.));
#52568=CARTESIAN_POINT('Origin',(0.,0.,-0.025));
#52569=CARTESIAN_POINT('Origin',(0.,0.,-0.975));
#52570=CARTESIAN_POINT('Origin',(0.62,0.,0.));
#52571=CARTESIAN_POINT('',(-0.62,-7.59281015471359E-17,8.67361737988404E-18));
#52572=CARTESIAN_POINT('Origin',(0.,0.,0.));
#52573=CARTESIAN_POINT('Origin',(0.,0.,0.32));
#52574=CARTESIAN_POINT('',(0.173205080756888,0.3,0.32));
#52575=CARTESIAN_POINT('',(0.346410161513775,0.,0.32));
#52576=CARTESIAN_POINT('',(0.346410161513775,0.,0.32));
#52577=CARTESIAN_POINT('Origin',(0.,0.,0.32));
#52578=CARTESIAN_POINT('Origin',(0.,0.,0.32));
#52579=CARTESIAN_POINT('',(0.173205080756888,-0.3,0.32));
#52580=CARTESIAN_POINT('',(0.173205080756888,-0.3,0.32));
#52581=CARTESIAN_POINT('Origin',(0.,0.,0.32));
#52582=CARTESIAN_POINT('Origin',(0.,0.,0.32));
#52583=CARTESIAN_POINT('',(-0.173205080756888,-0.3,0.32));
#52584=CARTESIAN_POINT('',(-0.173205080756888,-0.3,0.32));
#52585=CARTESIAN_POINT('Origin',(0.,0.,0.32));
#52586=CARTESIAN_POINT('Origin',(0.,0.,0.32));
#52587=CARTESIAN_POINT('',(-0.346410161513775,5.55111512312578E-17,0.32));
#52588=CARTESIAN_POINT('',(-0.346410161513775,4.24230095489963E-17,0.32));
#52589=CARTESIAN_POINT('Origin',(0.,0.,0.32));
#52590=CARTESIAN_POINT('Origin',(0.,0.,0.32));
#52591=CARTESIAN_POINT('',(-0.173205080756888,0.3,0.32));
#52592=CARTESIAN_POINT('',(-0.173205080756888,0.3,0.32));
#52593=CARTESIAN_POINT('Origin',(0.,0.,0.32));
#52594=CARTESIAN_POINT('Origin',(0.,0.,0.32));
#52595=CARTESIAN_POINT('',(0.173205080756888,0.3,0.32));
#52596=CARTESIAN_POINT('Origin',(0.,0.,0.32));
#52597=CARTESIAN_POINT('Origin',(0.,0.,0.216076951545867));
#52598=CARTESIAN_POINT('',(0.,0.,0.112153903091735));
#52599=CARTESIAN_POINT('',(-0.173205080756888,-2.12115047744981E-17,0.216076951545867));
#52600=CARTESIAN_POINT('Origin',(0.173205080756888,0.3,0.8));
#52601=CARTESIAN_POINT('',(0.173205080756888,0.3,0.8));
#52602=CARTESIAN_POINT('',(0.346410161513775,0.,0.8));
#52603=CARTESIAN_POINT('',(0.21650635094611,0.225,0.8));
#52604=CARTESIAN_POINT('',(0.173205080756888,0.3,0.8));
#52605=CARTESIAN_POINT('',(0.346410161513775,0.,0.8));
#52606=CARTESIAN_POINT('Origin',(-0.173205080756888,0.3,0.8));
#52607=CARTESIAN_POINT('',(-0.173205080756888,0.3,0.8));
#52608=CARTESIAN_POINT('',(-0.0866025403784438,0.3,0.8));
#52609=CARTESIAN_POINT('',(-0.173205080756888,0.3,0.8));
#52610=CARTESIAN_POINT('Origin',(-0.346410161513775,5.55111512312578E-17,
0.8));
#52611=CARTESIAN_POINT('',(-0.346410161513775,4.24230095489963E-17,0.8));
#52612=CARTESIAN_POINT('',(-0.303108891324554,0.0750000000000001,0.8));
#52613=CARTESIAN_POINT('',(-0.346410161513775,4.24230095489963E-17,0.8));
#52614=CARTESIAN_POINT('Origin',(-0.173205080756888,-0.3,0.8));
#52615=CARTESIAN_POINT('',(-0.173205080756888,-0.3,0.8));
#52616=CARTESIAN_POINT('',(-0.21650635094611,-0.225,0.8));
#52617=CARTESIAN_POINT('',(-0.173205080756888,-0.3,0.8));
#52618=CARTESIAN_POINT('Origin',(0.173205080756888,-0.3,0.8));
#52619=CARTESIAN_POINT('',(0.173205080756888,-0.3,0.8));
#52620=CARTESIAN_POINT('',(0.0866025403784439,-0.3,0.8));
#52621=CARTESIAN_POINT('',(0.173205080756888,-0.3,0.8));
#52622=CARTESIAN_POINT('Origin',(0.346410161513775,0.,0.8));
#52623=CARTESIAN_POINT('',(0.303108891324554,-0.075,0.8));
#52624=CARTESIAN_POINT('Origin',(0.635148348882184,-0.269604478657599,0.75));
#52625=CARTESIAN_POINT('',(0.606534182632106,-0.23370127363539,0.0499999999999999));
#52626=CARTESIAN_POINT('',(0.606534182632106,-0.23370127363539,0.75));
#52627=CARTESIAN_POINT('',(0.606534182632106,-0.23370127363539,0.39));
#52628=CARTESIAN_POINT('',(0.592006351095122,-0.215472690295171,0.0499999999999999));
#52629=CARTESIAN_POINT('',(0.635148348882184,-0.269604478657599,0.0499999999999999));
#52630=CARTESIAN_POINT('',(0.592006351095122,-0.215472690295171,0.75));
#52631=CARTESIAN_POINT('',(0.592006351095122,-0.215472690295171,0.75));
#52632=CARTESIAN_POINT('',(0.635148348882184,-0.269604478657599,0.75));
#52633=CARTESIAN_POINT('Origin',(0.625928316354808,-0.235670477458144,0.75));
#52634=CARTESIAN_POINT('',(0.614852423227828,-0.210847095429052,0.75));
#52635=CARTESIAN_POINT('Origin',(0.,0.,0.75));
#52636=CARTESIAN_POINT('',(0.592006351095122,-0.215472690295171,0.75));
#52637=CARTESIAN_POINT('Origin',(0.592006351095122,-0.215472690295171,0.75));
#52638=CARTESIAN_POINT('',(0.614852423227828,-0.210847095429052,0.0499999999999999));
#52639=CARTESIAN_POINT('',(0.614852423227828,-0.210847095429052,0.39));
#52640=CARTESIAN_POINT('',(0.592006351095122,-0.215472690295171,0.0499999999999999));
#52641=CARTESIAN_POINT('Origin',(0.625928316354808,-0.235670477458144,0.0499999999999999));
#52642=CARTESIAN_POINT('Origin',(0.,0.,0.0499999999999999));
#52643=CARTESIAN_POINT('Origin',(0.504634054117228,-0.470578868443124,0.75));
#52644=CARTESIAN_POINT('',(0.490025152569635,-0.427054270379195,0.0499999999999999));
#52645=CARTESIAN_POINT('',(0.490025152569635,-0.427054270379195,0.75));
#52646=CARTESIAN_POINT('',(0.490025152569635,-0.427054270379195,0.39));
#52647=CARTESIAN_POINT('',(0.482607999164956,-0.40495619410252,0.0499999999999999));
#52648=CARTESIAN_POINT('',(0.504634054117228,-0.470578868443124,0.0499999999999999));
#52649=CARTESIAN_POINT('',(0.482607999164956,-0.40495619410252,0.75));
#52650=CARTESIAN_POINT('',(0.482607999164956,-0.40495619410252,0.75));
#52651=CARTESIAN_POINT('',(0.504634054117228,-0.470578868443124,0.75));
#52652=CARTESIAN_POINT('Origin',(0.516833250548794,-0.437767531272822,0.75));
#52653=CARTESIAN_POINT('',(0.505658331181079,-0.408423373605339,0.75));
#52654=CARTESIAN_POINT('Origin',(0.,0.,0.75));
#52655=CARTESIAN_POINT('',(0.482607999164956,-0.40495619410252,0.75));
#52656=CARTESIAN_POINT('Origin',(0.482607999164956,-0.40495619410252,0.75));
#52657=CARTESIAN_POINT('',(0.505658331181079,-0.408423373605339,0.0499999999999999));
#52658=CARTESIAN_POINT('',(0.505658331181079,-0.408423373605339,0.39));
#52659=CARTESIAN_POINT('',(0.482607999164956,-0.40495619410252,0.0499999999999999));
#52660=CARTESIAN_POINT('Origin',(0.516833250548794,-0.437767531272822,0.0499999999999999));
#52661=CARTESIAN_POINT('Origin',(0.,0.,0.0499999999999999));
#52662=CARTESIAN_POINT('Origin',(0.313253444820287,-0.614794501689974,0.75));
#52663=CARTESIAN_POINT('',(0.314411857106244,-0.568898219465488,0.0499999999999999));
#52664=CARTESIAN_POINT('',(0.314411857106244,-0.568898219465488,0.75));
#52665=CARTESIAN_POINT('',(0.314411857106244,-0.568898219465488,0.39));
#52666=CARTESIAN_POINT('',(0.315,-0.545596004384196,0.0499999999999999));
#52667=CARTESIAN_POINT('',(0.313253444820287,-0.614794501689974,0.0499999999999999));
#52668=CARTESIAN_POINT('',(0.315,-0.545596004384196,0.75));
#52669=CARTESIAN_POINT('',(0.315,-0.545596004384196,0.75));
#52670=CARTESIAN_POINT('',(0.313253444820287,-0.614794501689974,0.75));
#52671=CARTESIAN_POINT('Origin',(0.344527189490328,-0.580195253037085,0.75));
#52672=CARTESIAN_POINT('',(0.335474381671726,-0.556737765237794,0.75));
#52673=CARTESIAN_POINT('Origin',(0.,0.,0.75));
#52674=CARTESIAN_POINT('',(0.315,-0.545596004384196,0.75));
#52675=CARTESIAN_POINT('Origin',(0.315,-0.545596004384196,0.75));
#52676=CARTESIAN_POINT('',(0.335474381671726,-0.556737765237794,0.0499999999999999));
#52677=CARTESIAN_POINT('',(0.335474381671726,-0.556737765237794,0.39));
#52678=CARTESIAN_POINT('',(0.315,-0.545596004384196,0.0499999999999999));
#52679=CARTESIAN_POINT('Origin',(0.344527189490328,-0.580195253037085,0.0499999999999999));
#52680=CARTESIAN_POINT('Origin',(0.,0.,0.0499999999999999));
#52681=CARTESIAN_POINT('Origin',(0.0840898469495519,-0.684856844632512,
0.75));
#52682=CARTESIAN_POINT('',(0.100875851451026,-0.642124647240729,0.0499999999999999));
#52683=CARTESIAN_POINT('',(0.100875851451026,-0.642124647240729,0.75));
#52684=CARTESIAN_POINT('',(0.100875851451026,-0.642124647240729,0.39));
#52685=CARTESIAN_POINT('',(0.109398351930166,-0.620428884397691,0.0499999999999999));
#52686=CARTESIAN_POINT('',(0.0840898469495519,-0.684856844632512,0.0499999999999999));
#52687=CARTESIAN_POINT('',(0.109398351930166,-0.620428884397691,0.75));
#52688=CARTESIAN_POINT('',(0.109398351930166,-0.620428884397691,0.75));
#52689=CARTESIAN_POINT('',(0.0840898469495519,-0.684856844632512,0.75));
#52690=CARTESIAN_POINT('Origin',(0.119653037223409,-0.652642864515102,0.75));
#52691=CARTESIAN_POINT('',(0.124827270658193,-0.637901365808246,0.75));
#52692=CARTESIAN_POINT('Origin',(0.,0.,0.75));
#52693=CARTESIAN_POINT('',(0.109398351930166,-0.620428884397691,0.75));
#52694=CARTESIAN_POINT('Origin',(0.109398351930166,-0.620428884397691,0.75));
#52695=CARTESIAN_POINT('',(0.124827270658193,-0.637901365808246,0.0499999999999999));
#52696=CARTESIAN_POINT('',(0.124827270658193,-0.637901365808246,0.39));
#52697=CARTESIAN_POINT('',(0.109398351930166,-0.620428884397691,0.0499999999999999));
#52698=CARTESIAN_POINT('Origin',(0.119653037223409,-0.652642864515102,0.0499999999999999));
#52699=CARTESIAN_POINT('Origin',(0.,0.,0.0499999999999999));
#52700=CARTESIAN_POINT('Origin',(-0.155216227497267,-0.672315344701812,
0.75));
#52701=CARTESIAN_POINT('',(-0.124827270658194,-0.637901365808246,0.0499999999999999));
#52702=CARTESIAN_POINT('',(-0.124827270658194,-0.637901365808246,0.75));
#52703=CARTESIAN_POINT('',(-0.124827270658194,-0.637901365808246,0.39));
#52704=CARTESIAN_POINT('',(-0.109398351930166,-0.620428884397691,0.0499999999999999));
#52705=CARTESIAN_POINT('',(-0.155216227497267,-0.672315344701812,0.0499999999999999));
#52706=CARTESIAN_POINT('',(-0.109398351930166,-0.620428884397691,0.75));
#52707=CARTESIAN_POINT('',(-0.109398351930166,-0.620428884397691,0.75));
#52708=CARTESIAN_POINT('',(-0.155216227497267,-0.672315344701812,0.75));
#52709=CARTESIAN_POINT('Origin',(-0.119653037223409,-0.652642864515102,
0.75));
#52710=CARTESIAN_POINT('',(-0.100875851451026,-0.642124647240729,0.75));
#52711=CARTESIAN_POINT('Origin',(0.,0.,0.75));
#52712=CARTESIAN_POINT('',(-0.109398351930166,-0.620428884397691,0.75));
#52713=CARTESIAN_POINT('Origin',(-0.109398351930166,-0.620428884397691,
0.75));
#52714=CARTESIAN_POINT('',(-0.100875851451026,-0.642124647240729,0.0499999999999999));
#52715=CARTESIAN_POINT('',(-0.100875851451026,-0.642124647240729,0.39));
#52716=CARTESIAN_POINT('',(-0.109398351930166,-0.620428884397691,0.0499999999999999));
#52717=CARTESIAN_POINT('Origin',(-0.119653037223409,-0.652642864515102,
0.0499999999999999));
#52718=CARTESIAN_POINT('Origin',(0.,0.,0.0499999999999999));
#52719=CARTESIAN_POINT('Origin',(-0.375800934160369,-0.578682691882343,
0.75));
#52720=CARTESIAN_POINT('',(-0.335474381671726,-0.556737765237794,0.0499999999999999));
#52721=CARTESIAN_POINT('',(-0.335474381671726,-0.556737765237794,0.75));
#52722=CARTESIAN_POINT('',(-0.335474381671726,-0.556737765237794,0.39));
#52723=CARTESIAN_POINT('',(-0.315,-0.545596004384196,0.0499999999999999));
#52724=CARTESIAN_POINT('',(-0.375800934160369,-0.578682691882343,0.0499999999999999));
#52725=CARTESIAN_POINT('',(-0.315,-0.545596004384196,0.75));
#52726=CARTESIAN_POINT('',(-0.315,-0.545596004384196,0.75));
#52727=CARTESIAN_POINT('',(-0.375800934160369,-0.578682691882343,0.75));
#52728=CARTESIAN_POINT('Origin',(-0.344527189490328,-0.580195253037085,
0.75));
#52729=CARTESIAN_POINT('',(-0.314411857106244,-0.568898219465488,0.75));
#52730=CARTESIAN_POINT('Origin',(0.,0.,0.75));
#52731=CARTESIAN_POINT('',(-0.315,-0.545596004384196,0.75));
#52732=CARTESIAN_POINT('Origin',(-0.315,-0.545596004384196,0.75));
#52733=CARTESIAN_POINT('',(-0.314411857106244,-0.568898219465488,0.0499999999999999));
#52734=CARTESIAN_POINT('',(-0.314411857106244,-0.568898219465488,0.39));
#52735=CARTESIAN_POINT('',(-0.315,-0.545596004384196,0.0499999999999999));
#52736=CARTESIAN_POINT('Origin',(-0.344527189490328,-0.580195253037085,
0.0499999999999999));
#52737=CARTESIAN_POINT('Origin',(0.,0.,0.0499999999999999));
#52738=CARTESIAN_POINT('Origin',(-0.551058501932632,-0.415252365974913,
0.75));
#52739=CARTESIAN_POINT('',(-0.505658331181079,-0.408423373605339,0.0499999999999999));
#52740=CARTESIAN_POINT('',(-0.505658331181079,-0.408423373605339,0.75));
#52741=CARTESIAN_POINT('',(-0.505658331181079,-0.408423373605339,0.39));
#52742=CARTESIAN_POINT('',(-0.482607999164956,-0.40495619410252,0.0499999999999999));
#52743=CARTESIAN_POINT('',(-0.551058501932632,-0.415252365974913,0.0499999999999999));
#52744=CARTESIAN_POINT('',(-0.482607999164956,-0.40495619410252,0.75));
#52745=CARTESIAN_POINT('',(-0.482607999164956,-0.40495619410252,0.75));
#52746=CARTESIAN_POINT('',(-0.551058501932632,-0.415252365974913,0.75));
#52747=CARTESIAN_POINT('Origin',(-0.516833250548794,-0.437767531272822,
0.75));
#52748=CARTESIAN_POINT('',(-0.490025152569635,-0.427054270379195,0.75));
#52749=CARTESIAN_POINT('Origin',(0.,0.,0.75));
#52750=CARTESIAN_POINT('',(-0.482607999164956,-0.40495619410252,0.75));
#52751=CARTESIAN_POINT('Origin',(-0.482607999164956,-0.40495619410252,0.75));
#52752=CARTESIAN_POINT('',(-0.490025152569635,-0.427054270379195,0.0499999999999999));
#52753=CARTESIAN_POINT('',(-0.490025152569635,-0.427054270379195,0.39));
#52754=CARTESIAN_POINT('',(-0.482607999164956,-0.40495619410252,0.0499999999999999));
#52755=CARTESIAN_POINT('Origin',(-0.516833250548794,-0.437767531272822,
0.0499999999999999));
#52756=CARTESIAN_POINT('Origin',(0.,0.,0.0499999999999999));
#52757=CARTESIAN_POINT('Origin',(-0.659850281614495,-0.201736476258688,
0.75));
#52758=CARTESIAN_POINT('',(-0.614852423227828,-0.210847095429052,0.0499999999999999));
#52759=CARTESIAN_POINT('',(-0.614852423227828,-0.210847095429052,0.75));
#52760=CARTESIAN_POINT('',(-0.614852423227828,-0.210847095429052,0.39));
#52761=CARTESIAN_POINT('',(-0.592006351095122,-0.215472690295171,0.0499999999999999));
#52762=CARTESIAN_POINT('',(-0.659850281614495,-0.201736476258688,0.0499999999999999));
#52763=CARTESIAN_POINT('',(-0.592006351095122,-0.215472690295171,0.75));
#52764=CARTESIAN_POINT('',(-0.592006351095122,-0.215472690295171,0.75));
#52765=CARTESIAN_POINT('',(-0.659850281614495,-0.201736476258688,0.75));
#52766=CARTESIAN_POINT('Origin',(-0.625928316354808,-0.235670477458144,
0.75));
#52767=CARTESIAN_POINT('',(-0.606534182632106,-0.23370127363539,0.75));
#52768=CARTESIAN_POINT('Origin',(0.,0.,0.75));
#52769=CARTESIAN_POINT('',(-0.592006351095122,-0.215472690295171,0.75));
#52770=CARTESIAN_POINT('Origin',(-0.592006351095122,-0.215472690295171,
0.75));
#52771=CARTESIAN_POINT('',(-0.606534182632106,-0.23370127363539,0.0499999999999999));
#52772=CARTESIAN_POINT('',(-0.606534182632106,-0.23370127363539,0.39));
#52773=CARTESIAN_POINT('',(-0.592006351095122,-0.215472690295171,0.0499999999999999));
#52774=CARTESIAN_POINT('Origin',(-0.625928316354808,-0.235670477458144,
0.0499999999999999));
#52775=CARTESIAN_POINT('Origin',(0.,0.,0.0499999999999999));
#52776=CARTESIAN_POINT('Origin',(-0.689054378980656,0.0361118098076312,
0.75));
#52777=CARTESIAN_POINT('',(-0.64988623877797,0.0121604542276944,0.0499999999999999));
#52778=CARTESIAN_POINT('',(-0.64988623877797,0.0121604542276944,0.75));
#52779=CARTESIAN_POINT('',(-0.64988623877797,0.0121604542276944,0.39));
#52780=CARTESIAN_POINT('',(-0.63,7.71527483462833E-17,0.0499999999999999));
#52781=CARTESIAN_POINT('',(-0.689054378980656,0.0361118098076312,0.0499999999999999));
#52782=CARTESIAN_POINT('',(-0.63,7.71527483462833E-17,0.75));
#52783=CARTESIAN_POINT('',(-0.63,7.71527483462833E-17,0.75));
#52784=CARTESIAN_POINT('',(-0.689054378980656,0.0361118098076312,0.75));
#52785=CARTESIAN_POINT('Origin',(-0.659527189490328,8.32667268468867E-17,
0.75));
#52786=CARTESIAN_POINT('',(-0.65,-7.9602041944578E-17,0.75));
#52787=CARTESIAN_POINT('Origin',(0.,0.,0.75));
#52788=CARTESIAN_POINT('',(-0.64988623877797,-0.0121604542276942,0.75));
#52789=CARTESIAN_POINT('',(-0.63,7.71527483462833E-17,0.75));
#52790=CARTESIAN_POINT('Origin',(0.,0.,0.75));
#52791=CARTESIAN_POINT('Origin',(-0.63,7.71527483462833E-17,0.75));
#52792=CARTESIAN_POINT('',(-0.64988623877797,-0.0121604542276942,0.0499999999999999));
#52793=CARTESIAN_POINT('',(-0.64988623877797,-0.0121604542276942,0.39));
#52794=CARTESIAN_POINT('',(-0.63,7.71527483462833E-17,0.0499999999999999));
#52795=CARTESIAN_POINT('Origin',(-0.659527189490328,8.32667268468867E-17,
0.0499999999999999));
#52796=CARTESIAN_POINT('',(-0.65,-7.9602041944578E-17,0.0499999999999999));
#52797=CARTESIAN_POINT('Origin',(0.,0.,0.0499999999999999));
#52798=CARTESIAN_POINT('Origin',(0.,0.,0.0499999999999999));
#52799=CARTESIAN_POINT('Origin',(-0.672315344701812,0.155216227497267,0.75));
#52800=CARTESIAN_POINT('',(-0.637901365808246,0.124827270658193,0.0499999999999999));
#52801=CARTESIAN_POINT('',(-0.637901365808246,0.124827270658193,0.75));
#52802=CARTESIAN_POINT('',(-0.637901365808246,0.124827270658193,0.39));
#52803=CARTESIAN_POINT('',(-0.620428884397691,0.109398351930166,0.0499999999999999));
#52804=CARTESIAN_POINT('',(-0.672315344701812,0.155216227497267,0.0499999999999999));
#52805=CARTESIAN_POINT('',(-0.620428884397691,0.109398351930166,0.75));
#52806=CARTESIAN_POINT('',(-0.620428884397691,0.109398351930166,0.75));
#52807=CARTESIAN_POINT('',(-0.672315344701812,0.155216227497267,0.75));
#52808=CARTESIAN_POINT('Origin',(-0.652642864515102,0.119653037223409,0.75));
#52809=CARTESIAN_POINT('',(-0.642124647240729,0.100875851451027,0.75));
#52810=CARTESIAN_POINT('Origin',(0.,0.,0.75));
#52811=CARTESIAN_POINT('',(-0.620428884397691,0.109398351930166,0.75));
#52812=CARTESIAN_POINT('Origin',(-0.620428884397691,0.109398351930166,0.75));
#52813=CARTESIAN_POINT('',(-0.642124647240729,0.100875851451027,0.0499999999999999));
#52814=CARTESIAN_POINT('',(-0.642124647240729,0.100875851451027,0.39));
#52815=CARTESIAN_POINT('',(-0.620428884397691,0.109398351930166,0.0499999999999999));
#52816=CARTESIAN_POINT('Origin',(-0.652642864515102,0.119653037223409,0.0499999999999999));
#52817=CARTESIAN_POINT('Origin',(0.,0.,0.0499999999999999));
#52818=CARTESIAN_POINT('Origin',(-0.578682691882343,0.375800934160369,0.75));
#52819=CARTESIAN_POINT('',(-0.556737765237794,0.335474381671726,0.0499999999999999));
#52820=CARTESIAN_POINT('',(-0.556737765237794,0.335474381671726,0.75));
#52821=CARTESIAN_POINT('',(-0.556737765237794,0.335474381671726,0.39));
#52822=CARTESIAN_POINT('',(-0.545596004384196,0.315,0.0499999999999999));
#52823=CARTESIAN_POINT('',(-0.578682691882343,0.375800934160369,0.0499999999999999));
#52824=CARTESIAN_POINT('',(-0.545596004384196,0.315,0.75));
#52825=CARTESIAN_POINT('',(-0.545596004384196,0.315,0.75));
#52826=CARTESIAN_POINT('',(-0.578682691882343,0.375800934160369,0.75));
#52827=CARTESIAN_POINT('Origin',(-0.580195253037085,0.344527189490328,0.75));
#52828=CARTESIAN_POINT('',(-0.568898219465488,0.314411857106244,0.75));
#52829=CARTESIAN_POINT('Origin',(0.,0.,0.75));
#52830=CARTESIAN_POINT('',(-0.545596004384196,0.315,0.75));
#52831=CARTESIAN_POINT('Origin',(-0.545596004384196,0.315,0.75));
#52832=CARTESIAN_POINT('',(-0.568898219465488,0.314411857106244,0.0499999999999999));
#52833=CARTESIAN_POINT('',(-0.568898219465488,0.314411857106244,0.39));
#52834=CARTESIAN_POINT('',(-0.545596004384196,0.315,0.0499999999999999));
#52835=CARTESIAN_POINT('Origin',(-0.580195253037085,0.344527189490328,0.0499999999999999));
#52836=CARTESIAN_POINT('Origin',(0.,0.,0.0499999999999999));
#52837=CARTESIAN_POINT('Origin',(-0.415252365974913,0.551058501932632,0.75));
#52838=CARTESIAN_POINT('',(-0.408423373605339,0.505658331181079,0.0499999999999999));
#52839=CARTESIAN_POINT('',(-0.408423373605339,0.505658331181079,0.75));
#52840=CARTESIAN_POINT('',(-0.408423373605339,0.505658331181079,0.39));
#52841=CARTESIAN_POINT('',(-0.40495619410252,0.482607999164956,0.0499999999999999));
#52842=CARTESIAN_POINT('',(-0.415252365974913,0.551058501932632,0.0499999999999999));
#52843=CARTESIAN_POINT('',(-0.40495619410252,0.482607999164956,0.75));
#52844=CARTESIAN_POINT('',(-0.40495619410252,0.482607999164956,0.75));
#52845=CARTESIAN_POINT('',(-0.415252365974913,0.551058501932632,0.75));
#52846=CARTESIAN_POINT('Origin',(-0.437767531272822,0.516833250548794,0.75));
#52847=CARTESIAN_POINT('',(-0.427054270379195,0.490025152569635,0.75));
#52848=CARTESIAN_POINT('Origin',(0.,0.,0.75));
#52849=CARTESIAN_POINT('',(-0.40495619410252,0.482607999164956,0.75));
#52850=CARTESIAN_POINT('Origin',(-0.40495619410252,0.482607999164956,0.75));
#52851=CARTESIAN_POINT('',(-0.427054270379195,0.490025152569635,0.0499999999999999));
#52852=CARTESIAN_POINT('',(-0.427054270379195,0.490025152569635,0.39));
#52853=CARTESIAN_POINT('',(-0.40495619410252,0.482607999164956,0.0499999999999999));
#52854=CARTESIAN_POINT('Origin',(-0.437767531272822,0.516833250548794,0.0499999999999999));
#52855=CARTESIAN_POINT('Origin',(0.,0.,0.0499999999999999));
#52856=CARTESIAN_POINT('Origin',(-0.201736476258688,0.659850281614495,0.75));
#52857=CARTESIAN_POINT('',(-0.210847095429052,0.614852423227828,0.0499999999999999));
#52858=CARTESIAN_POINT('',(-0.210847095429052,0.614852423227828,0.75));
#52859=CARTESIAN_POINT('',(-0.210847095429052,0.614852423227828,0.39));
#52860=CARTESIAN_POINT('',(-0.215472690295171,0.592006351095122,0.0499999999999999));
#52861=CARTESIAN_POINT('',(-0.201736476258688,0.659850281614495,0.0499999999999999));
#52862=CARTESIAN_POINT('',(-0.215472690295171,0.592006351095122,0.75));
#52863=CARTESIAN_POINT('',(-0.215472690295171,0.592006351095122,0.75));
#52864=CARTESIAN_POINT('',(-0.201736476258688,0.659850281614495,0.75));
#52865=CARTESIAN_POINT('Origin',(-0.235670477458144,0.625928316354808,0.75));
#52866=CARTESIAN_POINT('',(-0.23370127363539,0.606534182632106,0.75));
#52867=CARTESIAN_POINT('Origin',(0.,0.,0.75));
#52868=CARTESIAN_POINT('',(-0.215472690295171,0.592006351095122,0.75));
#52869=CARTESIAN_POINT('Origin',(-0.215472690295171,0.592006351095122,0.75));
#52870=CARTESIAN_POINT('',(-0.23370127363539,0.606534182632106,0.0499999999999999));
#52871=CARTESIAN_POINT('',(-0.23370127363539,0.606534182632106,0.39));
#52872=CARTESIAN_POINT('',(-0.215472690295171,0.592006351095122,0.0499999999999999));
#52873=CARTESIAN_POINT('Origin',(-0.235670477458144,0.625928316354808,0.0499999999999999));
#52874=CARTESIAN_POINT('Origin',(0.,0.,0.0499999999999999));
#52875=CARTESIAN_POINT('Origin',(0.0361118098076313,0.689054378980656,0.75));
#52876=CARTESIAN_POINT('',(0.0121604542276944,0.64988623877797,0.0499999999999999));
#52877=CARTESIAN_POINT('',(0.0121604542276944,0.64988623877797,0.75));
#52878=CARTESIAN_POINT('',(0.0121604542276944,0.64988623877797,0.39));
#52879=CARTESIAN_POINT('',(3.85763741731416E-17,0.63,0.0499999999999999));
#52880=CARTESIAN_POINT('',(0.0361118098076313,0.689054378980656,0.0499999999999999));
#52881=CARTESIAN_POINT('',(3.85763741731416E-17,0.63,0.75));
#52882=CARTESIAN_POINT('',(3.85763741731416E-17,0.63,0.75));
#52883=CARTESIAN_POINT('',(0.0361118098076313,0.689054378980656,0.75));
#52884=CARTESIAN_POINT('Origin',(4.16333634234434E-17,0.659527189490328,
0.75));
#52885=CARTESIAN_POINT('',(-0.0121604542276943,0.64988623877797,0.75));
#52886=CARTESIAN_POINT('Origin',(0.,0.,0.75));
#52887=CARTESIAN_POINT('',(3.85763741731416E-17,0.63,0.75));
#52888=CARTESIAN_POINT('Origin',(3.85763741731416E-17,0.63,0.75));
#52889=CARTESIAN_POINT('',(-0.0121604542276943,0.64988623877797,0.0499999999999999));
#52890=CARTESIAN_POINT('',(-0.0121604542276943,0.64988623877797,0.39));
#52891=CARTESIAN_POINT('',(3.85763741731416E-17,0.63,0.0499999999999999));
#52892=CARTESIAN_POINT('Origin',(4.16333634234434E-17,0.659527189490328,
0.0499999999999999));
#52893=CARTESIAN_POINT('Origin',(0.,0.,0.0499999999999999));
#52894=CARTESIAN_POINT('Origin',(0.269604478657599,0.635148348882184,0.75));
#52895=CARTESIAN_POINT('',(0.23370127363539,0.606534182632106,0.0499999999999999));
#52896=CARTESIAN_POINT('',(0.23370127363539,0.606534182632106,0.75));
#52897=CARTESIAN_POINT('',(0.23370127363539,0.606534182632106,0.39));
#52898=CARTESIAN_POINT('',(0.215472690295171,0.592006351095122,0.0499999999999999));
#52899=CARTESIAN_POINT('',(0.269604478657599,0.635148348882184,0.0499999999999999));
#52900=CARTESIAN_POINT('',(0.215472690295171,0.592006351095122,0.75));
#52901=CARTESIAN_POINT('',(0.215472690295171,0.592006351095122,0.75));
#52902=CARTESIAN_POINT('',(0.269604478657599,0.635148348882184,0.75));
#52903=CARTESIAN_POINT('Origin',(0.235670477458144,0.625928316354808,0.75));
#52904=CARTESIAN_POINT('',(0.210847095429052,0.614852423227828,0.75));
#52905=CARTESIAN_POINT('Origin',(0.,0.,0.75));
#52906=CARTESIAN_POINT('',(0.215472690295171,0.592006351095122,0.75));
#52907=CARTESIAN_POINT('Origin',(0.215472690295171,0.592006351095122,0.75));
#52908=CARTESIAN_POINT('',(0.210847095429052,0.614852423227828,0.0499999999999999));
#52909=CARTESIAN_POINT('',(0.210847095429052,0.614852423227828,0.39));
#52910=CARTESIAN_POINT('',(0.215472690295171,0.592006351095122,0.0499999999999999));
#52911=CARTESIAN_POINT('Origin',(0.235670477458144,0.625928316354808,0.0499999999999999));
#52912=CARTESIAN_POINT('Origin',(0.,0.,0.0499999999999999));
#52913=CARTESIAN_POINT('Origin',(0.470578868443124,0.504634054117228,0.75));
#52914=CARTESIAN_POINT('',(0.427054270379195,0.490025152569635,0.0499999999999999));
#52915=CARTESIAN_POINT('',(0.427054270379195,0.490025152569635,0.75));
#52916=CARTESIAN_POINT('',(0.427054270379195,0.490025152569635,0.39));
#52917=CARTESIAN_POINT('',(0.40495619410252,0.482607999164956,0.0499999999999999));
#52918=CARTESIAN_POINT('',(0.470578868443124,0.504634054117228,0.0499999999999999));
#52919=CARTESIAN_POINT('',(0.40495619410252,0.482607999164956,0.75));
#52920=CARTESIAN_POINT('',(0.40495619410252,0.482607999164956,0.75));
#52921=CARTESIAN_POINT('',(0.470578868443124,0.504634054117228,0.75));
#52922=CARTESIAN_POINT('Origin',(0.437767531272822,0.516833250548794,0.75));
#52923=CARTESIAN_POINT('',(0.408423373605339,0.505658331181079,0.75));
#52924=CARTESIAN_POINT('Origin',(0.,0.,0.75));
#52925=CARTESIAN_POINT('',(0.40495619410252,0.482607999164956,0.75));
#52926=CARTESIAN_POINT('Origin',(0.40495619410252,0.482607999164956,0.75));
#52927=CARTESIAN_POINT('',(0.408423373605339,0.505658331181079,0.0499999999999999));
#52928=CARTESIAN_POINT('',(0.408423373605339,0.505658331181079,0.39));
#52929=CARTESIAN_POINT('',(0.40495619410252,0.482607999164956,0.0499999999999999));
#52930=CARTESIAN_POINT('Origin',(0.437767531272822,0.516833250548794,0.0499999999999999));
#52931=CARTESIAN_POINT('Origin',(0.,0.,0.0499999999999999));
#52932=CARTESIAN_POINT('Origin',(0.614794501689974,0.313253444820287,0.75));
#52933=CARTESIAN_POINT('',(0.568898219465489,0.314411857106244,0.0499999999999999));
#52934=CARTESIAN_POINT('',(0.568898219465489,0.314411857106244,0.75));
#52935=CARTESIAN_POINT('',(0.568898219465489,0.314411857106244,0.39));
#52936=CARTESIAN_POINT('',(0.545596004384196,0.315,0.0499999999999999));
#52937=CARTESIAN_POINT('',(0.614794501689974,0.313253444820287,0.0499999999999999));
#52938=CARTESIAN_POINT('',(0.545596004384196,0.315,0.75));
#52939=CARTESIAN_POINT('',(0.545596004384196,0.315,0.75));
#52940=CARTESIAN_POINT('',(0.614794501689974,0.313253444820287,0.75));
#52941=CARTESIAN_POINT('Origin',(0.580195253037085,0.344527189490328,0.75));
#52942=CARTESIAN_POINT('',(0.556737765237794,0.335474381671726,0.75));
#52943=CARTESIAN_POINT('Origin',(0.,0.,0.75));
#52944=CARTESIAN_POINT('',(0.545596004384196,0.315,0.75));
#52945=CARTESIAN_POINT('Origin',(0.545596004384196,0.315,0.75));
#52946=CARTESIAN_POINT('',(0.556737765237794,0.335474381671726,0.0499999999999999));
#52947=CARTESIAN_POINT('',(0.556737765237794,0.335474381671726,0.39));
#52948=CARTESIAN_POINT('',(0.545596004384196,0.315,0.0499999999999999));
#52949=CARTESIAN_POINT('Origin',(0.580195253037085,0.344527189490328,0.0499999999999999));
#52950=CARTESIAN_POINT('Origin',(0.,0.,0.0499999999999999));
#52951=CARTESIAN_POINT('Origin',(0.684856844632512,0.0840898469495518,0.75));
#52952=CARTESIAN_POINT('',(0.642124647240729,0.100875851451026,0.0499999999999999));
#52953=CARTESIAN_POINT('',(0.642124647240729,0.100875851451026,0.75));
#52954=CARTESIAN_POINT('',(0.642124647240729,0.100875851451026,0.39));
#52955=CARTESIAN_POINT('',(0.620428884397691,0.109398351930166,0.0499999999999999));
#52956=CARTESIAN_POINT('',(0.684856844632512,0.0840898469495518,0.0499999999999999));
#52957=CARTESIAN_POINT('',(0.620428884397691,0.109398351930166,0.75));
#52958=CARTESIAN_POINT('',(0.620428884397691,0.109398351930166,0.75));
#52959=CARTESIAN_POINT('',(0.684856844632512,0.0840898469495518,0.75));
#52960=CARTESIAN_POINT('Origin',(0.652642864515102,0.119653037223409,0.75));
#52961=CARTESIAN_POINT('',(0.637901365808246,0.124827270658193,0.75));
#52962=CARTESIAN_POINT('Origin',(0.,0.,0.75));
#52963=CARTESIAN_POINT('',(0.620428884397691,0.109398351930166,0.75));
#52964=CARTESIAN_POINT('Origin',(0.620428884397691,0.109398351930166,0.75));
#52965=CARTESIAN_POINT('',(0.637901365808246,0.124827270658193,0.0499999999999999));
#52966=CARTESIAN_POINT('',(0.637901365808246,0.124827270658193,0.39));
#52967=CARTESIAN_POINT('',(0.620428884397691,0.109398351930166,0.0499999999999999));
#52968=CARTESIAN_POINT('Origin',(0.652642864515102,0.119653037223409,0.0499999999999999));
#52969=CARTESIAN_POINT('Origin',(0.,0.,0.0499999999999999));
#52970=CARTESIAN_POINT('Origin',(0.659850281614495,0.201736476258688,0.75));
#52971=CARTESIAN_POINT('',(0.614852423227828,0.210847095429052,0.0499999999999999));
#52972=CARTESIAN_POINT('',(0.614852423227828,0.210847095429052,0.75));
#52973=CARTESIAN_POINT('',(0.614852423227828,0.210847095429052,0.39));
#52974=CARTESIAN_POINT('',(0.592006351095122,0.215472690295171,0.0499999999999999));
#52975=CARTESIAN_POINT('',(0.659850281614495,0.201736476258688,0.0499999999999999));
#52976=CARTESIAN_POINT('',(0.592006351095122,0.215472690295171,0.75));
#52977=CARTESIAN_POINT('',(0.592006351095122,0.215472690295171,0.75));
#52978=CARTESIAN_POINT('',(0.659850281614495,0.201736476258688,0.75));
#52979=CARTESIAN_POINT('Origin',(0.625928316354808,0.235670477458144,0.75));
#52980=CARTESIAN_POINT('',(0.606534182632106,0.23370127363539,0.75));
#52981=CARTESIAN_POINT('Origin',(0.,0.,0.75));
#52982=CARTESIAN_POINT('',(0.592006351095122,0.215472690295171,0.75));
#52983=CARTESIAN_POINT('Origin',(0.592006351095122,0.215472690295171,0.75));
#52984=CARTESIAN_POINT('',(0.606534182632106,0.23370127363539,0.0499999999999999));
#52985=CARTESIAN_POINT('',(0.606534182632106,0.23370127363539,0.39));
#52986=CARTESIAN_POINT('',(0.592006351095122,0.215472690295171,0.0499999999999999));
#52987=CARTESIAN_POINT('Origin',(0.625928316354808,0.235670477458144,0.0499999999999999));
#52988=CARTESIAN_POINT('Origin',(0.,0.,0.0499999999999999));
#52989=CARTESIAN_POINT('Origin',(0.551058501932632,0.415252365974913,0.75));
#52990=CARTESIAN_POINT('',(0.505658331181079,0.408423373605339,0.0499999999999999));
#52991=CARTESIAN_POINT('',(0.505658331181079,0.408423373605339,0.75));
#52992=CARTESIAN_POINT('',(0.505658331181079,0.408423373605339,0.39));
#52993=CARTESIAN_POINT('',(0.482607999164956,0.40495619410252,0.0499999999999999));
#52994=CARTESIAN_POINT('',(0.551058501932632,0.415252365974913,0.0499999999999999));
#52995=CARTESIAN_POINT('',(0.482607999164956,0.40495619410252,0.75));
#52996=CARTESIAN_POINT('',(0.482607999164956,0.40495619410252,0.75));
#52997=CARTESIAN_POINT('',(0.551058501932632,0.415252365974913,0.75));
#52998=CARTESIAN_POINT('Origin',(0.516833250548794,0.437767531272822,0.75));
#52999=CARTESIAN_POINT('',(0.490025152569635,0.427054270379194,0.75));
#53000=CARTESIAN_POINT('Origin',(0.,0.,0.75));
#53001=CARTESIAN_POINT('',(0.482607999164956,0.40495619410252,0.75));
#53002=CARTESIAN_POINT('Origin',(0.482607999164956,0.40495619410252,0.75));
#53003=CARTESIAN_POINT('',(0.490025152569635,0.427054270379194,0.0499999999999999));
#53004=CARTESIAN_POINT('',(0.490025152569635,0.427054270379194,0.39));
#53005=CARTESIAN_POINT('',(0.482607999164956,0.40495619410252,0.0499999999999999));
#53006=CARTESIAN_POINT('Origin',(0.516833250548794,0.437767531272822,0.0499999999999999));
#53007=CARTESIAN_POINT('Origin',(0.,0.,0.0499999999999999));
#53008=CARTESIAN_POINT('Origin',(0.375800934160369,0.578682691882343,0.75));
#53009=CARTESIAN_POINT('',(0.335474381671726,0.556737765237794,0.0499999999999999));
#53010=CARTESIAN_POINT('',(0.335474381671726,0.556737765237794,0.75));
#53011=CARTESIAN_POINT('',(0.335474381671726,0.556737765237794,0.39));
#53012=CARTESIAN_POINT('',(0.315,0.545596004384196,0.0499999999999999));
#53013=CARTESIAN_POINT('',(0.375800934160369,0.578682691882343,0.0499999999999999));
#53014=CARTESIAN_POINT('',(0.315,0.545596004384196,0.75));
#53015=CARTESIAN_POINT('',(0.315,0.545596004384196,0.75));
#53016=CARTESIAN_POINT('',(0.375800934160369,0.578682691882343,0.75));
#53017=CARTESIAN_POINT('Origin',(0.344527189490328,0.580195253037085,0.75));
#53018=CARTESIAN_POINT('',(0.314411857106244,0.568898219465488,0.75));
#53019=CARTESIAN_POINT('Origin',(0.,0.,0.75));
#53020=CARTESIAN_POINT('',(0.315,0.545596004384196,0.75));
#53021=CARTESIAN_POINT('Origin',(0.315,0.545596004384196,0.75));
#53022=CARTESIAN_POINT('',(0.314411857106244,0.568898219465488,0.0499999999999999));
#53023=CARTESIAN_POINT('',(0.314411857106244,0.568898219465488,0.39));
#53024=CARTESIAN_POINT('',(0.315,0.545596004384196,0.0499999999999999));
#53025=CARTESIAN_POINT('Origin',(0.344527189490328,0.580195253037085,0.0499999999999999));
#53026=CARTESIAN_POINT('Origin',(0.,0.,0.0499999999999999));
#53027=CARTESIAN_POINT('Origin',(0.155216227497267,0.672315344701812,0.75));
#53028=CARTESIAN_POINT('',(0.124827270658193,0.637901365808246,0.0499999999999999));
#53029=CARTESIAN_POINT('',(0.124827270658193,0.637901365808246,0.75));
#53030=CARTESIAN_POINT('',(0.124827270658193,0.637901365808246,0.39));
#53031=CARTESIAN_POINT('',(0.109398351930166,0.620428884397691,0.0499999999999999));
#53032=CARTESIAN_POINT('',(0.155216227497267,0.672315344701812,0.0499999999999999));
#53033=CARTESIAN_POINT('',(0.109398351930166,0.620428884397691,0.75));
#53034=CARTESIAN_POINT('',(0.109398351930166,0.620428884397691,0.75));
#53035=CARTESIAN_POINT('',(0.155216227497267,0.672315344701812,0.75));
#53036=CARTESIAN_POINT('Origin',(0.119653037223409,0.652642864515102,0.75));
#53037=CARTESIAN_POINT('',(0.100875851451027,0.642124647240729,0.75));
#53038=CARTESIAN_POINT('Origin',(0.,0.,0.75));
#53039=CARTESIAN_POINT('',(0.109398351930166,0.620428884397691,0.75));
#53040=CARTESIAN_POINT('Origin',(0.109398351930166,0.620428884397691,0.75));
#53041=CARTESIAN_POINT('',(0.100875851451027,0.642124647240729,0.0499999999999999));
#53042=CARTESIAN_POINT('',(0.100875851451027,0.642124647240729,0.39));
#53043=CARTESIAN_POINT('',(0.109398351930166,0.620428884397691,0.0499999999999999));
#53044=CARTESIAN_POINT('Origin',(0.119653037223409,0.652642864515102,0.0499999999999999));
#53045=CARTESIAN_POINT('Origin',(0.,0.,0.0499999999999999));
#53046=CARTESIAN_POINT('Origin',(-0.0840898469495517,0.684856844632512,
0.75));
#53047=CARTESIAN_POINT('',(-0.100875851451027,0.642124647240729,0.0499999999999999));
#53048=CARTESIAN_POINT('',(-0.100875851451027,0.642124647240729,0.75));
#53049=CARTESIAN_POINT('',(-0.100875851451026,0.642124647240729,0.39));
#53050=CARTESIAN_POINT('',(-0.109398351930166,0.620428884397691,0.0499999999999999));
#53051=CARTESIAN_POINT('',(-0.0840898469495517,0.684856844632512,0.0499999999999999));
#53052=CARTESIAN_POINT('',(-0.109398351930166,0.620428884397691,0.75));
#53053=CARTESIAN_POINT('',(-0.109398351930166,0.620428884397691,0.75));
#53054=CARTESIAN_POINT('',(-0.0840898469495517,0.684856844632512,0.75));
#53055=CARTESIAN_POINT('Origin',(-0.119653037223409,0.652642864515102,0.75));
#53056=CARTESIAN_POINT('',(-0.124827270658193,0.637901365808246,0.75));
#53057=CARTESIAN_POINT('Origin',(0.,0.,0.75));
#53058=CARTESIAN_POINT('',(-0.109398351930166,0.620428884397691,0.75));
#53059=CARTESIAN_POINT('Origin',(-0.109398351930166,0.620428884397691,0.75));
#53060=CARTESIAN_POINT('',(-0.124827270658193,0.637901365808246,0.0499999999999999));
#53061=CARTESIAN_POINT('',(-0.124827270658193,0.637901365808246,0.39));
#53062=CARTESIAN_POINT('',(-0.109398351930166,0.620428884397691,0.0499999999999999));
#53063=CARTESIAN_POINT('Origin',(-0.119653037223409,0.652642864515102,0.0499999999999999));
#53064=CARTESIAN_POINT('Origin',(0.,0.,0.0499999999999999));
#53065=CARTESIAN_POINT('Origin',(-0.313253444820287,0.614794501689974,0.75));
#53066=CARTESIAN_POINT('',(-0.314411857106243,0.568898219465489,0.0499999999999999));
#53067=CARTESIAN_POINT('',(-0.314411857106243,0.568898219465489,0.75));
#53068=CARTESIAN_POINT('',(-0.314411857106243,0.568898219465489,0.39));
#53069=CARTESIAN_POINT('',(-0.315,0.545596004384196,0.0499999999999999));
#53070=CARTESIAN_POINT('',(-0.313253444820287,0.614794501689974,0.0499999999999999));
#53071=CARTESIAN_POINT('',(-0.315,0.545596004384196,0.75));
#53072=CARTESIAN_POINT('',(-0.315,0.545596004384196,0.75));
#53073=CARTESIAN_POINT('',(-0.313253444820287,0.614794501689974,0.75));
#53074=CARTESIAN_POINT('Origin',(-0.344527189490328,0.580195253037085,0.75));
#53075=CARTESIAN_POINT('',(-0.335474381671726,0.556737765237794,0.75));
#53076=CARTESIAN_POINT('Origin',(0.,0.,0.75));
#53077=CARTESIAN_POINT('',(-0.315,0.545596004384196,0.75));
#53078=CARTESIAN_POINT('Origin',(-0.315,0.545596004384196,0.75));
#53079=CARTESIAN_POINT('',(-0.335474381671726,0.556737765237794,0.0499999999999999));
#53080=CARTESIAN_POINT('',(-0.335474381671726,0.556737765237794,0.39));
#53081=CARTESIAN_POINT('',(-0.315,0.545596004384196,0.0499999999999999));
#53082=CARTESIAN_POINT('Origin',(-0.344527189490328,0.580195253037085,0.0499999999999999));
#53083=CARTESIAN_POINT('Origin',(0.,0.,0.0499999999999999));
#53084=CARTESIAN_POINT('Origin',(-0.504634054117228,0.470578868443124,0.75));
#53085=CARTESIAN_POINT('',(-0.490025152569635,0.427054270379195,0.0499999999999999));
#53086=CARTESIAN_POINT('',(-0.490025152569635,0.427054270379195,0.75));
#53087=CARTESIAN_POINT('',(-0.490025152569635,0.427054270379195,0.39));
#53088=CARTESIAN_POINT('',(-0.482607999164956,0.40495619410252,0.0499999999999999));
#53089=CARTESIAN_POINT('',(-0.504634054117228,0.470578868443124,0.0499999999999999));
#53090=CARTESIAN_POINT('',(-0.482607999164956,0.40495619410252,0.75));
#53091=CARTESIAN_POINT('',(-0.482607999164956,0.40495619410252,0.75));
#53092=CARTESIAN_POINT('',(-0.504634054117228,0.470578868443124,0.75));
#53093=CARTESIAN_POINT('Origin',(-0.516833250548794,0.437767531272822,0.75));
#53094=CARTESIAN_POINT('',(-0.505658331181079,0.408423373605339,0.75));
#53095=CARTESIAN_POINT('Origin',(0.,0.,0.75));
#53096=CARTESIAN_POINT('',(-0.482607999164956,0.40495619410252,0.75));
#53097=CARTESIAN_POINT('Origin',(-0.482607999164956,0.40495619410252,0.75));
#53098=CARTESIAN_POINT('',(-0.505658331181079,0.408423373605339,0.0499999999999999));
#53099=CARTESIAN_POINT('',(-0.505658331181079,0.408423373605339,0.39));
#53100=CARTESIAN_POINT('',(-0.482607999164956,0.40495619410252,0.0499999999999999));
#53101=CARTESIAN_POINT('Origin',(-0.516833250548794,0.437767531272822,0.0499999999999999));
#53102=CARTESIAN_POINT('Origin',(0.,0.,0.0499999999999999));
#53103=CARTESIAN_POINT('Origin',(-0.635148348882184,0.269604478657599,0.75));
#53104=CARTESIAN_POINT('',(-0.606534182632106,0.23370127363539,0.0499999999999999));
#53105=CARTESIAN_POINT('',(-0.606534182632106,0.23370127363539,0.75));
#53106=CARTESIAN_POINT('',(-0.606534182632106,0.23370127363539,0.39));
#53107=CARTESIAN_POINT('',(-0.592006351095122,0.215472690295171,0.0499999999999999));
#53108=CARTESIAN_POINT('',(-0.635148348882184,0.269604478657599,0.0499999999999999));
#53109=CARTESIAN_POINT('',(-0.592006351095122,0.215472690295171,0.75));
#53110=CARTESIAN_POINT('',(-0.592006351095122,0.215472690295171,0.75));
#53111=CARTESIAN_POINT('',(-0.635148348882184,0.269604478657599,0.75));
#53112=CARTESIAN_POINT('Origin',(-0.625928316354808,0.235670477458144,0.75));
#53113=CARTESIAN_POINT('',(-0.614852423227828,0.210847095429052,0.75));
#53114=CARTESIAN_POINT('Origin',(0.,0.,0.75));
#53115=CARTESIAN_POINT('',(-0.592006351095122,0.215472690295171,0.75));
#53116=CARTESIAN_POINT('Origin',(-0.592006351095122,0.215472690295171,0.75));
#53117=CARTESIAN_POINT('',(-0.614852423227828,0.210847095429052,0.0499999999999999));
#53118=CARTESIAN_POINT('',(-0.614852423227828,0.210847095429052,0.39));
#53119=CARTESIAN_POINT('',(-0.592006351095122,0.215472690295171,0.0499999999999999));
#53120=CARTESIAN_POINT('Origin',(-0.625928316354808,0.235670477458144,0.0499999999999999));
#53121=CARTESIAN_POINT('Origin',(0.,0.,0.0499999999999999));
#53122=CARTESIAN_POINT('Origin',(0.659527189490328,0.,0.75));
#53123=CARTESIAN_POINT('',(0.64988623877797,-0.0121604542276943,0.75));
#53124=CARTESIAN_POINT('',(0.64988623877797,0.0121604542276944,0.75));
#53125=CARTESIAN_POINT('Origin',(0.,0.,0.75));
#53126=CARTESIAN_POINT('',(0.63,0.,0.75));
#53127=CARTESIAN_POINT('',(0.689054378980656,-0.0361118098076312,0.75));
#53128=CARTESIAN_POINT('',(0.63,0.,0.75));
#53129=CARTESIAN_POINT('Origin',(0.689054378980656,-0.0361118098076312,
0.75));
#53130=CARTESIAN_POINT('',(0.64988623877797,-0.0121604542276943,0.0499999999999999));
#53131=CARTESIAN_POINT('',(0.64988623877797,-0.0121604542276943,0.39));
#53132=CARTESIAN_POINT('',(0.63,0.,0.0499999999999999));
#53133=CARTESIAN_POINT('',(0.689054378980656,-0.0361118098076312,0.0499999999999999));
#53134=CARTESIAN_POINT('',(0.63,0.,0.75));
#53135=CARTESIAN_POINT('Origin',(0.63,0.,0.75));
#53136=CARTESIAN_POINT('',(0.64988623877797,0.0121604542276944,0.0499999999999999));
#53137=CARTESIAN_POINT('',(0.64988623877797,0.0121604542276944,0.39));
#53138=CARTESIAN_POINT('',(0.63,0.,0.0499999999999999));
#53139=CARTESIAN_POINT('Origin',(0.659527189490328,0.,0.0499999999999999));
#53140=CARTESIAN_POINT('Origin',(0.,0.,0.0499999999999999));
#53141=CARTESIAN_POINT('Origin',(-0.684856844632512,-0.0840898469495517,
0.75));
#53142=CARTESIAN_POINT('',(-0.642124647240729,-0.100875851451027,0.0499999999999999));
#53143=CARTESIAN_POINT('',(-0.642124647240729,-0.100875851451027,0.75));
#53144=CARTESIAN_POINT('',(-0.642124647240729,-0.100875851451027,0.39));
#53145=CARTESIAN_POINT('',(-0.620428884397691,-0.109398351930166,0.0499999999999999));
#53146=CARTESIAN_POINT('',(-0.684856844632512,-0.0840898469495517,0.0499999999999999));
#53147=CARTESIAN_POINT('',(-0.620428884397691,-0.109398351930166,0.75));
#53148=CARTESIAN_POINT('',(-0.620428884397691,-0.109398351930166,0.75));
#53149=CARTESIAN_POINT('',(-0.684856844632512,-0.0840898469495517,0.75));
#53150=CARTESIAN_POINT('Origin',(-0.652642864515102,-0.119653037223409,
0.75));
#53151=CARTESIAN_POINT('',(-0.637901365808246,-0.124827270658193,0.75));
#53152=CARTESIAN_POINT('Origin',(0.,0.,0.75));
#53153=CARTESIAN_POINT('',(-0.620428884397691,-0.109398351930166,0.75));
#53154=CARTESIAN_POINT('Origin',(-0.620428884397691,-0.109398351930166,
0.75));
#53155=CARTESIAN_POINT('',(-0.637901365808246,-0.124827270658193,0.0499999999999999));
#53156=CARTESIAN_POINT('',(-0.637901365808246,-0.124827270658193,0.39));
#53157=CARTESIAN_POINT('',(-0.620428884397691,-0.109398351930166,0.0499999999999999));
#53158=CARTESIAN_POINT('Origin',(-0.652642864515102,-0.119653037223409,
0.0499999999999999));
#53159=CARTESIAN_POINT('Origin',(0.,0.,0.0499999999999999));
#53160=CARTESIAN_POINT('Origin',(-0.614794501689974,-0.313253444820287,
0.75));
#53161=CARTESIAN_POINT('',(-0.568898219465488,-0.314411857106244,0.0499999999999999));
#53162=CARTESIAN_POINT('',(-0.568898219465488,-0.314411857106244,0.75));
#53163=CARTESIAN_POINT('',(-0.568898219465488,-0.314411857106244,0.39));
#53164=CARTESIAN_POINT('',(-0.545596004384196,-0.315,0.0499999999999999));
#53165=CARTESIAN_POINT('',(-0.614794501689974,-0.313253444820287,0.0499999999999999));
#53166=CARTESIAN_POINT('',(-0.545596004384196,-0.315,0.75));
#53167=CARTESIAN_POINT('',(-0.545596004384196,-0.315,0.75));
#53168=CARTESIAN_POINT('',(-0.614794501689974,-0.313253444820287,0.75));
#53169=CARTESIAN_POINT('Origin',(-0.580195253037085,-0.344527189490328,
0.75));
#53170=CARTESIAN_POINT('',(-0.556737765237794,-0.335474381671726,0.75));
#53171=CARTESIAN_POINT('Origin',(0.,0.,0.75));
#53172=CARTESIAN_POINT('',(-0.545596004384196,-0.315,0.75));
#53173=CARTESIAN_POINT('Origin',(-0.545596004384196,-0.315,0.75));
#53174=CARTESIAN_POINT('',(-0.556737765237794,-0.335474381671726,0.0499999999999999));
#53175=CARTESIAN_POINT('',(-0.556737765237794,-0.335474381671726,0.39));
#53176=CARTESIAN_POINT('',(-0.545596004384196,-0.315,0.0499999999999999));
#53177=CARTESIAN_POINT('Origin',(-0.580195253037085,-0.344527189490328,
0.0499999999999999));
#53178=CARTESIAN_POINT('Origin',(0.,0.,0.0499999999999999));
#53179=CARTESIAN_POINT('Origin',(-0.470578868443124,-0.504634054117228,
0.75));
#53180=CARTESIAN_POINT('',(-0.427054270379195,-0.490025152569635,0.0499999999999999));
#53181=CARTESIAN_POINT('',(-0.427054270379195,-0.490025152569635,0.75));
#53182=CARTESIAN_POINT('',(-0.427054270379195,-0.490025152569635,0.39));
#53183=CARTESIAN_POINT('',(-0.40495619410252,-0.482607999164956,0.0499999999999999));
#53184=CARTESIAN_POINT('',(-0.470578868443124,-0.504634054117228,0.0499999999999999));
#53185=CARTESIAN_POINT('',(-0.40495619410252,-0.482607999164956,0.75));
#53186=CARTESIAN_POINT('',(-0.40495619410252,-0.482607999164956,0.75));
#53187=CARTESIAN_POINT('',(-0.470578868443124,-0.504634054117228,0.75));
#53188=CARTESIAN_POINT('Origin',(-0.437767531272822,-0.516833250548794,
0.75));
#53189=CARTESIAN_POINT('',(-0.408423373605339,-0.505658331181079,0.75));
#53190=CARTESIAN_POINT('Origin',(0.,0.,0.75));
#53191=CARTESIAN_POINT('',(-0.40495619410252,-0.482607999164956,0.75));
#53192=CARTESIAN_POINT('Origin',(-0.40495619410252,-0.482607999164956,0.75));
#53193=CARTESIAN_POINT('',(-0.408423373605339,-0.505658331181079,0.0499999999999999));
#53194=CARTESIAN_POINT('',(-0.408423373605339,-0.505658331181079,0.39));
#53195=CARTESIAN_POINT('',(-0.40495619410252,-0.482607999164956,0.0499999999999999));
#53196=CARTESIAN_POINT('Origin',(-0.437767531272822,-0.516833250548794,
0.0499999999999999));
#53197=CARTESIAN_POINT('Origin',(0.,0.,0.0499999999999999));
#53198=CARTESIAN_POINT('Origin',(-0.269604478657599,-0.635148348882184,
0.75));
#53199=CARTESIAN_POINT('',(-0.23370127363539,-0.606534182632106,0.0499999999999999));
#53200=CARTESIAN_POINT('',(-0.23370127363539,-0.606534182632106,0.75));
#53201=CARTESIAN_POINT('',(-0.23370127363539,-0.606534182632106,0.39));
#53202=CARTESIAN_POINT('',(-0.215472690295171,-0.592006351095122,0.0499999999999999));
#53203=CARTESIAN_POINT('',(-0.269604478657599,-0.635148348882184,0.0499999999999999));
#53204=CARTESIAN_POINT('',(-0.215472690295171,-0.592006351095122,0.75));
#53205=CARTESIAN_POINT('',(-0.215472690295171,-0.592006351095122,0.75));
#53206=CARTESIAN_POINT('',(-0.269604478657599,-0.635148348882184,0.75));
#53207=CARTESIAN_POINT('Origin',(-0.235670477458144,-0.625928316354808,
0.75));
#53208=CARTESIAN_POINT('',(-0.210847095429052,-0.614852423227828,0.75));
#53209=CARTESIAN_POINT('Origin',(0.,0.,0.75));
#53210=CARTESIAN_POINT('',(-0.215472690295171,-0.592006351095122,0.75));
#53211=CARTESIAN_POINT('Origin',(-0.215472690295171,-0.592006351095122,
0.75));
#53212=CARTESIAN_POINT('',(-0.210847095429052,-0.614852423227828,0.0499999999999999));
#53213=CARTESIAN_POINT('',(-0.210847095429052,-0.614852423227828,0.39));
#53214=CARTESIAN_POINT('',(-0.215472690295171,-0.592006351095122,0.0499999999999999));
#53215=CARTESIAN_POINT('Origin',(-0.235670477458144,-0.625928316354808,
0.0499999999999999));
#53216=CARTESIAN_POINT('Origin',(0.,0.,0.0499999999999999));
#53217=CARTESIAN_POINT('Origin',(-0.0361118098076316,-0.689054378980656,
0.75));
#53218=CARTESIAN_POINT('',(-0.0121604542276945,-0.64988623877797,0.0499999999999999));
#53219=CARTESIAN_POINT('',(-0.0121604542276945,-0.64988623877797,0.75));
#53220=CARTESIAN_POINT('',(-0.0121604542276945,-0.64988623877797,0.39));
#53221=CARTESIAN_POINT('',(-1.15729122519425E-16,-0.63,0.0499999999999999));
#53222=CARTESIAN_POINT('',(-0.0361118098076316,-0.689054378980656,0.0499999999999999));
#53223=CARTESIAN_POINT('',(-1.15729122519425E-16,-0.63,0.75));
#53224=CARTESIAN_POINT('',(-1.15729122519425E-16,-0.63,0.75));
#53225=CARTESIAN_POINT('',(-0.0361118098076316,-0.689054378980656,0.75));
#53226=CARTESIAN_POINT('Origin',(-1.2490009027033E-16,-0.659527189490328,
0.75));
#53227=CARTESIAN_POINT('',(0.0121604542276944,-0.64988623877797,0.75));
#53228=CARTESIAN_POINT('Origin',(0.,0.,0.75));
#53229=CARTESIAN_POINT('',(-1.15729122519425E-16,-0.63,0.75));
#53230=CARTESIAN_POINT('Origin',(-1.15729122519425E-16,-0.63,0.75));
#53231=CARTESIAN_POINT('',(0.0121604542276944,-0.64988623877797,0.0499999999999999));
#53232=CARTESIAN_POINT('',(0.0121604542276944,-0.64988623877797,0.39));
#53233=CARTESIAN_POINT('',(-1.15729122519425E-16,-0.63,0.0499999999999999));
#53234=CARTESIAN_POINT('Origin',(-1.2490009027033E-16,-0.659527189490328,
0.0499999999999999));
#53235=CARTESIAN_POINT('Origin',(0.,0.,0.0499999999999999));
#53236=CARTESIAN_POINT('Origin',(0.201736476258688,-0.659850281614495,0.75));
#53237=CARTESIAN_POINT('',(0.210847095429052,-0.614852423227828,0.0499999999999999));
#53238=CARTESIAN_POINT('',(0.210847095429052,-0.614852423227828,0.75));
#53239=CARTESIAN_POINT('',(0.210847095429052,-0.614852423227828,0.39));
#53240=CARTESIAN_POINT('',(0.215472690295171,-0.592006351095122,0.0499999999999999));
#53241=CARTESIAN_POINT('',(0.201736476258688,-0.659850281614495,0.0499999999999999));
#53242=CARTESIAN_POINT('',(0.215472690295171,-0.592006351095122,0.75));
#53243=CARTESIAN_POINT('',(0.215472690295171,-0.592006351095122,0.75));
#53244=CARTESIAN_POINT('',(0.201736476258688,-0.659850281614495,0.75));
#53245=CARTESIAN_POINT('Origin',(0.235670477458144,-0.625928316354808,0.75));
#53246=CARTESIAN_POINT('',(0.23370127363539,-0.606534182632106,0.75));
#53247=CARTESIAN_POINT('Origin',(0.,0.,0.75));
#53248=CARTESIAN_POINT('',(0.215472690295171,-0.592006351095122,0.75));
#53249=CARTESIAN_POINT('Origin',(0.215472690295171,-0.592006351095122,0.75));
#53250=CARTESIAN_POINT('',(0.23370127363539,-0.606534182632106,0.0499999999999999));
#53251=CARTESIAN_POINT('',(0.23370127363539,-0.606534182632106,0.39));
#53252=CARTESIAN_POINT('',(0.215472690295171,-0.592006351095122,0.0499999999999999));
#53253=CARTESIAN_POINT('Origin',(0.235670477458144,-0.625928316354808,0.0499999999999999));
#53254=CARTESIAN_POINT('Origin',(0.,0.,0.0499999999999999));
#53255=CARTESIAN_POINT('Origin',(0.415252365974913,-0.551058501932632,0.75));
#53256=CARTESIAN_POINT('',(0.408423373605339,-0.505658331181079,0.0499999999999999));
#53257=CARTESIAN_POINT('',(0.408423373605339,-0.505658331181079,0.75));
#53258=CARTESIAN_POINT('',(0.408423373605339,-0.505658331181079,0.39));
#53259=CARTESIAN_POINT('',(0.40495619410252,-0.482607999164956,0.0499999999999999));
#53260=CARTESIAN_POINT('',(0.415252365974913,-0.551058501932632,0.0499999999999999));
#53261=CARTESIAN_POINT('',(0.40495619410252,-0.482607999164956,0.75));
#53262=CARTESIAN_POINT('',(0.40495619410252,-0.482607999164956,0.75));
#53263=CARTESIAN_POINT('',(0.415252365974913,-0.551058501932632,0.75));
#53264=CARTESIAN_POINT('Origin',(0.437767531272822,-0.516833250548794,0.75));
#53265=CARTESIAN_POINT('',(0.427054270379194,-0.490025152569635,0.75));
#53266=CARTESIAN_POINT('Origin',(0.,0.,0.75));
#53267=CARTESIAN_POINT('',(0.40495619410252,-0.482607999164956,0.75));
#53268=CARTESIAN_POINT('Origin',(0.40495619410252,-0.482607999164956,0.75));
#53269=CARTESIAN_POINT('',(0.427054270379194,-0.490025152569635,0.0499999999999999));
#53270=CARTESIAN_POINT('',(0.427054270379194,-0.490025152569635,0.39));
#53271=CARTESIAN_POINT('',(0.40495619410252,-0.482607999164956,0.0499999999999999));
#53272=CARTESIAN_POINT('Origin',(0.437767531272822,-0.516833250548794,0.0499999999999999));
#53273=CARTESIAN_POINT('Origin',(0.,0.,0.0499999999999999));
#53274=CARTESIAN_POINT('Origin',(0.578682691882343,-0.375800934160369,0.75));
#53275=CARTESIAN_POINT('',(0.556737765237794,-0.335474381671726,0.0499999999999999));
#53276=CARTESIAN_POINT('',(0.556737765237794,-0.335474381671726,0.75));
#53277=CARTESIAN_POINT('',(0.556737765237794,-0.335474381671726,0.39));
#53278=CARTESIAN_POINT('',(0.545596004384196,-0.315,0.0499999999999999));
#53279=CARTESIAN_POINT('',(0.578682691882343,-0.375800934160369,0.0499999999999999));
#53280=CARTESIAN_POINT('',(0.545596004384196,-0.315,0.75));
#53281=CARTESIAN_POINT('',(0.545596004384196,-0.315,0.75));
#53282=CARTESIAN_POINT('',(0.578682691882343,-0.375800934160369,0.75));
#53283=CARTESIAN_POINT('Origin',(0.580195253037085,-0.344527189490328,0.75));
#53284=CARTESIAN_POINT('',(0.568898219465488,-0.314411857106244,0.75));
#53285=CARTESIAN_POINT('Origin',(0.,0.,0.75));
#53286=CARTESIAN_POINT('',(0.545596004384196,-0.315,0.75));
#53287=CARTESIAN_POINT('Origin',(0.545596004384196,-0.315,0.75));
#53288=CARTESIAN_POINT('',(0.568898219465488,-0.314411857106244,0.0499999999999999));
#53289=CARTESIAN_POINT('',(0.568898219465488,-0.314411857106244,0.39));
#53290=CARTESIAN_POINT('',(0.545596004384196,-0.315,0.0499999999999999));
#53291=CARTESIAN_POINT('Origin',(0.580195253037085,-0.344527189490328,0.0499999999999999));
#53292=CARTESIAN_POINT('Origin',(0.,0.,0.0499999999999999));
#53293=CARTESIAN_POINT('Origin',(0.672315344701812,-0.155216227497267,0.75));
#53294=CARTESIAN_POINT('',(0.637901365808246,-0.124827270658194,0.0499999999999999));
#53295=CARTESIAN_POINT('',(0.637901365808246,-0.124827270658194,0.75));
#53296=CARTESIAN_POINT('',(0.637901365808246,-0.124827270658194,0.39));
#53297=CARTESIAN_POINT('',(0.620428884397691,-0.109398351930166,0.0499999999999999));
#53298=CARTESIAN_POINT('',(0.672315344701812,-0.155216227497267,0.0499999999999999));
#53299=CARTESIAN_POINT('',(0.620428884397691,-0.109398351930166,0.75));
#53300=CARTESIAN_POINT('',(0.620428884397691,-0.109398351930166,0.75));
#53301=CARTESIAN_POINT('',(0.672315344701812,-0.155216227497267,0.75));
#53302=CARTESIAN_POINT('Origin',(0.652642864515102,-0.119653037223409,0.75));
#53303=CARTESIAN_POINT('',(0.642124647240729,-0.100875851451027,0.75));
#53304=CARTESIAN_POINT('Origin',(0.,0.,0.75));
#53305=CARTESIAN_POINT('',(0.620428884397691,-0.109398351930166,0.75));
#53306=CARTESIAN_POINT('Origin',(0.620428884397691,-0.109398351930166,0.75));
#53307=CARTESIAN_POINT('',(0.642124647240729,-0.100875851451027,0.0499999999999999));
#53308=CARTESIAN_POINT('',(0.642124647240729,-0.100875851451027,0.39));
#53309=CARTESIAN_POINT('',(0.620428884397691,-0.109398351930166,0.0499999999999999));
#53310=CARTESIAN_POINT('Origin',(0.652642864515102,-0.119653037223409,0.0499999999999999));
#53311=CARTESIAN_POINT('Origin',(0.,0.,0.0499999999999999));
#53312=CARTESIAN_POINT('Origin',(0.35,0.,-2.));
#53313=CARTESIAN_POINT('',(-0.35,-4.28626379701574E-17,-2.));
#53314=CARTESIAN_POINT('Origin',(0.,0.,-2.));
#53315=CARTESIAN_POINT('Origin',(0.,0.,-1.975));
#53316=CARTESIAN_POINT('',(-0.375,-4.59242549680257E-17,-1.975));
#53317=CARTESIAN_POINT('Origin',(0.,0.,0.015));
#53318=CARTESIAN_POINT('',(-0.65,-7.9602041944578E-17,0.03));
#53319=CARTESIAN_POINT('Origin',(0.,0.,0.03));
#53320=CARTESIAN_POINT('',(-0.635,-7.77650717458569E-17,0.015));
#53321=CARTESIAN_POINT('Origin',(0.,0.,0.39));
#53322=CARTESIAN_POINT('Origin',(0.,0.,0.75));
#53323=CARTESIAN_POINT('Origin',(0.,0.,0.75));
#53324=CARTESIAN_POINT('Origin',(0.,0.,0.75));
#53325=CARTESIAN_POINT('Origin',(0.,0.,0.75));
#53326=CARTESIAN_POINT('Origin',(0.,0.,0.75));
#53327=CARTESIAN_POINT('Origin',(0.,0.,0.75));
#53328=CARTESIAN_POINT('Origin',(0.,0.,0.75));
#53329=CARTESIAN_POINT('Origin',(0.,0.,0.75));
#53330=CARTESIAN_POINT('Origin',(0.,0.,0.75));
#53331=CARTESIAN_POINT('Origin',(0.,0.,0.75));
#53332=CARTESIAN_POINT('Origin',(0.,0.,0.75));
#53333=CARTESIAN_POINT('Origin',(0.,0.,0.75));
#53334=CARTESIAN_POINT('Origin',(0.,0.,0.75));
#53335=CARTESIAN_POINT('Origin',(0.,0.,0.75));
#53336=CARTESIAN_POINT('Origin',(0.,0.,0.75));
#53337=CARTESIAN_POINT('Origin',(0.,0.,0.75));
#53338=CARTESIAN_POINT('',(-0.65,-7.9602041944578E-17,0.39));
#53339=CARTESIAN_POINT('Origin',(0.,0.,0.75));
#53340=CARTESIAN_POINT('Origin',(0.,0.,0.75));
#53341=CARTESIAN_POINT('Origin',(0.,0.,0.75));
#53342=CARTESIAN_POINT('Origin',(0.,0.,0.75));
#53343=CARTESIAN_POINT('Origin',(0.,0.,0.75));
#53344=CARTESIAN_POINT('Origin',(0.,0.,0.75));
#53345=CARTESIAN_POINT('Origin',(0.,0.,0.75));
#53346=CARTESIAN_POINT('Origin',(0.,0.,0.75));
#53347=CARTESIAN_POINT('Origin',(0.,0.,0.75));
#53348=CARTESIAN_POINT('Origin',(0.,0.,0.75));
#53349=CARTESIAN_POINT('Origin',(0.,0.,0.75));
#53350=CARTESIAN_POINT('Origin',(0.,0.,0.75));
#53351=CARTESIAN_POINT('Origin',(0.,0.,0.75));
#53352=CARTESIAN_POINT('Origin',(0.,0.,0.75));
#53353=CARTESIAN_POINT('Origin',(0.,0.,0.75));
#53354=CARTESIAN_POINT('Origin',(0.,0.,0.75));
#53355=CARTESIAN_POINT('Origin',(0.,0.,0.75));
#53356=CARTESIAN_POINT('Origin',(0.,0.,0.75));
#53357=CARTESIAN_POINT('Origin',(0.,0.,0.75));
#53358=CARTESIAN_POINT('Origin',(0.,0.,0.75));
#53359=CARTESIAN_POINT('Origin',(0.,0.,0.775));
#53360=CARTESIAN_POINT('',(-0.6,-7.34788079488412E-17,0.8));
#53361=CARTESIAN_POINT('Origin',(0.,0.,0.8));
#53362=CARTESIAN_POINT('',(-0.625,-7.65404249467096E-17,0.775));
#53363=CARTESIAN_POINT('Origin',(0.,0.,0.8));
#76626=UNCERTAINTY_MEASURE_WITH_UNIT(LENGTH_MEASURE(0.001),#76661,
'DISTANCE_ACCURACY_VALUE',
'Maximum model space distance between geometric entities at asserted c
onnectivities');
#76638=UNCERTAINTY_MEASURE_WITH_UNIT(LENGTH_MEASURE(0.001),#76661,
'DISTANCE_ACCURACY_VALUE',
'Maximum model space distance between geometric entities at asserted c
onnectivities');
#76648=(
GEOMETRIC_REPRESENTATION_CONTEXT(3)
GLOBAL_UNCERTAINTY_ASSIGNED_CONTEXT((#76626))
GLOBAL_UNIT_ASSIGNED_CONTEXT((#76661,#76663,#76664))
REPRESENTATION_CONTEXT('','3D')
);
#76660=(
GEOMETRIC_REPRESENTATION_CONTEXT(3)
GLOBAL_UNCERTAINTY_ASSIGNED_CONTEXT((#76638))
GLOBAL_UNIT_ASSIGNED_CONTEXT((#76661,#76663,#76664))
REPRESENTATION_CONTEXT('','3D')
);
#76661=(
LENGTH_UNIT()
NAMED_UNIT(*)
SI_UNIT(.CENTI.,.METRE.)
);
#76663=(
NAMED_UNIT(*)
PLANE_ANGLE_UNIT()
SI_UNIT($,.RADIAN.)
);
#76664=(
NAMED_UNIT(*)
SI_UNIT($,.STERADIAN.)
SOLID_ANGLE_UNIT()
);
#76674=SHAPE_DEFINITION_REPRESENTATION(#76695,#76744);
#76695=PRODUCT_DEFINITION_SHAPE('',$,#76766);
#76744=SHAPE_REPRESENTATION('',(#27875),#76648);
#76756=PRODUCT_DEFINITION_CONTEXT('part definition',#76821,'design');
#76766=PRODUCT_DEFINITION('2026-10-26-11-13-05-542',
'10_Handwheel_Lock_Screw_ISO_4762_M8x20',#76787,#76756);
#76787=PRODUCT_DEFINITION_FORMATION('',$,#76832);
#76821=APPLICATION_CONTEXT(
'Core Data for Automotive Mechanical Design Process');
#76822=PRODUCT_CONTEXT('part definition',#76821,'mechanical');
#76832=PRODUCT('2026-10-26-11-13-05-542',
'10_Handwheel_Lock_Screw_ISO_4762_M8x20',$,(#76822));
#76907=COLOUR_RGB('Black',0.12,0.14,0.17);
#76908=FILL_AREA_STYLE_COLOUR('',#76907);
#76909=FILL_AREA_STYLE('',(#76908));
#76910=SURFACE_STYLE_FILL_AREA(#76909);
#76911=SURFACE_SIDE_STYLE('',(#76910));
#76912=SURFACE_STYLE_USAGE(.BOTH.,#76911);
#76913=PRESENTATION_STYLE_ASSIGNMENT((#76912));
ENDSEC;
END-ISO-10303-21;
